ISO-10303-21;
HEADER;
FILE_DESCRIPTION (('STEP AP214'),
    '1' );
FILE_NAME ('Pulley.step',
    '2026-10-12T23:53:07',
    ( '' ),
    ( '' ),
    'SwSTEP 2.0',
    'SolidWorks 2024',
    '' );
FILE_SCHEMA (( 'AUTOMOTIVE_DESIGN' ));
ENDSEC;

DATA;
#7=CARTESIAN_POINT ( 'NONE',  ( 0.01548846960707511190, -0.5198120922912051745, -0.07362328916749329155 ) ) ;
#29=CARTESIAN_POINT ( 'NONE',  ( -0.01548846960707524721, 0.000000000000000000, 0.000000000000000000 ) ) ;
#36=LINE ( 'NONE', #30842, #35705 ) ;
#41=ORIENTED_EDGE ( 'NONE', *, *, #38593, .T. ) ;
#45=CARTESIAN_POINT ( 'NONE',  ( -0.03650581953630592513, -0.4542932396444835375, -0.2355374485430490328 ) ) ;
#49=EDGE_LOOP ( 'NONE', ( #33530, #28150, #39778, #7630 ) ) ;
#58=ORIENTED_EDGE ( 'NONE', *, *, #32260, .T. ) ;
#59=FACE_OUTER_BOUND ( 'NONE', #105, .T. ) ;
#62=DIRECTION ( 'NONE',  ( 0.3468893892380631727, 0.9373665302208734618, -0.03180785525186744650 ) ) ;
#68=FACE_OUTER_BOUND ( 'NONE', #7963, .T. ) ;
#79=AXIS2_PLACEMENT_3D ( 'NONE', #37935, #9745, #19216 ) ;
#80=CARTESIAN_POINT ( 'NONE',  ( -0.04157143636675594833, 0.4416880288200871196, 0.1614235308635322275 ) ) ;
#85=FACE_OUTER_BOUND ( 'NONE', #18714, .T. ) ;
#93=DIRECTION ( 'NONE',  ( 0.000000000000000000, 0.9510565162951657436, 0.3090169943749095927 ) ) ;
#97=CIRCLE ( 'NONE', #11204, 0.5399999999999999245 ) ;
#105=EDGE_LOOP ( 'NONE', ( #14125, #9497, #24205 ) ) ;
#120=CARTESIAN_POINT ( 'NONE',  ( -0.04762200653274516887, 0.04294689284307845467, 0.4802757286815055315 ) ) ;
#124=DIRECTION ( 'NONE',  ( -1.000000000000000000, -2.341930812374887555E-31, 1.664003471950578127E-31 ) ) ;
#128=EDGE_CURVE ( 'NONE', #3309, #37479, #16156, .T. ) ;
#131=ORIENTED_EDGE ( 'NONE', *, *, #7728, .F. ) ;
#139=CARTESIAN_POINT ( 'NONE',  ( 0.05491348488830435220, 0.4316112672892343238, 0.1667783590291176121 ) ) ;
#141=CARTESIAN_POINT ( 'NONE',  ( 0.04762035657658141713, -0.2475516194925235502, -0.4138014489398372242 ) ) ;
#156=CARTESIAN_POINT ( 'NONE',  ( -0.04574984450155351878, 0.3363984555176486313, -0.3523422282978309616 ) ) ;
#166=DIRECTION ( 'NONE',  ( -1.000000000000000000, -2.280301054154495132E-31, 1.664003471950577689E-31 ) ) ;
#168=CARTESIAN_POINT ( 'NONE',  ( -0.05279185365593578455, 0.2420570131477374765, 0.4010466975930304101 ) ) ;
#186=EDGE_LOOP ( 'NONE', ( #31291, #14570, #23539, #27301 ) ) ;
#193=CARTESIAN_POINT ( 'NONE',  ( 0.04047170147977072197, 0.2415774042519071296, -0.4392095914548690416 ) ) ;
#215=CARTESIAN_POINT ( 'NONE',  ( 0.01548846960707511190, 0.09061086148575973886, 0.5171215251571029681 ) ) ;
#245=CARTESIAN_POINT ( 'NONE',  ( -0.03309057659885150660, -0.5154121718708730704, -0.07470590733143653295 ) ) ;
#263=LINE ( 'NONE', #2895, #2757 ) ;
#266=CYLINDRICAL_SURFACE ( 'NONE', #14545, 0.08139150547213670761 ) ;
#269=CARTESIAN_POINT ( 'NONE',  ( 0.1499999999999994671, 0.3880410510314737382, -0.3755318131855000519 ) ) ;
#278=DIRECTION ( 'NONE',  ( 0.000000000000000000, -3.330669073875469621E-16, -1.000000000000000000 ) ) ;
#289=CARTESIAN_POINT ( 'NONE',  ( -0.05268932808080252495, 0.4428506128075219150, 0.1535014714534106983 ) ) ;
#291=AXIS2_PLACEMENT_3D ( 'NONE', #15248, #34163, #18534 ) ;
#294=EDGE_LOOP ( 'NONE', ( #20612, #17660, #15719, #33560 ) ) ;
#300=ORIENTED_EDGE ( 'NONE', *, *, #29321, .T. ) ;
#335=CARTESIAN_POINT ( 'NONE',  ( -0.04085667396267392976, -0.02117046819984700137, 0.4712948116111314589 ) ) ;
#347=CARTESIAN_POINT ( 'NONE',  ( -0.01548846960707531660, -0.2306506793134033284, 0.4716198300880330985 ) ) ;
#349=EDGE_LOOP ( 'NONE', ( #38087, #24896, #35519, #8395 ) ) ;
#350=DIRECTION ( 'NONE',  ( 1.664003471950577032E-31, 3.330669073875470607E-16, 1.000000000000000000 ) ) ;
#374=CARTESIAN_POINT ( 'NONE',  ( -0.03654364704248851820, 0.3642884434513001812, 0.3592365245254293682 ) ) ;
#383=VECTOR ( 'NONE', #13117, 39.37007874015748143 ) ;
#388=CARTESIAN_POINT ( 'NONE',  ( 0.05279755784604305002, 0.4315508301037734862, -0.1821553064136585964 ) ) ;
#391=ADVANCED_FACE ( 'NONE', ( #29743 ), #11571, .T. ) ;
#392=CARTESIAN_POINT ( 'NONE',  ( 0.02231181081520647314, 0.2417894035777236605, -0.4519954025055041846 ) ) ;
#409=SPHERICAL_SURFACE ( 'NONE', #10121, 0.01499999999999999944 ) ;
#423=ORIENTED_EDGE ( 'NONE', *, *, #13770, .T. ) ;
#431=CARTESIAN_POINT ( 'NONE',  ( 0.1499999999999994948, 0.2306506793134049660, -0.4716198300880325434 ) ) ;
#437=AXIS2_PLACEMENT_3D ( 'NONE', #21342, #24418, #27501 ) ;
#441=SPHERICAL_SURFACE ( 'NONE', #7998, 0.01499999999999999944 ) ;
#455=DIRECTION ( 'NONE',  ( 0.000000000000000000, 3.330669073875469621E-16, 1.000000000000000000 ) ) ;
#460=ORIENTED_EDGE ( 'NONE', *, *, #16592, .T. ) ;
#462=CARTESIAN_POINT ( 'NONE',  ( -0.04582889109739221589, -0.4790149006698679046, -0.08746027838083869632 ) ) ;
#464=DIRECTION ( 'NONE',  ( 0.000000000000000000, -0.5877852522924817968, -0.8090169943749412340 ) ) ;
#472=CARTESIAN_POINT ( 'NONE',  ( -0.02869712619511769966, -0.4519224903895721068, 0.2102851490355757691 ) ) ;
#482=CARTESIAN_POINT ( 'NONE',  ( -0.05078493045284376145, -0.4330747843660891494, 0.1920285438095919728 ) ) ;
#493=AXIS2_PLACEMENT_3D ( 'NONE', #36564, #2611, #5267 ) ;
#500=EDGE_CURVE ( 'NONE', #40212, #36370, #23396, .T. ) ;
#501=DIRECTION ( 'NONE',  ( 0.000000000000000000, -0.7185945389471800615, 0.6954292836768448671 ) ) ;
#502=CARTESIAN_POINT ( 'NONE',  ( -0.03875673594170897518, 0.4622647171927845577, 0.1151965740700969104 ) ) ;
#503=CARTESIAN_POINT ( 'NONE',  ( 0.01548846960721238578, 0.07651041855108486889, -0.5222379212565272377 ) ) ;
#518=ORIENTED_EDGE ( 'NONE', *, *, #17003, .T. ) ;
#524=DIRECTION ( 'NONE',  ( 0.000000000000000000, -0.5877852522924708056, 0.8090169943749491166 ) ) ;
#534=CARTESIAN_POINT ( 'NONE',  ( 0.05562144613422553147, -0.4441896308501024349, 0.1229845283801415390 ) ) ;
#543=CARTESIAN_POINT ( 'NONE',  ( -0.02231181081520762152, 0.5045902076536090686, -0.09028112709016213044 ) ) ;
#544=CARTESIAN_POINT ( 'NONE',  ( -0.03301200226531592757, 0.08829440931815854543, 0.5134711413293278071 ) ) ;
#559=CARTESIAN_POINT ( 'NONE',  ( 0.04140212552917706818, 0.4420250499596288241, 0.1614397576335226681 ) ) ;
#577=CARTESIAN_POINT ( 'NONE',  ( -0.05082303569918707187, 0.2375724430107450658, 0.4097459652473644520 ) ) ;
#579=CYLINDRICAL_SURFACE ( 'NONE', #19254, 0.01500000000000003934 ) ;
#580=DIRECTION ( 'NONE',  ( 1.000000000000000000, 0.000000000000000000, 0.000000000000000000 ) ) ;
#586=CARTESIAN_POINT ( 'NONE',  ( 0.05634402396114631534, 0.4396062797411924294, -0.1319984305213748876 ) ) ;
#589=CARTESIAN_POINT ( 'NONE',  ( 0.03158843595483473710, -0.05459869295505930670, 0.4890616322892847312 ) ) ;
#592=DIRECTION ( 'NONE',  ( -1.000000000000000000, -2.280301054154496446E-31, -1.355854680848613603E-31 ) ) ;
#594=DIRECTION ( 'NONE',  ( 0.000000000000000000, 0.9510565162951594154, -0.3090169943749291326 ) ) ;
#595=CARTESIAN_POINT ( 'NONE',  ( -0.01548846960721204577, 0.07651041855109251555, 0.5222379212565261275 ) ) ;
#597=CARTESIAN_POINT ( 'NONE',  ( -0.01548846960712817709, -0.2450655194479502419, -0.4674710490748132941 ) ) ;
#599=CARTESIAN_POINT ( 'NONE',  ( -0.01548846960707477016, 0.4638115001430989648, -0.2459753896937820483 ) ) ;
#645=CARTESIAN_POINT ( 'NONE',  ( -0.01548846960707477016, 0.4638115001430989648, -0.2459753896937820483 ) ) ;
#679=CARTESIAN_POINT ( 'NONE',  ( 0.05561310505367090401, -0.2871713500421218535, 0.3605322861779084453 ) ) ;
#685=CARTESIAN_POINT ( 'NONE',  ( -0.04230170315644025264, 0.4483301424763313503, 0.1366247710447713870 ) ) ;
#687=EDGE_CURVE ( 'NONE', #37027, #22774, #24185, .T. ) ;
#697=ORIENTED_EDGE ( 'NONE', *, *, #128, .F. ) ;
#705=ORIENTED_EDGE ( 'NONE', *, *, #4864, .T. ) ;
#708=CYLINDRICAL_SURFACE ( 'NONE', #23368, 0.01500000000000000291 ) ;
#716=AXIS2_PLACEMENT_3D ( 'NONE', #34831, #37505, #34436 ) ;
#722=DIRECTION ( 'NONE',  ( 2.532366176626905388E-12, 0.3090169943749593862, 0.9510565162951497564 ) ) ;
#738=ORIENTED_EDGE ( 'NONE', *, *, #38819, .T. ) ;
#741=CARTESIAN_POINT ( 'NONE',  ( -0.01548846960721252282, 0.3688619771570396666, 0.3775276577325177296 ) ) ;
#742=FACE_OUTER_BOUND ( 'NONE', #16658, .T. ) ;
#743=CIRCLE ( 'NONE', #36174, 0.3698489655878002824 ) ;
#745=CARTESIAN_POINT ( 'NONE',  ( 0.02881195911414546548, -0.2420394953216108425, -0.4354516087588616302 ) ) ;
#752=DIRECTION ( 'NONE',  ( 0.000000000000000000, 3.330669073875470114E-16, 1.000000000000000000 ) ) ;
#758=B_SPLINE_CURVE_WITH_KNOTS ( 'NONE', 3,
 ( #1641, #39653, #1839, #39449, #4485, #17649, #7577, #33282, #14355, #5089, #11276, #13746, #23843, #35766, #20151, #14160, #5280, #26312 ),
 .UNSPECIFIED., .F., .F.,
 ( 4, 2, 2, 2, 2, 2, 2, 2, 4 ),
 ( -0.003133633995111071054, -0.002350221109836646283, -0.001566808224562221078, -0.0007833953392877958735, 1.754598662889739202E-08, 0.0007834304312610536683, 0.001566843316535479307, 0.002350256201809904077, 0.003133669087084328848 ),
 .UNSPECIFIED. ) ;
#760=CARTESIAN_POINT ( 'NONE',  ( -0.04087116408467002249, 0.2599586249408767924, -0.3936479624527424725 ) ) ;
#785=CARTESIAN_POINT ( 'NONE',  ( -0.02235124290213240730, -0.3550643254722131714, -0.3695962758878534316 ) ) ;
#822=DIRECTION ( 'NONE',  ( -0.9378410757839559242, 0.2807814858886551468, -0.2039996905746456479 ) ) ;
#830=CIRCLE ( 'NONE', #10656, 0.01500000000000000291 ) ;
#831=CARTESIAN_POINT ( 'NONE',  ( -0.08978098643734171158, 0.000000000000000000, 0.000000000000000000 ) ) ;
#832=CARTESIAN_POINT ( 'NONE',  ( 0.04582713223189451707, -0.2312054150958140764, 0.4285473768184998589 ) ) ;
#834=EDGE_LOOP ( 'NONE', ( #36795, #19771, #24755, #38611 ) ) ;
#838=CARTESIAN_POINT ( 'NONE',  ( 0.05561176441985724722, -0.2871508736821620222, -0.3605511861568529430 ) ) ;
#852=CARTESIAN_POINT ( 'NONE',  ( -0.01548846960721259221, -0.2450655194478906784, 0.4674710490746316616 ) ) ;
#861=CARTESIAN_POINT ( 'NONE',  ( -0.02869712619511922275, -0.06034133159975870603, -0.4947855140619938918 ) ) ;
#871=CARTESIAN_POINT ( 'NONE',  ( 0.01548846960707528191, -0.09061086148585918709, 0.5171215251570857596 ) ) ;
#874=CARTESIAN_POINT ( 'NONE',  ( 0.04229974373173746999, -0.2684538943183488180, 0.3841910309322000838 ) ) ;
#876=EDGE_CURVE ( 'NONE', #33794, #23035, #20325, .T. ) ;
#878=DIRECTION ( 'NONE',  ( 1.386669559958804888E-32, 0.8983234858819696411, 0.4393346272636231564 ) ) ;
#884=CARTESIAN_POINT ( 'NONE',  ( -0.02872242845530577349, 0.5252126300208015408, 0.08844866507292889479 ) ) ;
#888=AXIS2_PLACEMENT_3D ( 'NONE', #11720, #40510, #18097 ) ;
#927=CARTESIAN_POINT ( 'NONE',  ( 0.01548846960721238578, -0.4730347584884322942, -0.2341461249027902980 ) ) ;
#933=EDGE_CURVE ( 'NONE', #13311, #30248, #7555, .T. ) ;
#937=ORIENTED_EDGE ( 'NONE', *, *, #32050, .F. ) ;
#953=CARTESIAN_POINT ( 'NONE',  ( -0.03174036153403859972, 0.5170813853140294736, -0.08825077997795674478 ) ) ;
#960=AXIS2_PLACEMENT_3D ( 'NONE', #23321, #29667, #23920 ) ;
#967=CARTESIAN_POINT ( 'NONE',  ( -0.03877220711930364633, 0.2524486846094415871, -0.4039751870151973567 ) ) ;
#976=CARTESIAN_POINT ( 'NONE',  ( 0.03875523708677772183, 0.4416911308383487667, -0.1785246905291516251 ) ) ;
#980=DIRECTION ( 'NONE',  ( -1.000000000000000000, -2.280301054154495132E-31, 1.664003471950577689E-31 ) ) ;
#988=CARTESIAN_POINT ( 'NONE',  ( -0.03650577977170611083, -0.08362514765351501678, 0.5048437183011775797 ) ) ;
#993=DIRECTION ( 'NONE',  ( 1.000000000000000000, 2.341930812374887555E-31, -1.664003471950578127E-31 ) ) ;
#997=CIRCLE ( 'NONE', #26580, 0.5302738246768102792 ) ;
#1009=AXIS2_PLACEMENT_3D ( 'NONE', #23689, #17303, #8240 ) ;
#1030=CARTESIAN_POINT ( 'NONE',  ( 0.03159140494780052905, -0.3316214887069903750, -0.3635694333040951909 ) ) ;
#1038=ADVANCED_FACE ( 'NONE', ( #4840 ), #1389, .F. ) ;
#1051=ORIENTED_EDGE ( 'NONE', *, *, #37100, .T. ) ;
#1052=DIRECTION ( 'NONE',  ( 2.682900528199994008E-31, -0.9510565162951504226, 0.3090169943749569437 ) ) ;
#1061=VERTEX_POINT ( 'NONE', #36322 ) ;
#1083=CARTESIAN_POINT ( 'NONE',  ( 0.05269111014006107319, -0.2828051265736319930, 0.3737594984297867851 ) ) ;
#1115=DIRECTION ( 'NONE',  ( 0.000000000000000000, 0.9510565162951575280, 0.3090169943749354053 ) ) ;
#1126=( CONVERSION_BASED_UNIT ( 'INCH', #10967 ) LENGTH_UNIT ( ) NAMED_UNIT ( #23398 ) );
#1128=CARTESIAN_POINT ( 'NONE',  ( 0.02869942827333409746, -0.4892109928530976037, -0.09550568247006177569 ) ) ;
#1136=DIRECTION ( 'NONE',  ( -1.000000000000000000, -2.341930812374887555E-31, 1.664003471950578127E-31 ) ) ;
#1137=VERTEX_POINT ( 'NONE', #7741 ) ;
#1140=CARTESIAN_POINT ( 'NONE',  ( -0.01548846960707504251, -0.09061086148575646371, 0.5171215251571040783 ) ) ;
#1143=DIRECTION ( 'NONE',  ( 0.000000000000000000, 0.1725921171157338008, -0.9849933812516248333 ) ) ;
#1146=ORIENTED_EDGE ( 'NONE', *, *, #3396, .T. ) ;
#1149=CARTESIAN_POINT ( 'NONE',  ( 0.02953079040095700838, -0.09152108205202422186, -0.5223162075576424090 ) ) ;
#1151=CARTESIAN_POINT ( 'NONE',  ( -0.03672309138969752362, 0.4682479968340359511, -0.1092356788912411114 ) ) ;
#1164=CARTESIAN_POINT ( 'NONE',  ( 0.01548846960707511190, 0.09061086148586082467, -0.5171215251570855376 ) ) ;
#1168=CARTESIAN_POINT ( 'NONE',  ( -0.05078493045284195040, -0.4632364064579148066, -0.09920061604309324266 ) ) ;
#1169=DIRECTION ( 'NONE',  ( 0.000000000000000000, -4.555315873022820117E-16, -1.000000000000000000 ) ) ;
#1175=EDGE_CURVE ( 'NONE', #35830, #5083, #22257, .T. ) ;
#1178=CARTESIAN_POINT ( 'NONE',  ( 0.02881408050860729403, 0.4517606495562046520, -0.2100211630561587550 ) ) ;
#1181=CARTESIAN_POINT ( 'NONE',  ( 0.02869942827333529442, 0.06034320897027924124, 0.4947801815387842250 ) ) ;
#1189=ORIENTED_EDGE ( 'NONE', *, *, #24109, .T. ) ;
#1190=CARTESIAN_POINT ( 'NONE',  ( -0.03664605387828172994, -0.3149102792626771730, -0.3635688186731564353 ) ) ;
#1192=DIRECTION ( 'NONE',  ( 1.000000000000000000, 2.341930812374887555E-31, -1.664003471950578127E-31 ) ) ;
#1195=DIRECTION ( 'NONE',  ( 4.622231866529357837E-33, -0.6954292836767063113, -0.7185945389473142875 ) ) ;
#1205=ORIENTED_EDGE ( 'NONE', *, *, #15467, .T. ) ;
#1213=CARTESIAN_POINT ( 'NONE',  ( 0.02872242845529756824, -0.5252126300208226350, 0.08844866507292684088 ) ) ;
#1219=EDGE_CURVE ( 'NONE', #37479, #23130, #40629, .T. ) ;
#1221=EDGE_CURVE ( 'NONE', #20994, #2590, #10391, .T. ) ;
#1227=CARTESIAN_POINT ( 'NONE',  ( 0.04157143636675632997, 0.2900120080285063517, 0.3701876636500653350 ) ) ;
#1230=CARTESIAN_POINT ( 'NONE',  ( -0.04293701532779588964, 0.4875995331660218923, -0.08291810260646380326 ) ) ;
#1231=( BOUNDED_SURFACE ( )  B_SPLINE_SURFACE ( 3, 2, ( 
 ( #10864, #13545, #11064 ),
 ( #23437, #11256, #32449 ),
 ( #32660, #35953, #16840 ),
 ( #10646, #23011, #23221 ),
 ( #20524, #36347, #8164 ),
 ( #17435, #1823, #14339 ),
 ( #1618, #29382, #38626 ),
 ( #1227, #29572, #32850 ),
 ( #13726, #1413, #7558 ),
 ( #35746, #4653, #26116 ),
 ( #29777, #26902, #23825 ),
 ( #14141, #32238, #10445 ),
 ( #16625, #29172, #4465 ),
 ( #7334, #17032, #26292 ),
 ( #20132, #5473, #21133 ),
 ( #5266, #8368, #39847 ),
 ( #27319, #33265, #37170 ),
 ( #24838, #5074, #8985 ) ),
 .UNSPECIFIED., .F., .F., .F. ) 
 B_SPLINE_SURFACE_WITH_KNOTS ( ( 4, 2, 2, 2, 2, 2, 2, 2, 4 ),
 ( 3, 3 ),
 ( -0.001532620576208852279, -0.0007637936630077650328, 5.033250193322322090E-06, 0.0007738601633944096770, 0.001542687076595496923, 0.002311513989796584387, 0.003080340902997671416, 0.003849167816198758880, 0.004617994729399846343 ),
 ( 0.000000000000000000, 1.000000000000000000 ),
 .UNSPECIFIED. ) 
 GEOMETRIC_REPRESENTATION_ITEM ( )  RATIONAL_B_SPLINE_SURFACE ( (
 ( 1.000000000000000000, 0.7283825911960446486, 1.000000000000000000),
 ( 1.000000000000000000, 0.7404385082113230654, 1.000000000000000000),
 ( 1.000000000000000000, 0.7521504257739481947, 1.000000000000000000),
 ( 1.000000000000000000, 0.7744497410760382561, 1.000000000000000000),
 ( 1.000000000000000000, 0.7845654757373583532, 1.000000000000000000),
 ( 1.000000000000000000, 0.8022083990892612260, 1.000000000000000000),
 ( 1.000000000000000000, 0.8094167424699770796, 1.000000000000000000),
 ( 1.000000000000000000, 0.8194491993616178638, 1.000000000000000000),
 ( 1.000000000000000000, 0.8220634900779653087, 1.000000000000000000),
 ( 1.000000000000000000, 0.8220705070824310123, 1.000000000000000000),
 ( 1.000000000000000000, 0.8194468812480258935, 1.000000000000000000),
 ( 1.000000000000000000, 0.8094220769840151375, 1.000000000000000000),
 ( 1.000000000000000000, 0.8022659121985437070, 1.000000000000000000),
 ( 1.000000000000000000, 0.7845681159035545749, 1.000000000000000000),
 ( 1.000000000000000000, 0.7744426415185606816, 1.000000000000000000),
 ( 1.000000000000000000, 0.7522890290928357926, 1.000000000000000000),
 ( 1.000000000000000000, 0.7403540167215627577, 1.000000000000000000),
 ( 1.000000000000000000, 0.7283825911960218891, 1.000000000000000000) ) ) 
 REPRESENTATION_ITEM ( '' )  SURFACE ( )  );
#1236=CARTESIAN_POINT ( 'NONE',  ( -0.05137569054208568353, -0.2953118892970992282, 0.3683837247633758305 ) ) ;
#1243=SPHERICAL_SURFACE ( 'NONE', #1597, 0.01499999999999999944 ) ;
#1250=CARTESIAN_POINT ( 'NONE',  ( 0.1499999999999994671, -0.5198120922912051745, -0.07362328916749329155 ) ) ;
#1255=DIRECTION ( 'NONE',  ( 0.000000000000000000, -0.8090169943749496717, -0.5877852522924700285 ) ) ;
#1256=ADVANCED_FACE ( 'NONE', ( #29312 ), #25828, .F. ) ;
#1260=CARTESIAN_POINT ( 'NONE',  ( -0.01548846960707517956, -0.3772621329472692908, -0.3651003739303438911 ) ) ;
#1269=CARTESIAN_POINT ( 'NONE',  ( 0.05082303569918617675, 0.4631054925596486127, 0.09932635337952074039 ) ) ;
#1288=VERTEX_POINT ( 'NONE', #22542 ) ;
#1291=ORIENTED_EDGE ( 'NONE', *, *, #15550, .T. ) ;
#1293=CARTESIAN_POINT ( 'NONE',  ( 0.05187277790672186611, 0.4419080096627359122, 0.1624279055868750321 ) ) ;
#1310=CARTESIAN_POINT ( 'NONE',  ( -0.01548846960707524721, 0.09061086148575919763, -0.5171215251571033011 ) ) ;
#1316=CARTESIAN_POINT ( 'NONE',  ( -0.06980746140711623082, 5.828670879282072084E-17, 0.1749999999999999889 ) ) ;
#1322=CARTESIAN_POINT ( 'NONE',  ( -0.01548846960721190873, 0.4730347584884290191, -0.2341461249027944058 ) ) ;
#1337=CARTESIAN_POINT ( 'NONE',  ( -0.04230258372739850031, 0.4443637212174484930, -0.1488268768076315418 ) ) ;
#1352=SPHERICAL_SURFACE ( 'NONE', #37169, 0.01499999999999999944 ) ;
#1363=CARTESIAN_POINT ( 'NONE',  ( -0.05615703521555034244, -0.2616264896058714262, -0.3776298641847865012 ) ) ;
#1377=CARTESIAN_POINT ( 'NONE',  ( -0.06980746140711623082, 0.000000000000000000, 0.000000000000000000 ) ) ;
#1383=ORIENTED_EDGE ( 'NONE', *, *, #23535, .T. ) ;
#1389=CYLINDRICAL_SURFACE ( 'NONE', #5778, 0.2149999999999999967 ) ;
#1399=CARTESIAN_POINT ( 'NONE',  ( 0.01548846960707197032, -0.4730347584886857581, 0.2341461249029804237 ) ) ;
#1406=CARTESIAN_POINT ( 'NONE',  ( -0.01548846960707531660, -0.2372406987223574237, 0.4850946823762633531 ) ) ;
#1409=FACE_OUTER_BOUND ( 'NONE', #21743, .T. ) ;
#1413=CARTESIAN_POINT ( 'NONE',  ( 0.05268932808080566133, 0.2828369400135311573, 0.3737413977152168609 ) ) ;
#1424=CARTESIAN_POINT ( 'NONE',  ( -0.04762200653274045736, -0.2475542241873569527, 0.4137947767341018102 ) ) ;
#1431=CARTESIAN_POINT ( 'NONE',  ( 0.01548846960707292615, -0.2306506793133126232, -0.4716198300880852790 ) ) ;
#1440=CARTESIAN_POINT ( 'NONE',  ( -0.01548846960688914087, 0.3772621329476823493, -0.3651003739306282747 ) ) ;
#1446=EDGE_CURVE ( 'NONE', #36014, #16165, #31483, .T. ) ;
#1461=CARTESIAN_POINT ( 'NONE',  ( 0.000000000000000000, 0.000000000000000000, 0.000000000000000000 ) ) ;
#1464=TOROIDAL_SURFACE ( 'NONE', #25736, 0.5250000000000000222, 0.01499999999999999944 ) ;
#1491=EDGE_CURVE ( 'NONE', #26219, #3309, #29109, .T. ) ;
#1493=AXIS2_PLACEMENT_3D ( 'NONE', #29081, #19224, #29489 ) ;
#1510=DIRECTION ( 'NONE',  ( 0.000000000000000000, 0.9510565162951574170, 0.3090169943749355719 ) ) ;
#1530=PLANE ( 'NONE',  #2057 ) ;
#1534=ORIENTED_EDGE ( 'NONE', *, *, #8982, .T. ) ;
#1535=VERTEX_POINT ( 'NONE', #33809 ) ;
#1537=ORIENTED_EDGE ( 'NONE', *, *, #10931, .T. ) ;
#1542=CARTESIAN_POINT ( 'NONE',  ( -0.04945776359515308140, 0.4635931069071607125, -0.1136454792236678418 ) ) ;
#1548=CIRCLE ( 'NONE', #38959, 0.5302738246768106123 ) ;
#1553=ORIENTED_EDGE ( 'NONE', *, *, #33349, .F. ) ;
#1557=CARTESIAN_POINT ( 'NONE',  ( -0.03171102739523626313, 0.2433685106468593262, -0.4273977451499059166 ) ) ;
#1558=CARTESIAN_POINT ( 'NONE',  ( -0.04087116408466984208, -0.4547130927580663173, -0.1255914340181775168 ) ) ;
#1566=ORIENTED_EDGE ( 'NONE', *, *, #14670, .F. ) ;
#1569=CARTESIAN_POINT ( 'NONE',  ( -0.04140212552917830330, -0.2901315858634276323, -0.3705031754532651656 ) ) ;
#1570=VECTOR ( 'NONE', #27657, 39.37007874015748143 ) ;
#1574=CARTESIAN_POINT ( 'NONE',  ( -0.04293694706340299427, 0.07181688488226835310, -0.4893579783149998308 ) ) ;
#1575=CARTESIAN_POINT ( 'NONE',  ( -0.1399999999999997358, 7.160938508832261116E-17, 0.2149999999999999967 ) ) ;
#1578=ORIENTED_EDGE ( 'NONE', *, *, #32895, .F. ) ;
#1581=CARTESIAN_POINT ( 'NONE',  ( 0.04047170147976712068, 0.06272069502581248401, 0.4973236590858390316 ) ) ;
#1583=FACE_OUTER_BOUND ( 'NONE', #20207, .T. ) ;
#1597=AXIS2_PLACEMENT_3D ( 'NONE', #16856, #4483, #25702 ) ;
#1599=FACE_OUTER_BOUND ( 'NONE', #24496, .T. ) ;
#1603=CARTESIAN_POINT ( 'NONE',  ( 0.04157078424165398800, -0.4522175634759056373, 0.1290209392672012623 ) ) ;
#1604=VECTOR ( 'NONE', #18659, 39.37007874015748143 ) ;
#1611=CARTESIAN_POINT ( 'NONE',  ( 0.05634304521267755744, 1.092739197465705287E-15, 0.4588823192046724841 ) ) ;
#1616=CARTESIAN_POINT ( 'NONE',  ( 0.01548846960721238578, -0.2450655194478977839, -0.4674710490746283864 ) ) ;
#1618=CARTESIAN_POINT ( 'NONE',  ( 0.03875523708677762469, 0.3062771359410750294, 0.3649060648845446897 ) ) ;
#1621=CARTESIAN_POINT ( 'NONE',  ( -0.05283102792148821475, 0.4560693389104576445, -0.1064538768721981082 ) ) ;
#1624=CARTESIAN_POINT ( 'NONE',  ( -0.01548846960707517956, -0.4638115001430989648, -0.2459753896937853235 ) ) ;
#1629=CARTESIAN_POINT ( 'NONE',  ( -0.04087116408466998779, -0.2599586249408754601, 0.3936479624527436383 ) ) ;
#1639=CARTESIAN_POINT ( 'NONE',  ( 0.02953079040095519733, 0.2329676531120528360, -0.4763574306556333515 ) ) ;
#1641=CARTESIAN_POINT ( 'NONE',  ( -0.02953079040095639429, 0.4684706630666118365, 0.2484463060367366194 ) ) ;
#1668=CARTESIAN_POINT ( 'NONE',  ( 0.01548846960707524721, 0.000000000000000000, 0.000000000000000000 ) ) ;
#1671=CARTESIAN_POINT ( 'NONE',  ( 0.01548846960707524721, 0.000000000000000000, 0.000000000000000000 ) ) ;
#1682=CARTESIAN_POINT ( 'NONE',  ( 0.03868264068766629621, -0.03360988006411996798, -0.4753775160315163451 ) ) ;
#1688=AXIS2_PLACEMENT_3D ( 'NONE', #11790, #24347, #12399 ) ;
#1691=EDGE_LOOP ( 'NONE', ( #7815, #26358, #7067, #6159 ) ) ;
#1692=CIRCLE ( 'NONE', #24682, 0.2149999999999999967 ) ;
#1693=EDGE_LOOP ( 'NONE', ( #37648, #3502, #33966, #10993 ) ) ;
#1696=DIRECTION ( 'NONE',  ( 0.3468893892380782717, 0.9373665302208757932, 0.03180785525163551397 ) ) ;
#1734=EDGE_CURVE ( 'NONE', #38697, #13940, #14122, .T. ) ;
#1737=AXIS2_PLACEMENT_3D ( 'NONE', #2008, #13918, #35950 ) ;
#1739=EDGE_CURVE ( 'NONE', #13108, #10835, #35506, .T. ) ;
#1756=CARTESIAN_POINT ( 'NONE',  ( -0.03874953289575077536, 0.4622846869243777967, -0.1151793484519217925 ) ) ;
#1769=LINE ( 'NONE', #39976, #14748 ) ;
#1774=CARTESIAN_POINT ( 'NONE',  ( -0.05616044724337262289, -0.4399661196824186660, -0.1321902923858476464 ) ) ;
#1784=CARTESIAN_POINT ( 'NONE',  ( -0.04087116408467055678, -0.2940498268759209055, -0.3688792544161150766 ) ) ;
#1792=DIRECTION ( 'NONE',  ( 1.702140497302368477E-12, 0.9510565162951575280, 0.3090169943749354053 ) ) ;
#1793=LINE ( 'NONE', #29534, #34193 ) ;
#1797=CARTESIAN_POINT ( 'NONE',  ( 0.01548846960707524721, -0.09319974324249266640, -0.5318964258758781538 ) ) ;
#1799=CARTESIAN_POINT ( 'NONE',  ( -0.04582713223189553015, -0.2312054150958152143, -0.4285473768184985821 ) ) ;
#1801=DIRECTION ( 'NONE',  ( 0.000000000000000000, 1.000000000000000000, -3.330669073875470607E-16 ) ) ;
#1807=CARTESIAN_POINT ( 'NONE',  ( 0.1499999999999996614, -0.07651041855118867474, 0.5222379212568208917 ) ) ;
#1814=FACE_OUTER_BOUND ( 'NONE', #20604, .T. ) ;
#1820=CARTESIAN_POINT ( 'NONE',  ( -0.02872242845530502062, 0.2464193076120121673, 0.4721747535844850741 ) ) ;
#1821=CARTESIAN_POINT ( 'NONE',  ( 0.01548846960707524721, -0.3772621329472692908, -0.3651003739303438911 ) ) ;
#1823=CARTESIAN_POINT ( 'NONE',  ( 0.04760578872586636312, 0.3171112559587664914, 0.3633058139840091849 ) ) ;
#1826=CARTESIAN_POINT ( 'NONE',  ( -0.05083665881509060597, 0.4330284998000940577, -0.1917934360576658004 ) ) ;
#1831=CARTESIAN_POINT ( 'NONE',  ( -0.05138886601528206560, -0.2591656398409012962, 0.3946081992295803476 ) ) ;
#1834=DIRECTION ( 'NONE',  ( 0.000000000000000000, -1.000000000000000000, 3.330669073875470607E-16 ) ) ;
#1839=CARTESIAN_POINT ( 'NONE',  ( -0.03650581953630665372, 0.4542932396444838705, 0.2355374485430446752 ) ) ;
#1848=CARTESIAN_POINT ( 'NONE',  ( -0.02231181081520722254, -0.3551561381230117775, 0.3696296485972567769 ) ) ;
#1854=CARTESIAN_POINT ( 'NONE',  ( 0.04155248107635919896, 0.4416604393009538887, 0.1616214326753678820 ) ) ;
#1860=CARTESIAN_POINT ( 'NONE',  ( 0.01548846960706677829, 0.2306506793134169842, 0.4716198300880505845 ) ) ;
#1861=CARTESIAN_POINT ( 'NONE',  ( 0.04293701532779498065, 0.2295363440003037880, -0.4381116105132950023 ) ) ;
#1885=VERTEX_POINT ( 'NONE', #40016 ) ;
#1897=ORIENTED_EDGE ( 'NONE', *, *, #31877, .F. ) ;
#1910=SPHERICAL_SURFACE ( 'NONE', #38995, 0.01499999999999999944 ) ;
#1919=CARTESIAN_POINT ( 'NONE',  ( 0.04760578872586464921, -0.04300259564631973147, -0.4803138972568000153 ) ) ;
#1929=EDGE_CURVE ( 'NONE', #20340, #5616, #30164, .T. ) ;
#1932=VERTEX_POINT ( 'NONE', #17804 ) ;
#1940=CARTESIAN_POINT ( 'NONE',  ( -0.01548846960707442842, 0.4730347584886794854, -0.2341461249029804237 ) ) ;
#1948=ADVANCED_FACE ( 'NONE', ( #40219 ), #24210, .T. ) ;
#1952=CARTESIAN_POINT ( 'NONE',  ( 0.02953079040095687308, -0.4684706630666107263, -0.2484463060367401721 ) ) ;
#1964=LINE ( 'NONE', #23773, #14684 ) ;
#1968=CARTESIAN_POINT ( 'NONE',  ( -0.04047161733259861671, -0.3430572239576335503, -0.3654812350069442939 ) ) ;
#1976=DIRECTION ( 'NONE',  ( 0.000000000000000000, 2.986499936241660365E-14, -1.000000000000000000 ) ) ;
#1982=CARTESIAN_POINT ( 'NONE',  ( -0.05562144613422698863, -0.2870684680408737144, -0.3605846877396493011 ) ) ;
#2000=CARTESIAN_POINT ( 'NONE',  ( 0.04762035657658240939, -0.4700462218748481802, 0.1075639008183879169 ) ) ;
#2008=CARTESIAN_POINT ( 'NONE',  ( 0.01548846960707524721, -0.3772621329472692908, -0.3651003739303438911 ) ) ;
#2020=DIRECTION ( 'NONE',  ( -1.000000000000000000, -2.341930812374887555E-31, 1.664003471950578127E-31 ) ) ;
#2023=CARTESIAN_POINT ( 'NONE',  ( -0.03309060444528695577, 0.3730661130945406301, -0.3633899800202425312 ) ) ;
#2036=CARTESIAN_POINT ( 'NONE',  ( 0.01548846960712810944, 0.4730347584885798429, -0.2341461249029115899 ) ) ;
#2040=CARTESIAN_POINT ( 'NONE',  ( 0.01548846960721296691, 0.4730347584884322942, 0.2341461249027875779 ) ) ;
#2052=CARTESIAN_POINT ( 'NONE',  ( 0.04155248107635842181, -0.4523094957185427312, 0.1288470070525104538 ) ) ;
#2054=AXIS2_PLACEMENT_3D ( 'NONE', #1377, #26869, #7914 ) ;
#2057=AXIS2_PLACEMENT_3D ( 'NONE', #31116, #11980, #2530 ) ;
#2059=CARTESIAN_POINT ( 'NONE',  ( 0.01895494625228225788, 0.07381100255646896868, -0.5147985126481140483 ) ) ;
#2062=CARTESIAN_POINT ( 'NONE',  ( 0.1499999999999993561, 0.000000000000000000, 0.000000000000000000 ) ) ;
#2069=DIRECTION ( 'NONE',  ( 1.000000000000000000, 2.341930812374887555E-31, -1.664003471950578127E-31 ) ) ;
#2074=DIRECTION ( 'NONE',  ( 1.702140497302367467E-12, 0.9510565162951502005, -0.3090169943749580539 ) ) ;
#2096=EDGE_CURVE ( 'NONE', #33486, #31970, #31672, .T. ) ;
#2107=CARTESIAN_POINT ( 'NONE',  ( 0.05634206451479396166, -0.01034894336415755935, -0.4588844674656199496 ) ) ;
#2121=CARTESIAN_POINT ( 'NONE',  ( 0.04154009738085473469, 0.2902754972779525988, 0.3700679770908117394 ) ) ;
#2127=CARTESIAN_POINT ( 'NONE',  ( 0.01548846960721296691, 0.4730347584884322942, 0.2341461249027875779 ) ) ;
#2128=CARTESIAN_POINT ( 'NONE',  ( 0.01548846960707511190, 0.09319974324249648279, 0.5318964258758775987 ) ) ;
#2143=CARTESIAN_POINT ( 'NONE',  ( 0.04293317454820588797, -0.4432234940308283355, -0.2195257349118454882 ) ) ;
#2150=CARTESIAN_POINT ( 'NONE',  ( 0.04293701532779389124, -0.4432143466407630350, 0.2195216604697207696 ) ) ;
#2162=DIRECTION ( 'NONE',  ( 0.000000000000000000, 3.330669073875470114E-16, 1.000000000000000000 ) ) ;
#2177=CARTESIAN_POINT ( 'NONE',  ( 0.03672447062657722278, 0.04080285735492172883, 0.4790833464420496957 ) ) ;
#2178=CARTESIAN_POINT ( 'NONE',  ( 0.03647060353175650416, -0.4543627241291142149, -0.2356060312622652864 ) ) ;
#2182=CARTESIAN_POINT ( 'NONE',  ( 0.02953079040095559285, 0.5250338024619285449, 0.07436286310882497808 ) ) ;
#2184=FACE_OUTER_BOUND ( 'NONE', #27289, .T. ) ;
#2185=EDGE_LOOP ( 'NONE', ( #16379, #10385, #22146, #8192 ) ) ;
#2192=CARTESIAN_POINT ( 'NONE',  ( -0.02953079040095700838, -0.4684706630666085614, 0.2484463060367459175 ) ) ;
#2196=ORIENTED_EDGE ( 'NONE', *, *, #11512, .F. ) ;
#2202=CARTESIAN_POINT ( 'NONE',  ( -0.02235124290213187995, 0.5044963136724002206, 0.09030809412322121643 ) ) ;
#2252=CIRCLE ( 'NONE', #34417, 0.01500000000000006016 ) ;
#2254=AXIS2_PLACEMENT_3D ( 'NONE', #1860, #39471, #7601 ) ;
#2258=CARTESIAN_POINT ( 'NONE',  ( 0.03654368633476911404, 0.08356155710620580268, -0.5047517311408941110 ) ) ;
#2259=EDGE_CURVE ( 'NONE', #29592, #5283, #14910, .T. ) ;
#2262=CARTESIAN_POINT ( 'NONE',  ( 0.05634301242525762560, 0.2780425975185383813, -0.3652000572937701972 ) ) ;
#2287=VERTEX_POINT ( 'NONE', #21215 ) ;
#2288=CARTESIAN_POINT ( 'NONE',  ( 0.03664605387828134830, 0.4684681574363447343, -0.1090337349854987731 ) ) ;
#2296=EDGE_LOOP ( 'NONE', ( #9337, #21762, #2564, #18314, #37181 ) ) ;
#2323=CARTESIAN_POINT ( 'NONE',  ( 0.02881408050861685236, -0.06014027758171745092, -0.4945500181289065322 ) ) ;
#2332=DIRECTION ( 'NONE',  ( 1.000000000000000000, 3.624433060062967676E-13, -2.563064096159672774E-12 ) ) ;
#2333=ORIENTED_EDGE ( 'NONE', *, *, #3960, .F. ) ;
#2340=CARTESIAN_POINT ( 'NONE',  ( 0.1499999999999994671, 0.5230810839623357689, -0.1699593469062178064 ) ) ;
#2353=CIRCLE ( 'NONE', #25350, 0.01500000000000005496 ) ;
#2368=DIRECTION ( 'NONE',  ( -2.280301054154496008E-31, 1.000000000000000000, -2.106022274728121591E-16 ) ) ;
#2373=CARTESIAN_POINT ( 'NONE',  ( -0.05634490452572842034, -0.005064009952712422366, -0.4588782462578062660 ) ) ;
#2374=ADVANCED_FACE ( 'NONE', ( #31296 ), #40234, .T. ) ;
#2376=VERTEX_POINT ( 'NONE', #13582 ) ;
#2378=CARTESIAN_POINT ( 'NONE',  ( -0.03868649100028188209, 0.3066017772948842479, 0.3648306000529296100 ) ) ;
#2379=CARTESIAN_POINT ( 'NONE',  ( 0.03478489236950984415, -0.07228210831916198620, 0.5113624180529658947 ) ) ;
#2381=CARTESIAN_POINT ( 'NONE',  ( 0.04308611741968229603, -0.4494132222463866344, -0.2058373899768682624 ) ) ;
#2385=CARTESIAN_POINT ( 'NONE',  ( 0.04139678531769570152, 0.4525211694413215358, 0.1291682248591994320 ) ) ;
#2407=EDGE_CURVE ( 'NONE', #22774, #2376, #19949, .T. ) ;
#2408=CARTESIAN_POINT ( 'NONE',  ( 0.8248651029816849167, 0.000000000000000000, 0.000000000000000000 ) ) ;
#2410=CYLINDRICAL_SURFACE ( 'NONE', #29228, 0.5400000000000017009 ) ;
#2414=CARTESIAN_POINT ( 'NONE',  ( -0.05281452789367933193, 0.3064952470002013651, 0.3541670097232195169 ) ) ;
#2425=DIRECTION ( 'NONE',  ( -0.3468893892380657262, 0.7396492646828742856, 0.5767033179097595941 ) ) ;
#2430=EDGE_CURVE ( 'NONE', #35420, #12540, #11621, .T. ) ;
#2431=FACE_OUTER_BOUND ( 'NONE', #12347, .T. ) ;
#2443=DIRECTION ( 'NONE',  ( 1.000000000000000000, 0.000000000000000000, 0.000000000000000000 ) ) ;
#2444=ORIENTED_EDGE ( 'NONE', *, *, #15258, .T. ) ;
#2445=CARTESIAN_POINT ( 'NONE',  ( -0.04155248107635957366, 0.2623121065566128007, -0.3903559784317159886 ) ) ;
#2456=FACE_OUTER_BOUND ( 'NONE', #19343, .T. ) ;
#2471=CARTESIAN_POINT ( 'NONE',  ( 0.01895494625228151542, -0.5124113341948460798, 0.08888305413160187129 ) ) ;
#2474=CARTESIAN_POINT ( 'NONE',  ( -0.01548846960707531660, -0.4638115001431011297, -0.2459753896937847684 ) ) ;
#2487=CARTESIAN_POINT ( 'NONE',  ( 0.02235124290213165790, 0.5044963136723996655, -0.09030809412322095275 ) ) ;
#2488=ORIENTED_EDGE ( 'NONE', *, *, #35188, .T. ) ;
#2496=CARTESIAN_POINT ( 'NONE',  ( -0.01548846960707517956, -0.09319974324249266640, -0.5318964258758781538 ) ) ;
#2498=CARTESIAN_POINT ( 'NONE',  ( -0.05252049209742432057, -0.4488546425834899489, 0.1362647994370363713 ) ) ;
#2522=CARTESIAN_POINT ( 'NONE',  ( 0.03875523708678083740, -0.03329700455359455719, -0.4752403914626249226 ) ) ;
#2530=DIRECTION ( 'NONE',  ( -1.355854680848614260E-31, 3.330669073875470114E-16, 1.000000000000000000 ) ) ;
#2531=VERTEX_POINT ( 'NONE', #40494 ) ;
#2536=CYLINDRICAL_SURFACE ( 'NONE', #23761, 0.08139150547213644393 ) ;
#2537=CYLINDRICAL_SURFACE ( 'NONE', #5527, 0.08139150547213643005 ) ;
#2539=DIRECTION ( 'NONE',  ( 1.000000000000000000, 2.280301054154495132E-31, -1.664003471950577689E-31 ) ) ;
#2544=DIRECTION ( 'NONE',  ( 1.000000000000000000, 2.280301054154495132E-31, -1.664003471950577689E-31 ) ) ;
#2547=EDGE_LOOP ( 'NONE', ( #27677, #37805, #21257, #21609 ) ) ;
#2549=DIRECTION ( 'NONE',  ( -8.628166150854818811E-32, 0.1402348365093016580, 0.9901182710308954471 ) ) ;
#2553=DIRECTION ( 'NONE',  ( 1.000000000000000000, 2.280301054154495132E-31, -1.664003471950577689E-31 ) ) ;
#2554=ADVANCED_FACE ( 'NONE', ( #14792 ), #34109, .T. ) ;
#2563=FACE_OUTER_BOUND ( 'NONE', #39505, .T. ) ;
#2564=ORIENTED_EDGE ( 'NONE', *, *, #36768, .F. ) ;
#2566=CARTESIAN_POINT ( 'NONE',  ( -0.05615703521555030775, -0.2783003116137191535, 0.3655156233916935227 ) ) ;
#2569=CARTESIAN_POINT ( 'NONE',  ( -0.04140212552917817840, -0.01694508110950210950, -0.4702784328063241981 ) ) ;
#2574=CARTESIAN_POINT ( 'NONE',  ( 0.05279905671745407925, -0.03987410640504257531, 0.4667149812770405859 ) ) ;
#2575=CARTESIAN_POINT ( 'NONE',  ( 0.04760578872587207383, -0.4700941947101299201, -0.1075272580797730498 ) ) ;
#2578=CARTESIAN_POINT ( 'NONE',  ( 0.03874953289575387705, 0.4622846869243721901, 0.1151793484519291338 ) ) ;
#2580=CARTESIAN_POINT ( 'NONE',  ( -0.05561176441985808683, -0.2541700551350222215, -0.3845131534397778772 ) ) ;
#2586=CARTESIAN_POINT ( 'NONE',  ( -0.01548846960707531660, -0.5198120922912100594, 0.07362328916748400731 ) ) ;
#2590=VERTEX_POINT ( 'NONE', #24258 ) ;
#2596=ORIENTED_EDGE ( 'NONE', *, *, #24119, .F. ) ;
#2604=ADVANCED_FACE ( 'NONE', ( #2456 ), #5728, .T. ) ;
#2605=CARTESIAN_POINT ( 'NONE',  ( -0.04211812644076948220, 0.2825523317586323135, 0.3743635450761847450 ) ) ;
#2611=DIRECTION ( 'NONE',  ( 2.341930812374876608E-31, 0.6954292836768424246, -0.7185945389471826150 ) ) ;
#2623=ADVANCED_FACE ( 'NONE', ( #34922 ), #19097, .T. ) ;
#2627=CARTESIAN_POINT ( 'NONE',  ( 0.02872242845529807825, 0.3729171224323813982, -0.3802687114177593641 ) ) ;
#2642=CIRCLE ( 'NONE', #28327, 0.01500000000000003934 ) ;
#2646=ORIENTED_EDGE ( 'NONE', *, *, #20141, .T. ) ;
#2661=CARTESIAN_POINT ( 'NONE',  ( 0.02869712619511899723, -0.4892154842446472252, 0.09550911579581831956 ) ) ;
#2679=ORIENTED_EDGE ( 'NONE', *, *, #3341, .F. ) ;
#2680=DIRECTION ( 'NONE',  ( -1.355854680848614260E-31, 3.330669073875470114E-16, 1.000000000000000000 ) ) ;
#2688=ORIENTED_EDGE ( 'NONE', *, *, #5019, .F. ) ;
#2691=CARTESIAN_POINT ( 'NONE',  ( -0.04087116408466824613, -0.4416914123362196687, 0.1656680454788615198 ) ) ;
#2707=DIRECTION ( 'NONE',  ( 0.000000000000000000, 2.964295475749157234E-14, 1.000000000000000000 ) ) ;
#2714=CARTESIAN_POINT ( 'NONE',  ( 0.01548846960706645737, 0.07651041855119844470, -0.5222379212568389883 ) ) ;
#2715=ADVANCED_FACE ( 'NONE', ( #34718 ), #16403, .F. ) ;
#2724=ORIENTED_EDGE ( 'NONE', *, *, #1929, .F. ) ;
#2728=ORIENTED_EDGE ( 'NONE', *, *, #38593, .F. ) ;
#2732=TOROIDAL_SURFACE ( 'NONE', #716, 0.5250000000000000222, 0.01499999999999999944 ) ;
#2733=CARTESIAN_POINT ( 'NONE',  ( -0.01548846960712763066, 0.4730347584885825629, 0.2341461249029053171 ) ) ;
#2742=CARTESIAN_POINT ( 'NONE',  ( -0.05283102792148802046, -0.3063958269170686255, 0.3541938269410537243 ) ) ;
#2749=CIRCLE ( 'NONE', #25756, 0.01500000000000005322 ) ;
#2750=ADVANCED_FACE ( 'NONE', ( #1814 ), #12136, .T. ) ;
#2757=VECTOR ( 'NONE', #18322, 39.37007874015748143 ) ;
#2759=CIRCLE ( 'NONE', #34286, 0.01499999999999999424 ) ;
#2770=CARTESIAN_POINT ( 'NONE',  ( -0.05138886601528149661, -0.02227547295148940218, -0.4715784802958458699 ) ) ;
#2776=CARTESIAN_POINT ( 'NONE',  ( 0.04285427992854268925, -0.07198917448059444224, 0.4895546022328310931 ) ) ;
#2780=TOROIDAL_SURFACE ( 'NONE', #4723, 0.6154198107346402491, 0.7750185148639454624 ) ;
#2783=CARTESIAN_POINT ( 'NONE',  ( 0.04047170147976334592, -0.3430616206016776637, -0.3654769923554794797 ) ) ;
#2785=CARTESIAN_POINT ( 'NONE',  ( -0.01548846960707490547, 0.09319974324249648279, 0.5318964258758775987 ) ) ;
#2795=CIRCLE ( 'NONE', #20507, 0.01500000000000004802 ) ;
#2802=CARTESIAN_POINT ( 'NONE',  ( -0.03662792686184404567, 0.4431041838557920332, 0.1872093443778342081 ) ) ;
#2804=DIRECTION ( 'NONE',  ( -1.000000000000000000, -2.341930812374887555E-31, 1.664003471950578127E-31 ) ) ;
#2807=CARTESIAN_POINT ( 'NONE',  ( -0.03170752374382458660, 0.2433701302032824365, 0.4274053688542782670 ) ) ;
#2809=AXIS2_PLACEMENT_3D ( 'NONE', #31198, #9364, #21943 ) ;
#2832=ORIENTED_EDGE ( 'NONE', *, *, #17594, .T. ) ;
#2845=ADVANCED_FACE ( 'NONE', ( #33650, #30584 ), #5862, .F. ) ;
#2866=CARTESIAN_POINT ( 'NONE',  ( 0.01548846960707524721, 0.000000000000000000, 0.000000000000000000 ) ) ;
#2888=CIRCLE ( 'NONE', #9457, 0.01499999999999999251 ) ;
#2895=CARTESIAN_POINT ( 'NONE',  ( 0.1499999999999996336, 0.09319974324249648279, 0.5318964258758775987 ) ) ;
#2896=ORIENTED_EDGE ( 'NONE', *, *, #15767, .T. ) ;
#2901=CARTESIAN_POINT ( 'NONE',  ( -0.05489899477340421524, -0.4472784955204494595, 0.1186631084353751558 ) ) ;
#2905=AXIS2_PLACEMENT_3D ( 'NONE', #14308, #13887, #20294 ) ;
#2916=CIRCLE ( 'NONE', #4193, 0.2149999999999999967 ) ;
#2936=CIRCLE ( 'NONE', #39723, 0.01500000000000001159 ) ;
#2938=CIRCLE ( 'NONE', #8180, 0.01499999999999994914 ) ;
#2941=CARTESIAN_POINT ( 'NONE',  ( 0.01548846960707511190, -0.2306506793134033284, 0.4716198300880330985 ) ) ;
#2945=ORIENTED_EDGE ( 'NONE', *, *, #11667, .F. ) ;
#2961=DIRECTION ( 'NONE',  ( 0.000000000000000000, 0.000000000000000000, 1.000000000000000000 ) ) ;
#2962=EDGE_CURVE ( 'NONE', #24540, #26513, #17934, .T. ) ;
#2964=ADVANCED_FACE ( 'NONE', ( #21942 ), #16343, .T. ) ;
#2965=AXIS2_PLACEMENT_3D ( 'NONE', #5816, #5015, #40390 ) ;
#2974=CIRCLE ( 'NONE', #31234, 0.5302738246768097241 ) ;
#2975=CARTESIAN_POINT ( 'NONE',  ( -0.05615703521554896854, -0.01030498872321393249, 0.4592891699083805346 ) ) ;
#2976=EDGE_LOOP ( 'NONE', ( #39123, #29194, #36082, #518 ) ) ;
#2979=SPHERICAL_SURFACE ( 'NONE', #23946, 0.01499999999999999944 ) ;
#2981=CARTESIAN_POINT ( 'NONE',  ( -0.04308449196698978939, 0.05688586270224989944, -0.4910287377915250606 ) ) ;
#2989=AXIS2_PLACEMENT_3D ( 'NONE', #28280, #31567, #12258 ) ;
#2992=CARTESIAN_POINT ( 'NONE',  ( 0.03174036153404483779, 0.5170813853140181493, 0.08825077997795766072 ) ) ;
#3020=EDGE_CURVE ( 'NONE', #36888, #37954, #26656, .T. ) ;
#3022=CARTESIAN_POINT ( 'NONE',  ( -0.05634490452573013425, 0.2738187358596016474, 0.3682637492038642879 ) ) ;
#3034=CARTESIAN_POINT ( 'NONE',  ( -0.01548846960721245516, -0.07651041855108924039, -0.5222379212565266826 ) ) ;
#3053=ORIENTED_EDGE ( 'NONE', *, *, #21065, .F. ) ;
#3072=CARTESIAN_POINT ( 'NONE',  ( 0.03654364704248811574, 0.3642884434512987379, -0.3592365245254292572 ) ) ;
#3077=DIRECTION ( 'NONE',  ( -0.3468893892380660593, -0.2594111197898882892, -0.9013177145509778665 ) ) ;
#3090=CARTESIAN_POINT ( 'NONE',  ( -0.01895494625228218155, 0.07381100255646892705, 0.5147985126481148255 ) ) ;
#3091=CARTESIAN_POINT ( 'NONE',  ( 0.02869712619511915336, 0.2420104654861724158, 0.4357576342647241363 ) ) ;
#3093=CYLINDRICAL_SURFACE ( 'NONE', #35086, 0.5400000000000001465 ) ;
#3095=ORIENTED_EDGE ( 'NONE', *, *, #25279, .T. ) ;
#3106=CARTESIAN_POINT ( 'NONE',  ( -0.02238765564324999430, -0.5044129532808624417, 0.09031612285223891701 ) ) ;
#3116=CARTESIAN_POINT ( 'NONE',  ( 0.05279755784604373697, -0.2420637527537941869, 0.4010259520538019262 ) ) ;
#3124=CARTESIAN_POINT ( 'NONE',  ( -0.02881408050861471171, 0.4517606495562093705, 0.2100211630561648612 ) ) ;
#3129=DIRECTION ( 'NONE',  ( -9.244463733058732095E-32, 0.1402348365094961968, 0.9901182710308678026 ) ) ;
#3138=ORIENTED_EDGE ( 'NONE', *, *, #17502, .F. ) ;
#3169=CARTESIAN_POINT ( 'NONE',  ( -0.05543910610525255162, -0.02035452233659878693, 0.4608669713610800134 ) ) ;
#3171=DIRECTION ( 'NONE',  ( 0.000000000000000000, 3.330669073875470114E-16, 1.000000000000000000 ) ) ;
#3175=CARTESIAN_POINT ( 'NONE',  ( -0.03478556507500901035, -0.07228131100493927208, -0.5113607228826313467 ) ) ;
#3178=ORIENTED_EDGE ( 'NONE', *, *, #36470, .T. ) ;
#3183=DIRECTION ( 'NONE',  ( -0.3468893892380648936, -0.9373665302208731287, 0.03180785525185938351 ) ) ;
#3199=CARTESIAN_POINT ( 'NONE',  ( -0.05562144613422703721, 0.2870684680408743805, 0.3605846877396484684 ) ) ;
#3205=CARTESIAN_POINT ( 'NONE',  ( -0.02872242845530542654, 0.3729171224323668543, 0.3802687114177480399 ) ) ;
#3215=LINE ( 'NONE', #19066, #40346 ) ;
#3229=VERTEX_POINT ( 'NONE', #24777 ) ;
#3236=( BOUNDED_SURFACE ( )  B_SPLINE_SURFACE ( 3, 2, ( 
 ( #23140, #29086, #22939 ),
 ( #29914, #953, #26218 ),
 ( #7470, #11180, #13464 ),
 ( #20048, #26418, #4189 ),
 ( #29304, #32580, #10376 ),
 ( #1151, #17358, #36071 ),
 ( #1756, #1542, #14063 ),
 ( #32774, #4396, #29497 ),
 ( #26640, #26029, #14268 ),
 ( #7689, #35454, #13652 ),
 ( #10566, #38953, #13845 ),
 ( #1337, #7870, #10783 ),
 ( #23356, #35875, #20253 ),
 ( #17149, #39361, #29698 ),
 ( #39170, #10996, #26832 ),
 ( #23554, #20443, #4783 ),
 ( #15280, #24344, #39966 ),
 ( #33582, #39548, #11382 ),
 ( #8687, #23954, #18364 ),
 ( #30910, #8297, #27237 ),
 ( #36878, #8491, #30303 ),
 ( #1940, #27441, #18163 ) ),
 .UNSPECIFIED., .F., .F., .T. ) 
 B_SPLINE_SURFACE_WITH_KNOTS ( ( 4, 2, 2, 2, 2, 2, 2, 2, 2, 2, 4 ),
 ( 3, 3 ),
 ( 0.002013519961495850458, 0.002780892266055759107, 0.003548264570615667322, 0.004315636875175575538, 0.004699323027455529211, 0.005083009179735483753, 0.005466695332015438294, 0.005850381484295391968, 0.006617753788855301050, 0.007385126093415209265, 0.008152498397975117481 ),
 ( 0.000000000000000000, 1.000000000000000000 ),
 .UNSPECIFIED. ) 
 GEOMETRIC_REPRESENTATION_ITEM ( )  RATIONAL_B_SPLINE_SURFACE ( (
 ( 1.000000000000000000, 0.7283825911960394306, 1.000000000000000000),
 ( 1.000000000000000000, 0.7404375345927788343, 1.000000000000000000),
 ( 1.000000000000000000, 0.7521483142434980396, 1.000000000000000000),
 ( 1.000000000000000000, 0.7744460733777461803, 1.000000000000000000),
 ( 1.000000000000000000, 0.7845612039380909231, 1.000000000000000000),
 ( 1.000000000000000000, 0.8022035258263227053, 1.000000000000000000),
 ( 1.000000000000000000, 0.8093965293320134480, 1.000000000000000000),
 ( 1.000000000000000000, 0.8169028692726254537, 1.000000000000000000),
 ( 1.000000000000000000, 0.8188329634863041884, 1.000000000000000000),
 ( 1.000000000000000000, 0.8214004505364363995, 1.000000000000000000),
 ( 1.000000000000000000, 0.8220602406259868156, 1.000000000000000000),
 ( 1.000000000000000000, 0.8220736605436752553, 1.000000000000000000),
 ( 1.000000000000000000, 0.8214126668415123733, 1.000000000000000000),
 ( 1.000000000000000000, 0.8188520474558839135, 1.000000000000000000),
 ( 1.000000000000000000, 0.8169545908334268081, 1.000000000000000000),
 ( 1.000000000000000000, 0.8094771004219970534, 1.000000000000000000),
 ( 1.000000000000000000, 0.8022723753809176683, 1.000000000000000000),
 ( 1.000000000000000000, 0.7845733350635825110, 1.000000000000000000),
 ( 1.000000000000000000, 0.7744472902493447775, 1.000000000000000000),
 ( 1.000000000000000000, 0.7522916829163305286, 1.000000000000000000),
 ( 1.000000000000000000, 0.7403553004665949233, 1.000000000000000000),
 ( 1.000000000000000000, 0.7283825911960398747, 1.000000000000000000) ) ) 
 REPRESENTATION_ITEM ( '' )  SURFACE ( )  );
#3238=CARTESIAN_POINT ( 'NONE',  ( 0.8248651029816849167, 0.000000000000000000, 0.000000000000000000 ) ) ;
#3242=VERTEX_POINT ( 'NONE', #37299 ) ;
#3249=CARTESIAN_POINT ( 'NONE',  ( 0.01548846960707309615, -0.09061086148586028344, 0.5171215251570917548 ) ) ;
#3255=DIRECTION ( 'NONE',  ( -1.355854680848614478E-31, 3.330669073875470114E-16, 1.000000000000000000 ) ) ;
#3262=CARTESIAN_POINT ( 'NONE',  ( -0.01548846960707463312, 0.3772621329472714558, -0.3651003739303425033 ) ) ;
#3271=CARTESIAN_POINT ( 'NONE',  ( 0.03309060444528755252, -0.3730661130945429060, -0.3633899800202398112 ) ) ;
#3274=CARTESIAN_POINT ( 'NONE',  ( 0.04230188431063456461, 0.2825024449121547598, 0.3739792551055085013 ) ) ;
#3288=ORIENTED_EDGE ( 'NONE', *, *, #5421, .T. ) ;
#3292=CARTESIAN_POINT ( 'NONE',  ( -0.04760454375021171830, -0.4700983808485184046, 0.1075238135162354253 ) ) ;
#3298=FACE_OUTER_BOUND ( 'NONE', #22679, .T. ) ;
#3303=CARTESIAN_POINT ( 'NONE',  ( 0.04230170315644018325, -0.2824006788359444409, 0.3740536075335759159 ) ) ;
#3309=VERTEX_POINT ( 'NONE', #18178 ) ;
#3318=EDGE_LOOP ( 'NONE', ( #13637, #9817 ) ) ;
#3319=CARTESIAN_POINT ( 'NONE',  ( -0.02953079040095700838, 0.000000000000000000, 0.000000000000000000 ) ) ;
#3336=ORIENTED_EDGE ( 'NONE', *, *, #33349, .T. ) ;
#3341=EDGE_CURVE ( 'NONE', #1885, #20917, #17765, .T. ) ;
#3347=CARTESIAN_POINT ( 'NONE',  ( 0.03662792686184266483, -0.4685177067346144031, -0.1089945633920614554 ) ) ;
#3351=CARTESIAN_POINT ( 'NONE',  ( -0.02953079040095700838, -0.4684706630666085614, 0.2484463060367459175 ) ) ;
#3352=EDGE_CURVE ( 'NONE', #22491, #27922, #31220, .T. ) ;
#3357=CARTESIAN_POINT ( 'NONE',  ( -0.04229883635638143069, -0.004358580242002279247, 0.4686119955506233281 ) ) ;
#3362=FACE_OUTER_BOUND ( 'NONE', #22808, .T. ) ;
#3369=VERTEX_POINT ( 'NONE', #15295 ) ;
#3370=DIRECTION ( 'NONE',  ( 0.000000000000000000, -0.9510565162951650775, -0.3090169943749118686 ) ) ;
#3376=CARTESIAN_POINT ( 'NONE',  ( 0.05269111014006448712, -0.2680748163012488527, -0.3844616952933890830 ) ) ;
#3379=CARTESIAN_POINT ( 'NONE',  ( -0.03158843595483510486, 0.2432919444504241524, -0.4277514783322111658 ) ) ;
#3396=EDGE_CURVE ( 'NONE', #37512, #15646, #7557, .T. ) ;
#3398=CARTESIAN_POINT ( 'NONE',  ( -0.05283710938261135942, 0.3063690517300509675, 0.3541964274677629754 ) ) ;
#3400=DIRECTION ( 'NONE',  ( 1.664003471950577032E-31, 3.330669073875470114E-16, 1.000000000000000000 ) ) ;
#3401=FACE_OUTER_BOUND ( 'NONE', #6161, .T. ) ;
#3420=CARTESIAN_POINT ( 'NONE',  ( -0.05283094505690077991, -0.03968992937477339167, 0.4666439588235272162 ) ) ;
#3424=AXIS2_PLACEMENT_3D ( 'NONE', #6422, #25379, #37912 ) ;
#3428=CARTESIAN_POINT ( 'NONE',  ( 0.04946426091936732133, 0.3082279967728599468, -0.3644356914998777563 ) ) ;
#3429=AXIS2_PLACEMENT_3D ( 'NONE', #7064, #25603, #25411 ) ;
#3434=ORIENTED_EDGE ( 'NONE', *, *, #4412, .F. ) ;
#3453=FACE_OUTER_BOUND ( 'NONE', #26820, .T. ) ;
#3457=AXIS2_PLACEMENT_3D ( 'NONE', #16722, #23320, #38915 ) ;
#3459=CARTESIAN_POINT ( 'NONE',  ( -0.01548846960707531660, -0.2306506793134033284, 0.4716198300880330985 ) ) ;
#3464=FACE_OUTER_BOUND ( 'NONE', #5660, .T. ) ;
#3467=DIRECTION ( 'NONE',  ( 0.000000000000000000, 0.5877852522924454926, 0.8090169943749673243 ) ) ;
#3482=ORIENTED_EDGE ( 'NONE', *, *, #8005, .F. ) ;
#3483=CARTESIAN_POINT ( 'NONE',  ( -0.02869712619511944132, 0.06034133159976073219, 0.4947855140619930592 ) ) ;
#3487=CARTESIAN_POINT ( 'NONE',  ( 0.1499999999999996336, -0.3232818887608602809, 0.4449593469062218531 ) ) ;
#3491=VECTOR ( 'NONE', #10270, 39.37007874015748143 ) ;
#3492=EDGE_LOOP ( 'NONE', ( #32968, #35680, #2896, #31463 ) ) ;
#3497=SPHERICAL_SURFACE ( 'NONE', #8266, 0.01499999999999999944 ) ;
#3499=AXIS2_PLACEMENT_3D ( 'NONE', #7808, #10102, #35207 ) ;
#3502=ORIENTED_EDGE ( 'NONE', *, *, #34273, .T. ) ;
#3508=CARTESIAN_POINT ( 'NONE',  ( -0.03171102739523275899, -0.4481073524712075318, 0.2027236177532028560 ) ) ;
#3520=CYLINDRICAL_SURFACE ( 'NONE', #17894, 0.01500000000000001853 ) ;
#3523=CIRCLE ( 'NONE', #26524, 0.01500000000000002894 ) ;
#3526=CARTESIAN_POINT ( 'NONE',  ( -0.02872242845530507613, 0.4768947642620184335, 0.2371557650701880127 ) ) ;
#3528=TOROIDAL_SURFACE ( 'NONE', #39672, 0.5250000000000000222, 0.01499999999999999944 ) ;
#3551=DIRECTION ( 'NONE',  ( 0.000000000000000000, 3.330669073875470114E-16, 1.000000000000000000 ) ) ;
#3553=CARTESIAN_POINT ( 'NONE',  ( -0.01548846960712817709, -0.2450655194479502419, -0.4674710490748132941 ) ) ;
#3568=AXIS2_PLACEMENT_3D ( 'NONE', #38135, #19829, #9959 ) ;
#3570=CARTESIAN_POINT ( 'NONE',  ( -0.04229956186878666008, 0.4429651807893704163, -0.1531492745855134174 ) ) ;
#3571=CARTESIAN_POINT ( 'NONE',  ( -0.02242905165738922138, 0.06991915049797693682, 0.5075494376218457893 ) ) ;
#3572=AXIS2_PLACEMENT_3D ( 'NONE', #18697, #8603, #27556 ) ;
#3580=AXIS2_PLACEMENT_3D ( 'NONE', #39183, #11007, #24356 ) ;
#3590=CARTESIAN_POINT ( 'NONE',  ( 0.05279755784604436147, -0.3065965315811355341, -0.3541401437853726741 ) ) ;
#3595=ORIENTED_EDGE ( 'NONE', *, *, #11027, .T. ) ;
#3610=CARTESIAN_POINT ( 'NONE',  ( -0.02881302694829762298, 0.3393464602396041307, -0.3647504210684009429 ) ) ;
#3613=CARTESIAN_POINT ( 'NONE',  ( -0.05076541221973945167, -0.4330952608417186211, -0.1921093419630976185 ) ) ;
#3617=LINE ( 'NONE', #35474, #10269 ) ;
#3623=CARTESIAN_POINT ( 'NONE',  ( 0.01895884884825203495, 0.07380796352548452122, 0.5147901372834206013 ) ) ;
#3625=EDGE_CURVE ( 'NONE', #30050, #27922, #9534, .T. ) ;
#3628=AXIS2_PLACEMENT_3D ( 'NONE', #16065, #15848, #19563 ) ;
#3636=ORIENTED_EDGE ( 'NONE', *, *, #33352, .F. ) ;
#3637=CARTESIAN_POINT ( 'NONE',  ( -0.02231181081520667783, -0.2417894035777224948, -0.4519954025055052949 ) ) ;
#3646=ORIENTED_EDGE ( 'NONE', *, *, #12679, .T. ) ;
#3684=EDGE_CURVE ( 'NONE', #26731, #12540, #20090, .T. ) ;
#3712=EDGE_CURVE ( 'NONE', #9762, #20386, #22715, .T. ) ;
#3716=CARTESIAN_POINT ( 'NONE',  ( -0.02242905165738846504, -0.4611019942560602436, 0.2233384654055033669 ) ) ;
#3736=CARTESIAN_POINT ( 'NONE',  ( -0.05201840200954667426, 0.4415345355162883512, 0.1624690192511396847 ) ) ;
#3760=DIRECTION ( 'NONE',  ( 1.000000000000000000, 2.341930812374887555E-31, -1.664003471950578127E-31 ) ) ;
#3763=CARTESIAN_POINT ( 'NONE',  ( -0.03654364704248840023, -0.2290829176602870165, 0.4574690890339265237 ) ) ;
#3769=DIRECTION ( 'NONE',  ( -1.000000000000000000, -2.280301054154495132E-31, 1.664003471950577689E-31 ) ) ;
#3770=CARTESIAN_POINT ( 'NONE',  ( 0.1499999999999993561, -0.3688619771572893558, 0.3775276577327004723 ) ) ;
#3777=CARTESIAN_POINT ( 'NONE',  ( -0.03664605387828201444, 0.4430871221163654727, -0.1871485295462624598 ) ) ;
#3788=ORIENTED_EDGE ( 'NONE', *, *, #15994, .T. ) ;
#3792=CARTESIAN_POINT ( 'NONE',  ( 0.04762200653274697992, 0.4434980416368364264, 0.1892582844414469612 ) ) ;
#3793=CARTESIAN_POINT ( 'NONE',  ( 0.03478489236951255031, -0.2420938338886949037, -0.4561872437641432132 ) ) ;
#3803=ORIENTED_EDGE ( 'NONE', *, *, #11426, .F. ) ;
#3806=CARTESIAN_POINT ( 'NONE',  ( -0.04140212552917943434, 0.2627138686861255623, -0.3904233130033975541 ) ) ;
#3807=CARTESIAN_POINT ( 'NONE',  ( -0.03874953289575389093, -0.4416968903498208476, -0.1785420710361537711 ) ) ;
#3808=CARTESIAN_POINT ( 'NONE',  ( 0.01548846960707524721, 0.4638115001430989648, -0.2459753896937820483 ) ) ;
#3817=ORIENTED_EDGE ( 'NONE', *, *, #16755, .F. ) ;
#3818=DIRECTION ( 'NONE',  ( -1.355854680848614260E-31, 3.330669073875470114E-16, 1.000000000000000000 ) ) ;
#3826=DIRECTION ( 'NONE',  ( 4.930380657631316120E-32, -0.4685245517976818208, -0.8834504764630450868 ) ) ;
#3853=CARTESIAN_POINT ( 'NONE',  ( -0.8248651029816859159, -5.463695987328526437E-16, 0.000000000000000000 ) ) ;
#3854=EDGE_CURVE ( 'NONE', #26513, #11533, #2353, .T. ) ;
#3864=DIRECTION ( 'NONE',  ( 0.000000000000000000, -0.9510565162951467588, -0.3090169943749687675 ) ) ;
#3867=DIRECTION ( 'NONE',  ( 1.000000000000000000, 2.341930812374887555E-31, -1.664003471950578127E-31 ) ) ;
#3873=CARTESIAN_POINT ( 'NONE',  ( 0.05283102792148707677, -0.2421768296208668403, 0.4008516595826059903 ) ) ;
#3877=CARTESIAN_POINT ( 'NONE',  ( 0.05083665881508966922, -0.2375940621857673685, -0.4096919151850476060 ) ) ;
#3886=ORIENTED_EDGE ( 'NONE', *, *, #27831, .F. ) ;
#3891=CARTESIAN_POINT ( 'NONE',  ( -0.02869712619511926438, -0.2420104654861697513, 0.4357576342647261347 ) ) ;
#3899=CARTESIAN_POINT ( 'NONE',  ( -0.03159140494780136865, 0.05458666898339525897, -0.4890560705835249600 ) ) ;
#3904=EDGE_CURVE ( 'NONE', #3966, #13311, #39109, .T. ) ;
#3915=ADVANCED_FACE ( 'NONE', ( #35140 ), #7326, .T. ) ;
#3918=CARTESIAN_POINT ( 'NONE',  ( -0.03301162916268465808, 0.5156255563253698826, 0.07469829950279255337 ) ) ;
#3939=FACE_OUTER_BOUND ( 'NONE', #26306, .T. ) ;
#3944=CARTESIAN_POINT ( 'NONE',  ( -0.04293324258486928141, 0.07181764475133092795, 0.4893676133895074054 ) ) ;
#3951=AXIS2_PLACEMENT_3D ( 'NONE', #7811, #20381, #29840 ) ;
#3956=CARTESIAN_POINT ( 'NONE',  ( 0.01548846960703782229, 0.2306506793134120714, 0.4716198300880287131 ) ) ;
#3960=EDGE_CURVE ( 'NONE', #13108, #36780, #1692, .T. ) ;
#3963=EDGE_CURVE ( 'NONE', #20650, #11991, #13924, .T. ) ;
#3966=VERTEX_POINT ( 'NONE', #1406 ) ;
#3980=DIRECTION ( 'NONE',  ( -1.000000000000000000, -2.341930812374887555E-31, 1.664003471950578127E-31 ) ) ;
#3994=DIRECTION ( 'NONE',  ( 1.602373713730174099E-31, 0.9849933812515909715, 0.1725921171159281731 ) ) ;
#3997=CARTESIAN_POINT ( 'NONE',  ( -0.04047076529492919100, 0.3430644450807475709, -0.3654777640200485012 ) ) ;
#3999=AXIS2_PLACEMENT_3D ( 'NONE', #8388, #7976, #24059 ) ;
#4007=CARTESIAN_POINT ( 'NONE',  ( 0.04047043078436408925, 0.4923670751789746003, -0.09403524049742247037 ) ) ;
#4013=EDGE_LOOP ( 'NONE', ( #10496, #738, #1897, #3178 ) ) ;
#4032=ORIENTED_EDGE ( 'NONE', *, *, #32113, .F. ) ;
#4060=CARTESIAN_POINT ( 'NONE',  ( 0.1499999999999994671, 0.4770632572900446178, -0.2530032579707474083 ) ) ;
#4073=ORIENTED_EDGE ( 'NONE', *, *, #16326, .T. ) ;
#4074=DIRECTION ( 'NONE',  ( -1.000000000000000000, -2.280301054154495132E-31, 1.664003471950577689E-31 ) ) ;
#4078=VERTEX_POINT ( 'NONE', #33051 ) ;
#4086=CARTESIAN_POINT ( 'NONE',  ( -0.02869942827333585647, -0.4892109928530954388, 0.09550568247005927769 ) ) ;
#4105=CYLINDRICAL_SURFACE ( 'NONE', #37568, 0.01499999999999999424 ) ;
#4107=SPHERICAL_SURFACE ( 'NONE', #26014, 0.01499999999999999944 ) ;
#4117=EDGE_CURVE ( 'NONE', #19277, #29903, #18112, .T. ) ;
#4132=ORIENTED_EDGE ( 'NONE', *, *, #15204, .F. ) ;
#4140=ORIENTED_EDGE ( 'NONE', *, *, #34287, .F. ) ;
#4146=EDGE_CURVE ( 'NONE', #12540, #19277, #12859, .T. ) ;
#4162=CARTESIAN_POINT ( 'NONE',  ( 0.04155248107635953203, -0.4416604393009532781, -0.1616214326753676322 ) ) ;
#4169=CARTESIAN_POINT ( 'NONE',  ( 0.1499999999999994671, -0.5203207976467947304, -0.08861466064782093366 ) ) ;
#4176=DIRECTION ( 'NONE',  ( -0.9378410757839560352, -0.1072489841977636443, 0.3300784330442384507 ) ) ;
#4187=CARTESIAN_POINT ( 'NONE',  ( 0.05634304521267768928, -0.01028123094845369810, -0.4588823192046729837 ) ) ;
#4188=CARTESIAN_POINT ( 'NONE',  ( 0.1499999999999996336, -0.2450655194479764432, 0.4674710490749318659 ) ) ;
#4189=CARTESIAN_POINT ( 'NONE',  ( -0.04285534776242039268, 0.4878382857517714610, -0.08280911155782545718 ) ) ;
#4193=AXIS2_PLACEMENT_3D ( 'NONE', #36801, #8612, #18099 ) ;
#4197=CARTESIAN_POINT ( 'NONE',  ( 0.01548846960707524721, -0.4638115001430530571, -0.2459753896938768336 ) ) ;
#4202=EDGE_CURVE ( 'NONE', #35448, #35420, #8554, .T. ) ;
#4205=EDGE_CURVE ( 'NONE', #15646, #13008, #32551, .T. ) ;
#4207=CARTESIAN_POINT ( 'NONE',  ( -0.02242905165738677542, 0.2417642932583395632, -0.4517135660370341088 ) ) ;
#4208=CARTESIAN_POINT ( 'NONE',  ( -0.05281452789367512696, -0.4561340086821544793, -0.1063737436285870225 ) ) ;
#4210=DIRECTION ( 'NONE',  ( 0.000000000000000000, 1.000000000000000000, -3.330669073875470607E-16 ) ) ;
#4214=AXIS2_PLACEMENT_3D ( 'NONE', #18264, #24658, #15590 ) ;
#4216=DIRECTION ( 'NONE',  ( 0.000000000000000000, 0.8834504764630474183, 0.4685245517976774354 ) ) ;
#4218=CARTESIAN_POINT ( 'NONE',  ( 0.01899496522502736040, 0.4667215747137400395, -0.2292237458735868205 ) ) ;
#4222=AXIS2_PLACEMENT_3D ( 'NONE', #38260, #12983, #10691 ) ;
#4223=CARTESIAN_POINT ( 'NONE',  ( -0.04285534776242177352, -0.2295064659597282342, -0.4383723578020129463 ) ) ;
#4225=VERTEX_POINT ( 'NONE', #5682 ) ;
#4227=DIRECTION ( 'NONE',  ( 1.702140497302374535E-12, 0.000000000000000000, 1.000000000000000000 ) ) ;
#4242=VERTEX_POINT ( 'NONE', #39839 ) ;
#4260=CARTESIAN_POINT ( 'NONE',  ( 0.04285640132274102371, -0.4433417433457782497, 0.2197472875419871907 ) ) ;
#4283=CARTESIAN_POINT ( 'NONE',  ( -0.05076541221973634999, -0.3165406372985192784, 0.3525330185552920104 ) ) ;
#4286=EDGE_LOOP ( 'NONE', ( #28059, #25268, #36009 ) ) ;
#4302=CARTESIAN_POINT ( 'NONE',  ( -0.03664605387828073768, -0.4430871221163693585, 0.1871485295462612941 ) ) ;
#4313=DIRECTION ( 'NONE',  ( 0.000000000000000000, 0.5877852522924655876, -0.8090169943749527803 ) ) ;
#4315=AXIS2_PLACEMENT_3D ( 'NONE', #38812, #29378, #19908 ) ;
#4318=( BOUNDED_SURFACE ( )  B_SPLINE_SURFACE ( 3, 2, ( 
 ( #18539, #14856, #40551 ),
 ( #11762, #24319, #36847 ),
 ( #5359, #30486, #8660 ),
 ( #28017, #31094, #37455 ),
 ( #21232, #9272, #21848 ),
 ( #33770, #34375, #6191 ),
 ( #18760, #31308, #3116 ),
 ( #15659, #28208, #25959 ),
 ( #874, #13168, #7005 ),
 ( #3303, #1083, #38483 ),
 ( #29226, #22064, #679 ),
 ( #22670, #19755, #38265 ),
 ( #16280, #25737, #13381 ),
 ( #25343, #19374, #32104 ),
 ( #25540, #31493, #34774 ),
 ( #10315, #31909, #37880 ),
 ( #29012, #22879, #16673 ),
 ( #9695, #38068, #10096 ) ),
 .UNSPECIFIED., .F., .F., .T. ) 
 B_SPLINE_SURFACE_WITH_KNOTS ( ( 4, 2, 2, 2, 2, 2, 2, 2, 4 ),
 ( 3, 3 ),
 ( -0.001532620576208848159, -0.0007637936630077626476, 5.033250193322864191E-06, 0.0007738601633944083760, 0.001542687076595493888, 0.002311513989796579183, 0.003080340902997664911, 0.003849167816198750640, 0.004617994729399835935 ),
 ( 0.000000000000000000, 1.000000000000000000 ),
 .UNSPECIFIED. ) 
 GEOMETRIC_REPRESENTATION_ITEM ( )  RATIONAL_B_SPLINE_SURFACE ( (
 ( 1.000000000000000000, 0.7283825911960447597, 1.000000000000000000),
 ( 1.000000000000000000, 0.7404385082112692196, 1.000000000000000000),
 ( 1.000000000000000000, 0.7521504257740204702, 1.000000000000000000),
 ( 1.000000000000000000, 0.7744497410759664247, 1.000000000000000000),
 ( 1.000000000000000000, 0.7845654757374723731, 1.000000000000000000),
 ( 1.000000000000000000, 0.8022083990891452077, 1.000000000000000000),
 ( 1.000000000000000000, 0.8094167424699479918, 1.000000000000000000),
 ( 1.000000000000000000, 0.8194491993616462855, 1.000000000000000000),
 ( 1.000000000000000000, 0.8220634900780513510, 1.000000000000000000),
 ( 1.000000000000000000, 0.8220705070823443039, 1.000000000000000000),
 ( 1.000000000000000000, 0.8194468812479829278, 1.000000000000000000),
 ( 1.000000000000000000, 0.8094220769840587693, 1.000000000000000000),
 ( 1.000000000000000000, 0.8022659121986455144, 1.000000000000000000),
 ( 1.000000000000000000, 0.7845681159034547658, 1.000000000000000000),
 ( 1.000000000000000000, 0.7744426415184183510, 1.000000000000000000),
 ( 1.000000000000000000, 0.7522890290929796775, 1.000000000000000000),
 ( 1.000000000000000000, 0.7403540167214540668, 1.000000000000000000),
 ( 1.000000000000000000, 0.7283825911960212229, 1.000000000000000000) ) ) 
 REPRESENTATION_ITEM ( '' )  SURFACE ( )  );
#4329=DIRECTION ( 'NONE',  ( 0.000000000000000000, 0.000000000000000000, -1.000000000000000000 ) ) ;
#4339=ORIENTED_EDGE ( 'NONE', *, *, #3020, .F. ) ;
#4369=ADVANCED_FACE ( 'NONE', ( #6482 ), #9780, .T. ) ;
#4396=CARTESIAN_POINT ( 'NONE',  ( -0.05137569054208514924, 0.4554428576828045139, -0.1244487204292454574 ) ) ;
#4409=CARTESIAN_POINT ( 'NONE',  ( -0.03674260963082301434, 0.2486114773148996593, -0.4115095709379173461 ) ) ;
#4411=CARTESIAN_POINT ( 'NONE',  ( -0.04229883635637964739, -0.4443296166163696603, -0.1489543265340548261 ) ) ;
#4412=EDGE_CURVE ( 'NONE', #9762, #20650, #25439, .T. ) ;
#4422=CARTESIAN_POINT ( 'NONE',  ( -0.05252049209742690183, -0.2682992380086431927, -0.3847779939372243385 ) ) ;
#4432=EDGE_LOOP ( 'NONE', ( #10663, #11973, #23092, #20506, #8387 ) ) ;
#4434=CARTESIAN_POINT ( 'NONE',  ( 0.1499999999999994671, 0.4638115001430989648, -0.2459753896937820483 ) ) ;
#4442=ORIENTED_EDGE ( 'NONE', *, *, #8723, .F. ) ;
#4447=ORIENTED_EDGE ( 'NONE', *, *, #17578, .T. ) ;
#4452=DIRECTION ( 'NONE',  ( 0.000000000000000000, 3.330669073875469621E-16, 1.000000000000000000 ) ) ;
#4459=CARTESIAN_POINT ( 'NONE',  ( 0.05562150110511214496, -0.02029635476683555595, 0.4604536315446556283 ) ) ;
#4465=CARTESIAN_POINT ( 'NONE',  ( 0.05078310099560720547, 0.2374900923169198097, 0.4099167927581913728 ) ) ;
#4471=EDGE_CURVE ( 'NONE', #39166, #35163, #35211, .T. ) ;
#4475=CARTESIAN_POINT ( 'NONE',  ( -0.05491348488830474078, -0.2511509903618516226, 0.3886212643843945380 ) ) ;
#4483=DIRECTION ( 'NONE',  ( 0.000000000000000000, 0.3090169943749439541, -0.9510565162951547524 ) ) ;
#4485=CARTESIAN_POINT ( 'NONE',  ( -0.04582713223189551627, 0.4389429380065683617, 0.2108029774974878590 ) ) ;
#4491=ORIENTED_EDGE ( 'NONE', *, *, #16592, .F. ) ;
#4504=CARTESIAN_POINT ( 'NONE',  ( 0.02953079040095687308, 0.09152108205202039160, -0.5223162075576429642 ) ) ;
#4507=SPHERICAL_SURFACE ( 'NONE', #22645, 0.01499999999999999944 ) ;
#4508=LINE ( 'NONE', #10310, #11302 ) ;
#4509=DIRECTION ( 'NONE',  ( 1.000000000000000000, 0.000000000000000000, 0.000000000000000000 ) ) ;
#4510=CARTESIAN_POINT ( 'NONE',  ( 0.02953079040095700838, -0.09152108205202422186, -0.5223162075576424090 ) ) ;
#4523=LINE ( 'NONE', #33128, #36169 ) ;
#4533=CARTESIAN_POINT ( 'NONE',  ( 0.02872242845529790478, 0.4768947642620333105, 0.2371557650701984765 ) ) ;
#4553=CARTESIAN_POINT ( 'NONE',  ( -0.01548846960707524721, 0.000000000000000000, 0.000000000000000000 ) ) ;
#4554=DIRECTION ( 'NONE',  ( 1.000000000000000000, 0.000000000000000000, 0.000000000000000000 ) ) ;
#4571=VERTEX_POINT ( 'NONE', #10802 ) ;
#4573=DIRECTION ( 'NONE',  ( 1.000000000000000000, 2.280301054154495132E-31, -1.664003471950577689E-31 ) ) ;
#4575=CIRCLE ( 'NONE', #20463, 0.01499999999999994220 ) ;
#4586=ORIENTED_EDGE ( 'NONE', *, *, #32264, .T. ) ;
#4590=ADVANCED_FACE ( 'NONE', ( #35896 ), #1352, .T. ) ;
#4592=CARTESIAN_POINT ( 'NONE',  ( -0.04085667396267319423, -0.4416859672262361536, -0.1657724178830653206 ) ) ;
#4596=DIRECTION ( 'NONE',  ( 1.000000000000000000, 2.341930812374887555E-31, -1.664003471950578127E-31 ) ) ;
#4598=CARTESIAN_POINT ( 'NONE',  ( 0.01896931156525897069, 0.5123785568735239604, -0.08888416637129735454 ) ) ;
#4603=CARTESIAN_POINT ( 'NONE',  ( -0.05616044724337304617, -0.2782405634116419391, -0.3655497896892178078 ) ) ;
#4607=CARTESIAN_POINT ( 'NONE',  ( -0.04582705327698308878, 0.06484491888963164752, -0.4826014279685446606 ) ) ;
#4610=EDGE_CURVE ( 'NONE', #1885, #32432, #16160, .T. ) ;
#4614=CARTESIAN_POINT ( 'NONE',  ( 0.05082303569918651676, 0.3162776479886627023, 0.3525632866555266642 ) ) ;
#4615=CARTESIAN_POINT ( 'NONE',  ( 0.01548846960703785525, -0.3772621329472687357, 0.3651003739303496087 ) ) ;
#4624=VERTEX_POINT ( 'NONE', #32599 ) ;
#4627=ORIENTED_EDGE ( 'NONE', *, *, #24402, .F. ) ;
#4633=ORIENTED_EDGE ( 'NONE', *, *, #17472, .T. ) ;
#4640=CARTESIAN_POINT ( 'NONE',  ( 0.04157143636675179887, -0.4416880288200910609, 0.1614235308635223742 ) ) ;
#4651=CARTESIAN_POINT ( 'NONE',  ( 0.03868264068766632396, -0.3066108573455326725, -0.3648330973802358379 ) ) ;
#4653=CARTESIAN_POINT ( 'NONE',  ( 0.05269111014005566779, 0.2680748163012560137, 0.3844616952934046816 ) ) ;
#4662=CARTESIAN_POINT ( 'NONE',  ( -0.01548846960707415434, -0.3688619771572919093, 0.3775276577327012495 ) ) ;
#4668=AXIS2_PLACEMENT_3D ( 'NONE', #6502, #22973, #35314 ) ;
#4679=B_SPLINE_CURVE_WITH_KNOTS ( 'NONE', 3,
 ( #30725, #34008, #40168, #5812, #18371, #30918, #2742, #27846, #24770, #6013, #18795, #28441, #34621, #28659, #37485, #3763, #31136, #13210 ),
 .UNSPECIFIED., .F., .F.,
 ( 4, 2, 2, 2, 2, 2, 2, 2, 4 ),
 ( 0.000000000000000000, 0.0007746617437634289397, 0.001549323487526857879, 0.002323985231290287036, 0.003098646975053715759, 0.003873308718817144482, 0.004647970462580574072, 0.005422632206344002795, 0.006197293950107431518 ),
 .UNSPECIFIED. ) ;
#4682=VERTEX_POINT ( 'NONE', #5410 ) ;
#4698=AXIS2_PLACEMENT_3D ( 'NONE', #21019, #36833, #8648 ) ;
#4706=DIRECTION ( 'NONE',  ( -1.000000000000000000, -2.280301054154495132E-31, 1.664003471950577689E-31 ) ) ;
#4723=AXIS2_PLACEMENT_3D ( 'NONE', #2408, #30780, #30977 ) ;
#4731=AXIS2_PLACEMENT_3D ( 'NONE', #34364, #18951, #34156 ) ;
#4733=CARTESIAN_POINT ( 'NONE',  ( -0.01548846960712817709, -0.4730347584885852830, -0.2341461249029094249 ) ) ;
#4738=ORIENTED_EDGE ( 'NONE', *, *, #5886, .F. ) ;
#4760=AXIS2_PLACEMENT_3D ( 'NONE', #29379, #17222, #29773 ) ;
#4768=FACE_OUTER_BOUND ( 'NONE', #10949, .T. ) ;
#4779=CARTESIAN_POINT ( 'NONE',  ( 0.05561170715395058473, -0.02038383341412211558, -0.4604752114371308824 ) ) ;
#4783=CARTESIAN_POINT ( 'NONE',  ( -0.05281452789367998418, 0.4315450824722493750, -0.1820506770215899739 ) ) ;
#4787=CIRCLE ( 'NONE', #23885, 0.1749999999999999889 ) ;
#4800=CARTESIAN_POINT ( 'NONE',  ( -0.05252359774140240994, -0.4488292542424489051, -0.1363200544095012345 ) ) ;
#4820=CONICAL_SURFACE ( 'NONE', #19948, 0.3698489655878005045, 1.211529128687673262 ) ;
#4823=CARTESIAN_POINT ( 'NONE',  ( -0.01548846960712763066, 0.2450655194479529619, 0.4674710490748108516 ) ) ;
#4825=CARTESIAN_POINT ( 'NONE',  ( 0.02872242845530406652, 0.07817994906157187118, 0.5268390348591149852 ) ) ;
#4834=ORIENTED_EDGE ( 'NONE', *, *, #5360, .F. ) ;
#4840=FACE_OUTER_BOUND ( 'NONE', #17506, .T. ) ;
#4844=CARTESIAN_POINT ( 'NONE',  ( -0.01548846960707545191, -0.5198120922912057296, -0.07362328916749273644 ) ) ;
#4864=EDGE_CURVE ( 'NONE', #5616, #25917, #11572, .T. ) ;
#4875=CARTESIAN_POINT ( 'NONE',  ( -0.04211471441534175852, -0.2826022563026960310, 0.3743350969764960845 ) ) ;
#4878=CIRCLE ( 'NONE', #27906, 0.01500000000000000291 ) ;
#4888=CARTESIAN_POINT ( 'NONE',  ( -0.05634301242525835418, 0.2614060064472178424, -0.3772872482281192652 ) ) ;
#4896=DIRECTION ( 'NONE',  ( 1.000000000000000000, 0.000000000000000000, 0.000000000000000000 ) ) ;
#4909=CARTESIAN_POINT ( 'NONE',  ( 0.01548846960721238578, 0.5203207976464816475, -0.08861466064783077301 ) ) ;
#4915=CARTESIAN_POINT ( 'NONE',  ( 0.02953079040095728247, 0.000000000000000000, 0.000000000000000000 ) ) ;
#4923=CARTESIAN_POINT ( 'NONE',  ( 0.03159140494779937719, -0.4482517543799813264, 0.2030416442520436293 ) ) ;
#4929=CARTESIAN_POINT ( 'NONE',  ( 0.04155248107635944876, 0.01723053523177107277, -0.4699878081388669804 ) ) ;
#4933=DIRECTION ( 'NONE',  ( -1.000000000000000000, -2.280301054154495132E-31, 1.664003471950577689E-31 ) ) ;
#4934=ORIENTED_EDGE ( 'NONE', *, *, #18563, .T. ) ;
#4966=CARTESIAN_POINT ( 'NONE',  ( -0.01548846960707517956, -0.09061086148575756005, -0.5171215251571035232 ) ) ;
#4969=EDGE_CURVE ( 'NONE', #30248, #26219, #12608, .T. ) ;
#4980=CARTESIAN_POINT ( 'NONE',  ( 0.02242828275838999394, 0.06992002095335812795, -0.5075510395145109710 ) ) ;
#4988=ORIENTED_EDGE ( 'NONE', *, *, #15696, .T. ) ;
#5000=ORIENTED_EDGE ( 'NONE', *, *, #11727, .F. ) ;
#5002=VECTOR ( 'NONE', #16868, 39.37007874015748143 ) ;
#5015=DIRECTION ( 'NONE',  ( -1.000000000000000000, -2.280301054154495132E-31, 1.664003471950577689E-31 ) ) ;
#5016=CARTESIAN_POINT ( 'NONE',  ( 0.03650581953630420429, -0.4542932396444889220, 0.2355374485430444531 ) ) ;
#5017=CARTESIAN_POINT ( 'NONE',  ( -0.03647137243075312951, -0.5060707921514409069, -0.07645882641830938076 ) ) ;
#5019=EDGE_CURVE ( 'NONE', #23130, #4242, #9590, .T. ) ;
#5029=DIRECTION ( 'NONE',  ( -1.416619696839553536E-11, 0.9510565162951574170, 0.3090169943749355719 ) ) ;
#5031=CARTESIAN_POINT ( 'NONE',  ( -0.03874953289575396032, -0.2523958943867713467, -0.4040664878102112056 ) ) ;
#5040=CARTESIAN_POINT ( 'NONE',  ( -0.02869942827333567606, 0.2420058122830187619, 0.4357544236535290105 ) ) ;
#5041=CARTESIAN_POINT ( 'NONE',  ( 0.03875523708677763163, 0.03329700455359576455, 0.4752403914626244230 ) ) ;
#5042=CARTESIAN_POINT ( 'NONE',  ( 0.02238826743732996727, -0.5044115272350837564, -0.09031638658505519723 ) ) ;
#5048=CARTESIAN_POINT ( 'NONE',  ( -0.03309060444528731659, -0.2303206394829994674, -0.4671006372792942396 ) ) ;
#5059=CIRCLE ( 'NONE', #28073, 0.01500000000000001853 ) ;
#5064=CARTESIAN_POINT ( 'NONE',  ( 0.05634206451479450983, -0.4332270636364607408, 0.1516455289248211102 ) ) ;
#5071=CARTESIAN_POINT ( 'NONE',  ( -0.06980746140711623082, 7.160938508832261116E-17, 0.2149999999999999967 ) ) ;
#5074=CARTESIAN_POINT ( 'NONE',  ( 0.02872242845529805050, 0.2464193076120176074, 0.4721747535845016164 ) ) ;
#5077=CARTESIAN_POINT ( 'NONE',  ( -0.03650581953630666066, 0.5059763899182377900, -0.07647306779615337113 ) ) ;
#5083=VERTEX_POINT ( 'NONE', #20418 ) ;
#5084=CARTESIAN_POINT ( 'NONE',  ( -0.01548846960707545191, -0.5346638663566692928, 0.07572681171513533094 ) ) ;
#5089=CARTESIAN_POINT ( 'NONE',  ( -0.05634301242525814601, 0.4396003943662979419, 0.1320237143668709923 ) ) ;
#5093=CARTESIAN_POINT ( 'NONE',  ( 0.04293317454820645696, 0.4876093284570318653, -0.08292018301452643014 ) ) ;
#5095=DIRECTION ( 'NONE',  ( 0.3468893892380797150, 0.2594111197900920152, 0.9013177145509138066 ) ) ;
#5113=CARTESIAN_POINT ( 'NONE',  ( 0.05562144613422637801, 0.2870684680408734923, -0.3605846877396488570 ) ) ;
#5115=CARTESIAN_POINT ( 'NONE',  ( 0.01548846960707524721, 0.5346638663566677385, -0.07572681171513587217 ) ) ;
#5136=ORIENTED_EDGE ( 'NONE', *, *, #18783, .F. ) ;
#5143=CARTESIAN_POINT ( 'NONE',  ( -0.03868264068766668479, -0.4417248602032604055, -0.1788646266443680855 ) ) ;
#5152=ADVANCED_FACE ( 'NONE', ( #28799 ), #3497, .T. ) ;
#5175=CARTESIAN_POINT ( 'NONE',  ( 0.03478489236951704672, 0.07228210831916115353, -0.5113624180529584562 ) ) ;
#5176=DIRECTION ( 'NONE',  ( 0.000000000000000000, 0.9510565162951627460, -0.3090169943749190296 ) ) ;
#5184=CARTESIAN_POINT ( 'NONE',  ( -0.03309060444528701822, -0.4608881774262385544, -0.2425132784556381649 ) ) ;
#5191=DIRECTION ( 'NONE',  ( 0.000000000000000000, 0.5877852522924701395, -0.8090169943749496717 ) ) ;
#5196=DIRECTION ( 'NONE',  ( 0.000000000000000000, -0.9510565162951465368, -0.3090169943749687120 ) ) ;
#5204=CARTESIAN_POINT ( 'NONE',  ( 0.01548846960706681299, -0.3772621329472835017, 0.3651003739303615991 ) ) ;
#5217=ADVANCED_FACE ( 'NONE', ( #38459 ), #23466, .T. ) ;
#5225=VERTEX_POINT ( 'NONE', #2036 ) ;
#5228=CARTESIAN_POINT ( 'NONE',  ( -0.03647137243075214419, -0.3644785006310388709, -0.3593174381849628674 ) ) ;
#5234=CARTESIAN_POINT ( 'NONE',  ( 0.03171861681796955129, -0.07587220456996765505, 0.5191007718638491752 ) ) ;
#5235=CARTESIAN_POINT ( 'NONE',  ( 0.03875523708678054596, -0.4622698113760334016, -0.1151900242215433134 ) ) ;
#5238=EDGE_CURVE ( 'NONE', #5225, #38396, #39269, .T. ) ;
#5243=ORIENTED_EDGE ( 'NONE', *, *, #23622, .T. ) ;
#5252=EDGE_LOOP ( 'NONE', ( #15782, #28149, #18458, #38492 ) ) ;
#5266=CARTESIAN_POINT ( 'NONE',  ( 0.02242828275839013272, 0.2417645306140285832, 0.4517153736362803929 ) ) ;
#5267=DIRECTION ( 'NONE',  ( 5.264498737790487855E-15, -0.7185945389471846134, -0.6954292836768403152 ) ) ;
#5277=CARTESIAN_POINT ( 'NONE',  ( -0.05562144613422701639, 0.2542273817772375821, -0.3844451335760736277 ) ) ;
#5280=CARTESIAN_POINT ( 'NONE',  ( -0.03309057659885079189, 0.5154121718708730704, 0.07470590733143719908 ) ) ;
#5283=VERTEX_POINT ( 'NONE', #23853 ) ;
#5290=CARTESIAN_POINT ( 'NONE',  ( -0.03159140494780091069, -0.3316214887069892647, 0.3635694333040963011 ) ) ;
#5295=CARTESIAN_POINT ( 'NONE',  ( 0.1499999999999993561, 0.000000000000000000, 0.000000000000000000 ) ) ;
#5308=AXIS2_PLACEMENT_3D ( 'NONE', #215, #6729, #31847 ) ;
#5317=CIRCLE ( 'NONE', #32907, 0.2526340763130724976 ) ;
#5321=ORIENTED_EDGE ( 'NONE', *, *, #27622, .T. ) ;
#5324=DIRECTION ( 'NONE',  ( 1.000000000000000000, 2.341930812374887555E-31, -1.664003471950578127E-31 ) ) ;
#5331=VERTEX_POINT ( 'NONE', #35567 ) ;
#5338=AXIS2_PLACEMENT_3D ( 'NONE', #14846, #11562, #24126 ) ;
#5346=CIRCLE ( 'NONE', #23219, 0.1749999999999999889 ) ;
#5357=DIRECTION ( 'NONE',  ( 0.000000000000000000, -0.5877852522924640333, 0.8090169943749540016 ) ) ;
#5359=CARTESIAN_POINT ( 'NONE',  ( 0.02238826743732924215, -0.2417677220642108493, 0.4518145715460074596 ) ) ;
#5360=EDGE_CURVE ( 'NONE', #14981, #36888, #34588, .T. ) ;
#5367=AXIS2_PLACEMENT_3D ( 'NONE', #31690, #35577, #4313 ) ;
#5370=CARTESIAN_POINT ( 'NONE',  ( 0.04575185649130582288, 0.06505045373102633088, -0.4827759578813190511 ) ) ;
#5408=CARTESIAN_POINT ( 'NONE',  ( 0.01548846960707292615, 0.5198120922912253805, -0.07362328916738401785 ) ) ;
#5409=VECTOR ( 'NONE', #2069, 39.37007874015748143 ) ;
#5410=CARTESIAN_POINT ( 'NONE',  ( -0.02953079040095652960, 0.09152108205202803826, 0.5223162075576412988 ) ) ;
#5421=EDGE_CURVE ( 'NONE', #16052, #40212, #26056, .T. ) ;
#5427=CARTESIAN_POINT ( 'NONE',  ( -0.05269191099236000819, -0.004472488327042840883, -0.4686046460979745309 ) ) ;
#5430=DIRECTION ( 'NONE',  ( 1.000000000000000000, -1.544378112879837308E-12, -7.552944938426195655E-13 ) ) ;
#5432=TOROIDAL_SURFACE ( 'NONE', #34350, 0.5250000000000000222, 0.01499999999999999944 ) ;
#5433=CARTESIAN_POINT ( 'NONE',  ( 0.05279755784604317492, 0.03988345070377673218, 0.4667183143801719170 ) ) ;
#5434=EDGE_CURVE ( 'NONE', #33332, #5225, #8300, .T. ) ;
#5435=CARTESIAN_POINT ( 'NONE',  ( 0.04229974373173520791, -0.4483441990207298611, -0.1365932678717892423 ) ) ;
#5443=ORIENTED_EDGE ( 'NONE', *, *, #35326, .T. ) ;
#5446=EDGE_LOOP ( 'NONE', ( #2196, #5000, #22033, #8564 ) ) ;
#5451=CARTESIAN_POINT ( 'NONE',  ( -0.03654364704248686674, -0.4542255574219898895, 0.2354487068768213731 ) ) ;
#5461=DIRECTION ( 'NONE',  ( 1.000000000000000000, 2.341930812374887555E-31, -1.664003471950578127E-31 ) ) ;
#5473=CARTESIAN_POINT ( 'NONE',  ( 0.04047043078435960672, 0.2415826219374435924, 0.4392104278743103052 ) ) ;
#5497=ORIENTED_EDGE ( 'NONE', *, *, #11148, .T. ) ;
#5499=SPHERICAL_SURFACE ( 'NONE', #9938, 0.01499999999999999944 ) ;
#5508=ORIENTED_EDGE ( 'NONE', *, *, #37754, .T. ) ;
#5520=DIRECTION ( 'NONE',  ( 0.000000000000000000, -0.5877852522924607026, -0.8090169943749563330 ) ) ;
#5523=DIRECTION ( 'NONE',  ( 0.000000000000000000, -2.697841949839120927E-14, -1.000000000000000000 ) ) ;
#5527=AXIS2_PLACEMENT_3D ( 'NONE', #2340, #40374, #24759 ) ;
#5542=EDGE_LOOP ( 'NONE', ( #25312, #11118, #8858, #14251 ) ) ;
#5544=ORIENTED_EDGE ( 'NONE', *, *, #23991, .T. ) ;
#5561=AXIS2_PLACEMENT_3D ( 'NONE', #12825, #31738, #25386 ) ;
#5564=CARTESIAN_POINT ( 'NONE',  ( -0.03672309138969633013, -0.4682479968340325094, 0.1092356788912448168 ) ) ;
#5575=CARTESIAN_POINT ( 'NONE',  ( -0.01548846960707524721, 0.3772621329472709006, 0.3651003739303413931 ) ) ;
#5589=CARTESIAN_POINT ( 'NONE',  ( 0.03643058821096969296, -0.08373535757664375689, -0.5050280785339864575 ) ) ;
#5603=FACE_OUTER_BOUND ( 'NONE', #12081, .T. ) ;
#5613=SPHERICAL_SURFACE ( 'NONE', #13844, 0.01499999999999999944 ) ;
#5616=VERTEX_POINT ( 'NONE', #13927 ) ;
#5639=CARTESIAN_POINT ( 'NONE',  ( -0.02881329448201062557, -0.3393412917002096019, -0.3647544004888587099 ) ) ;
#5640=ORIENTED_EDGE ( 'NONE', *, *, #30794, .F. ) ;
#5641=CARTESIAN_POINT ( 'NONE',  ( -0.08978098643734171158, 0.000000000000000000, 0.000000000000000000 ) ) ;
#5642=CARTESIAN_POINT ( 'NONE',  ( -0.04575334816098278190, -0.2311426348461427527, 0.4288046462019637350 ) ) ;
#5646=CARTESIAN_POINT ( 'NONE',  ( -0.02881302694830004812, 0.06014213504333749266, -0.4945521340962376056 ) ) ;
#5650=FACE_OUTER_BOUND ( 'NONE', #31232, .T. ) ;
#5651=CARTESIAN_POINT ( 'NONE',  ( 0.04047043078436458191, -0.06271696546453207899, 0.4973274026419853278 ) ) ;
#5658=CARTESIAN_POINT ( 'NONE',  ( 0.03303737228521275160, -0.3731855291841249533, -0.3634704002369493203 ) ) ;
#5660=EDGE_LOOP ( 'NONE', ( #24762, #35441, #20112 ) ) ;
#5678=ORIENTED_EDGE ( 'NONE', *, *, #27507, .T. ) ;
#5679=CARTESIAN_POINT ( 'NONE',  ( -0.04154009738085488734, 0.4416556227939107404, 0.1617111092119882798 ) ) ;
#5682=CARTESIAN_POINT ( 'NONE',  ( -0.08978098643734171158, -4.231851475640401875E-16, 0.3698489655878013371 ) ) ;
#5683=AXIS2_PLACEMENT_3D ( 'NONE', #39461, #8197, #36378 ) ;
#5685=CARTESIAN_POINT ( 'NONE',  ( -0.02881329448201175314, 0.3393412917002295859, 0.3647544004888629288 ) ) ;
#5692=CIRCLE ( 'NONE', #22821, 0.01500000000000001159 ) ;
#5699=ORIENTED_EDGE ( 'NONE', *, *, #8406, .F. ) ;
#5704=CARTESIAN_POINT ( 'NONE',  ( 0.03875673594170014197, 0.3062691647558835606, -0.3649083695375474057 ) ) ;
#5713=ORIENTED_EDGE ( 'NONE', *, *, #25352, .F. ) ;
#5724=EDGE_LOOP ( 'NONE', ( #11049, #30551 ) ) ;
#5728=CYLINDRICAL_SURFACE ( 'NONE', #35756, 0.5400000000000017009 ) ;
#5757=ORIENTED_EDGE ( 'NONE', *, *, #24584, .T. ) ;
#5765=EDGE_CURVE ( 'NONE', #22491, #28751, #25406, .T. ) ;
#5772=CARTESIAN_POINT ( 'NONE',  ( -0.03642997641688847099, -0.5061875831641888812, 0.07642488348722685509 ) ) ;
#5778=AXIS2_PLACEMENT_3D ( 'NONE', #30366, #29972, #8352 ) ;
#5790=CARTESIAN_POINT ( 'NONE',  ( 0.04946426091936618336, 0.03515176265875070982, -0.4760065386269222709 ) ) ;
#5796=CARTESIAN_POINT ( 'NONE',  ( -0.01548846960712831414, -0.5203207976466733831, 0.08861466064782504148 ) ) ;
#5805=DIRECTION ( 'NONE',  ( 0.000000000000000000, -1.000000000000000000, 3.330669073875470607E-16 ) ) ;
#5812=CARTESIAN_POINT ( 'NONE',  ( -0.04293701532779557045, -0.3457382709204471771, 0.3536859687696398136 ) ) ;
#5816=CARTESIAN_POINT ( 'NONE',  ( 0.01548846960707524721, 0.000000000000000000, 0.000000000000000000 ) ) ;
#5826=CARTESIAN_POINT ( 'NONE',  ( -0.03174036153405352528, -0.07585545617081303205, 0.5190446117378583191 ) ) ;
#5832=CARTESIAN_POINT ( 'NONE',  ( -0.03303708955568570443, 0.08827115631758945813, -0.5134073995267796064 ) ) ;
#5837=DIRECTION ( 'NONE',  ( 0.3468893892380643384, 0.7770416411310695493, 0.5252371270030109507 ) ) ;
#5839=CARTESIAN_POINT ( 'NONE',  ( 0.02953079040094806068, -0.09152108205202535984, 0.5223162075576641694 ) ) ;
#5840=CARTESIAN_POINT ( 'NONE',  ( 0.04575106512774684830, -0.4792499720836655430, -0.08732285767966210810 ) ) ;
#5843=CARTESIAN_POINT ( 'NONE',  ( 0.01899468245560481314, 0.5123206680798495505, 0.08888613072388773517 ) ) ;
#5849=CARTESIAN_POINT ( 'NONE',  ( 0.05634304521267756438, 0.01028123094841836525, 0.4588823192046724841 ) ) ;
#5858=FACE_OUTER_BOUND ( 'NONE', #24697, .T. ) ;
#5862=PLANE ( 'NONE',  #31829 ) ;
#5864=CARTESIAN_POINT ( 'NONE',  ( -0.04155248107635943489, 0.4523094957185410658, 0.1288470070525102595 ) ) ;
#5866=CARTESIAN_POINT ( 'NONE',  ( 0.01548846960721238578, 0.07651041855108486889, -0.5222379212565272377 ) ) ;
#5870=CARTESIAN_POINT ( 'NONE',  ( -0.03674260963082939813, 0.3145436874713448683, 0.3636070162938564443 ) ) ;
#5882=EDGE_CURVE ( 'NONE', #38697, #4624, #37906, .T. ) ;
#5886=EDGE_CURVE ( 'NONE', #24301, #30304, #11627, .T. ) ;
#5892=CARTESIAN_POINT ( 'NONE',  ( 0.04230170315644368045, 0.2824006788359467723, -0.3740536075335736399 ) ) ;
#5899=DIRECTION ( 'NONE',  ( 7.967889981520751253E-15, 0.9901182710308658041, 0.1402348365095101024 ) ) ;
#5909=VERTEX_POINT ( 'NONE', #8518 ) ;
#5913=VERTEX_POINT ( 'NONE', #33609 ) ;
#5914=DIRECTION ( 'NONE',  ( 1.000000000000000000, 2.280301054154495132E-31, -1.664003471950577689E-31 ) ) ;
#5934=AXIS2_PLACEMENT_3D ( 'NONE', #28475, #9754, #350 ) ;
#5940=CARTESIAN_POINT ( 'NONE',  ( -0.01548846960688982435, -0.5198120922917083275, 0.07362328916747526431 ) ) ;
#5946=LINE ( 'NONE', #24489, #26374 ) ;
#5950=EDGE_LOOP ( 'NONE', ( #21037, #37396, #15447, #21709 ) ) ;
#5951=CARTESIAN_POINT ( 'NONE',  ( 0.03868264068766662234, 0.4417248602032609606, -0.1788646266443645882 ) ) ;
#5953=ADVANCED_FACE ( 'NONE', ( #29944 ), #15565, .T. ) ;
#5962=ADVANCED_FACE ( 'NONE', ( #11020 ), #11207, .T. ) ;
#5965=CARTESIAN_POINT ( 'NONE',  ( -0.03303708955568582240, -0.5155567402493581586, 0.07470075307485188332 ) ) ;
#5976=CIRCLE ( 'NONE', #28973, 0.01499999999999995261 ) ;
#5987=CARTESIAN_POINT ( 'NONE',  ( 0.03309060444528739986, -0.2303206394829937220, 0.4671006372792966821 ) ) ;
#5994=ORIENTED_EDGE ( 'NONE', *, *, #33815, .T. ) ;
#6002=DIRECTION ( 'NONE',  ( -1.000000000000000000, -2.280301054154495132E-31, 1.664003471950577689E-31 ) ) ;
#6006=EDGE_LOOP ( 'NONE', ( #7813, #31891, #14351 ) ) ;
#6013=CARTESIAN_POINT ( 'NONE',  ( -0.05634301242525816683, -0.2614060064472246703, 0.3772872482281147688 ) ) ;
#6020=FACE_OUTER_BOUND ( 'NONE', #25602, .T. ) ;
#6034=CARTESIAN_POINT ( 'NONE',  ( -0.03674260963082456866, -0.3145436874713427589, -0.3636070162938578876 ) ) ;
#6037=CARTESIAN_POINT ( 'NONE',  ( -0.03301200226531778026, -0.2303790867044788193, 0.4673050311136081603 ) ) ;
#6040=CARTESIAN_POINT ( 'NONE',  ( -0.04047076529493147390, 0.06272252650431850429, -0.4973259435627279679 ) ) ;
#6047=CARTESIAN_POINT ( 'NONE',  ( 0.03674078017396070067, -0.4430116966224423858, -0.1867947199041681827 ) ) ;
#6052=CARTESIAN_POINT ( 'NONE',  ( 0.05561310505367052931, -0.2541457526436871062, -0.3845267872006568055 ) ) ;
#6060=CARTESIAN_POINT ( 'NONE',  ( -0.05634307799789353005, -0.4395998308137162858, 0.1320249839696058525 ) ) ;
#6062=CARTESIAN_POINT ( 'NONE',  ( 0.02953079040095728247, 0.000000000000000000, 0.000000000000000000 ) ) ;
#6063=CARTESIAN_POINT ( 'NONE',  ( -0.01548846960707490547, 0.5346638663566671834, 0.07572681171513505338 ) ) ;
#6064=AXIS2_PLACEMENT_3D ( 'NONE', #18114, #37241, #33958 ) ;
#6075=CARTESIAN_POINT ( 'NONE',  ( -0.05137569054208737662, 0.2590973494995081339, 0.3946951280584610200 ) ) ;
#6077=CIRCLE ( 'NONE', #23854, 0.01499999999999998730 ) ;
#6083=CIRCLE ( 'NONE', #6737, 0.01500000000000001159 ) ;
#6109=CARTESIAN_POINT ( 'NONE',  ( 0.08978098643734212791, 0.000000000000000000, 0.000000000000000000 ) ) ;
#6145=DIRECTION ( 'NONE',  ( -0.3515883117872521946, -1.971562692052851690E-16, -0.9361547195921140485 ) ) ;
#6159=ORIENTED_EDGE ( 'NONE', *, *, #20846, .T. ) ;
#6161=EDGE_LOOP ( 'NONE', ( #8569, #3636, #19069, #27869 ) ) ;
#6163=ORIENTED_EDGE ( 'NONE', *, *, #28999, .F. ) ;
#6172=DIRECTION ( 'NONE',  ( -1.000000000000000000, -2.341930812374887555E-31, 1.664003471950578127E-31 ) ) ;
#6174=CARTESIAN_POINT ( 'NONE',  ( -0.04947837552028811620, -0.4418396724781367690, 0.1804413675089040769 ) ) ;
#6179=VECTOR ( 'NONE', #20544, 39.37007874015748143 ) ;
#6182=EDGE_CURVE ( 'NONE', #16401, #20994, #13227, .T. ) ;
#6191=CARTESIAN_POINT ( 'NONE',  ( 0.05076679145662076759, -0.2374648372614181491, 0.4099810879409593878 ) ) ;
#6197=EDGE_CURVE ( 'NONE', #38396, #26954, #23679, .T. ) ;
#6198=CARTESIAN_POINT ( 'NONE',  ( 0.01548846960707524721, 0.000000000000000000, 0.000000000000000000 ) ) ;
#6213=ORIENTED_EDGE ( 'NONE', *, *, #18563, .F. ) ;
#6217=CARTESIAN_POINT ( 'NONE',  ( 0.05283102792148738902, 0.4315398646667468197, -0.1819478359276330837 ) ) ;
#6250=CARTESIAN_POINT ( 'NONE',  ( -0.04140212552917823391, 0.01694508110950332727, 0.4702784328063239760 ) ) ;
#6256=CARTESIAN_POINT ( 'NONE',  ( -0.01548846960707421332, 0.07651041855119253277, -0.5222379212568226681 ) ) ;
#6267=AXIS2_PLACEMENT_3D ( 'NONE', #3808, #31799, #580 ) ;
#6270=EDGE_LOOP ( 'NONE', ( #9050, #40098, #24235, #27073 ) ) ;
#6283=CIRCLE ( 'NONE', #39126, 0.01499999999999995434 ) ;
#6284=CARTESIAN_POINT ( 'NONE',  ( -0.04285534776242241189, 0.3459954891507885377, -0.3537381284079011423 ) ) ;
#6286=CARTESIAN_POINT ( 'NONE',  ( -0.01548846960707490547, 0.5198120922912040642, 0.07362328916749247276 ) ) ;
#6290=CARTESIAN_POINT ( 'NONE',  ( -0.05269191099235786407, 0.2790572191958478054, 0.3764802596566349524 ) ) ;
#6304=DIRECTION ( 'NONE',  ( 1.000000000000000000, 2.280301054154495132E-31, -1.664003471950577689E-31 ) ) ;
#6306=AXIS2_PLACEMENT_3D ( 'NONE', #9832, #7550, #31855 ) ;
#6316=ORIENTED_EDGE ( 'NONE', *, *, #14046, .F. ) ;
#6321=FACE_OUTER_BOUND ( 'NONE', #15826, .T. ) ;
#6341=CARTESIAN_POINT ( 'NONE',  ( 0.01548846960712797240, 0.07651041855115807422, 0.5222379212567064277 ) ) ;
#6346=DIRECTION ( 'NONE',  ( 1.000000000000000000, 2.280301054154495132E-31, -1.664003471950577689E-31 ) ) ;
#6359=CARTESIAN_POINT ( 'NONE',  ( 0.01548846960707524721, 0.000000000000000000, 0.000000000000000000 ) ) ;
#6360=ORIENTED_EDGE ( 'NONE', *, *, #37822, .T. ) ;
#6362=CARTESIAN_POINT ( 'NONE',  ( -0.05634301242525809744, -0.4396003943662958324, -0.1320237143668771818 ) ) ;
#6377=ORIENTED_EDGE ( 'NONE', *, *, #12396, .T. ) ;
#6378=ORIENTED_EDGE ( 'NONE', *, *, #28608, .F. ) ;
#6381=CARTESIAN_POINT ( 'NONE',  ( -0.01548846960707318636, -0.5203207976467986162, 0.08861466064781882424 ) ) ;
#6397=CARTESIAN_POINT ( 'NONE',  ( -0.03174060074381365032, 0.4701996045334384533, 0.2325360656123088010 ) ) ;
#6422=CARTESIAN_POINT ( 'NONE',  ( 0.02953079040095728247, 0.000000000000000000, 0.000000000000000000 ) ) ;
#6438=CARTESIAN_POINT ( 'NONE',  ( -0.03674260963082575521, 0.04074834683009517095, 0.4790483961530583312 ) ) ;
#6452=EDGE_LOOP ( 'NONE', ( #31543, #15427, #26564, #3095 ) ) ;
#6456=CARTESIAN_POINT ( 'NONE',  ( 0.04047161733259613953, 0.4536038223829707006, 0.2133268955647583121 ) ) ;
#6458=CARTESIAN_POINT ( 'NONE',  ( 0.04229974373173535362, -0.2824305679197178232, -0.3740363831607549927 ) ) ;
#6465=ORIENTED_EDGE ( 'NONE', *, *, #24649, .T. ) ;
#6478=CARTESIAN_POINT ( 'NONE',  ( -0.04293701532779567454, 0.2295363440003043154, 0.4381116105132950023 ) ) ;
#6480=CARTESIAN_POINT ( 'NONE',  ( -0.03642997641689288413, -0.4544357765433681418, -0.2357005667431724405 ) ) ;
#6482=FACE_OUTER_BOUND ( 'NONE', #18724, .T. ) ;
#6489=CARTESIAN_POINT ( 'NONE',  ( 0.04230188431063448828, 0.2683773510969753029, -0.3842417364743022090 ) ) ;
#6491=ORIENTED_EDGE ( 'NONE', *, *, #27622, .F. ) ;
#6502=CARTESIAN_POINT ( 'NONE',  ( -0.8248651029816859159, -3.413936256264365647E-16, 0.6154198107346400271 ) ) ;
#6503=CARTESIAN_POINT ( 'NONE',  ( 0.03301162916268060576, 0.3732432789822053287, -0.3635092914618242577 ) ) ;
#6505=DIRECTION ( 'NONE',  ( 0.000000000000000000, 3.330669073875469621E-16, 1.000000000000000000 ) ) ;
#6508=ORIENTED_EDGE ( 'NONE', *, *, #29068, .F. ) ;
#6520=DIRECTION ( 'NONE',  ( 0.000000000000000000, 0.1725921171157359935, 0.9849933812516245002 ) ) ;
#6525=DIRECTION ( 'NONE',  ( 1.000000000000000000, 2.341930812374887555E-31, -1.664003471950578127E-31 ) ) ;
#6543=B_SPLINE_CURVE_WITH_KNOTS ( 'NONE', 3,
 ( #32065, #5987, #28966, #16424, #832, #37268, #3873, #18549, #15476, #28031, #40558, #12379, #9280, #35541, #24934, #13341, #9085, #12575 ),
 .UNSPECIFIED., .F., .F.,
 ( 4, 2, 2, 2, 2, 2, 2, 2, 4 ),
 ( -0.003133633995111254067, -0.002350221109836764244, -0.001566808224562274855, -0.0007833953392877854652, 1.754598670435786323E-08, 0.0007834304312611941809, 0.001566843316535683137, 0.002350256201810172960, 0.003133669087084662783 ),
 .UNSPECIFIED. ) ;
#6550=CARTESIAN_POINT ( 'NONE',  ( -0.03662792686184423302, -0.04111994379180376746, 0.4792679903722390500 ) ) ;
#6556=ORIENTED_EDGE ( 'NONE', *, *, #28608, .T. ) ;
#6558=EDGE_LOOP ( 'NONE', ( #9389, #18727, #7621 ) ) ;
#6576=CARTESIAN_POINT ( 'NONE',  ( -0.01548846960707524721, 0.000000000000000000, 0.000000000000000000 ) ) ;
#6578=DIRECTION ( 'NONE',  ( 0.3468893892380794930, 0.7396492646830054030, 0.5767033179095832907 ) ) ;
#6584=CARTESIAN_POINT ( 'NONE',  ( -0.04308558661660367994, 0.4494156853470179791, 0.2058346122081028406 ) ) ;
#6587=ORIENTED_EDGE ( 'NONE', *, *, #15550, .F. ) ;
#6590=FACE_BOUND ( 'NONE', #21583, .T. ) ;
#6597=EDGE_LOOP ( 'NONE', ( #12900, #2488, #13690, #27536, #28097, #11735, #13854, #29456, #17517, #4447, #27727, #12541, #26582, #3434 ) ) ;
#6603=CIRCLE ( 'NONE', #11872, 0.01499999999999995434 ) ;
#6635=CIRCLE ( 'NONE', #8607, 0.5399999999999999245 ) ;
#6636=CARTESIAN_POINT ( 'NONE',  ( -0.05252359774140137605, 0.009047791085684511042, 0.4689872004378276005 ) ) ;
#6656=EDGE_LOOP ( 'NONE', ( #10429, #1146, #18255, #40302 ) ) ;
#6657=CARTESIAN_POINT ( 'NONE',  ( -0.01895494625228198032, 0.2428766181966292015, -0.4598657641708846500 ) ) ;
#6663=EDGE_CURVE ( 'NONE', #22491, #24257, #5059, .T. ) ;
#6674=CARTESIAN_POINT ( 'NONE',  ( -0.03474824846560518876, 0.3591470389155430598, -0.3712557345097572403 ) ) ;
#6678=CARTESIAN_POINT ( 'NONE',  ( -0.04574984450154874482, -0.4390502118250590446, -0.2110542068117175485 ) ) ;
#6687=CARTESIAN_POINT ( 'NONE',  ( 0.02872242845530422264, 0.4768947642620191552, -0.2371557650701889286 ) ) ;
#6688=AXIS2_PLACEMENT_3D ( 'NONE', #6062, #19451, #9573 ) ;
#6691=CARTESIAN_POINT ( 'NONE',  ( -0.01548846960707524721, 0.000000000000000000, 0.000000000000000000 ) ) ;
#6701=CARTESIAN_POINT ( 'NONE',  ( -0.03662792686184342811, -0.2484399233013400432, -0.4119056456069905003 ) ) ;
#6702=VECTOR ( 'NONE', #31083, 39.37007874015748143 ) ;
#6727=FACE_OUTER_BOUND ( 'NONE', #18780, .T. ) ;
#6729=DIRECTION ( 'NONE',  ( 5.546678239835219551E-32, 0.9849933812516251663, -0.1725921171157328571 ) ) ;
#6737=AXIS2_PLACEMENT_3D ( 'NONE', #22957, #17927, #7280 ) ;
#6740=DIRECTION ( 'NONE',  ( 0.000000000000000000, 0.8090169943749455639, -0.5877852522924756906 ) ) ;
#6742=AXIS2_PLACEMENT_3D ( 'NONE', #1440, #13954, #14360 ) ;
#6744=DIRECTION ( 'NONE',  ( 0.3468893892380652821, -0.3199132558032009022, -0.8816593788960893630 ) ) ;
#6746=CARTESIAN_POINT ( 'NONE',  ( 0.1499999999999989120, -0.3880410510314797334, -0.3755318131854984420 ) ) ;
#6779=CARTESIAN_POINT ( 'NONE',  ( -0.03868649100028198617, -0.03360400204099364685, -0.4753701585314240030 ) ) ;
#6781=AXIS2_PLACEMENT_3D ( 'NONE', #33407, #2553, #30732 ) ;
#6782=DIRECTION ( 'NONE',  ( 7.114187483500656449E-15, 0.8834504764630435325, -0.4685245517976845409 ) ) ;
#6783=CYLINDRICAL_SURFACE ( 'NONE', #5367, 0.01500000000000001853 ) ;
#6784=EDGE_CURVE ( 'NONE', #37319, #35448, #32478, .T. ) ;
#6788=DIRECTION ( 'NONE',  ( 0.000000000000000000, -0.8090169943749413450, 0.5877852522924816858 ) ) ;
#6813=CARTESIAN_POINT ( 'NONE',  ( -0.01548846960707531660, -0.2372406987223689145, -0.4850946823762606330 ) ) ;
#6815=ORIENTED_EDGE ( 'NONE', *, *, #3684, .T. ) ;
#6834=AXIS2_PLACEMENT_3D ( 'NONE', #3956, #28862, #722 ) ;
#6838=CARTESIAN_POINT ( 'NONE',  ( 0.1499999999999994948, 0.4730347584886787082, 0.2341461249029790914 ) ) ;
#6845=CARTESIAN_POINT ( 'NONE',  ( -0.03171893264487783692, 0.07587196131163785606, 0.5190999561769922277 ) ) ;
#6848=ORIENTED_EDGE ( 'NONE', *, *, #3020, .T. ) ;
#6877=CYLINDRICAL_SURFACE ( 'NONE', #21174, 0.08139150547213643005 ) ;
#6882=CARTESIAN_POINT ( 'NONE',  ( -0.05634490452573035629, 0.2656249956367463527, -0.3742168499391961278 ) ) ;
#6892=CARTESIAN_POINT ( 'NONE',  ( 0.01548846960706664298, 0.09061086148576029398, -0.5171215251571253946 ) ) ;
#6895=CARTESIAN_POINT ( 'NONE',  ( 0.04047170147976451166, 0.4536011460193595246, -0.2133323880731119726 ) ) ;
#6898=CARTESIAN_POINT ( 'NONE',  ( 0.03159140494780057068, -0.2432984029592170083, 0.4277399113045166623 ) ) ;
#6906=AXIS2_PLACEMENT_3D ( 'NONE', #17220, #29766, #26897 ) ;
#6921=EDGE_CURVE ( 'NONE', #24870, #26513, #24324, .T. ) ;
#6931=VERTEX_POINT ( 'NONE', #11116 ) ;
#6934=ORIENTED_EDGE ( 'NONE', *, *, #17479, .F. ) ;
#6937=DIRECTION ( 'NONE',  ( 0.9378410757839522605, -0.1072489841977682656, 0.3300784330442477765 ) ) ;
#6954=LINE ( 'NONE', #4060, #38930 ) ;
#6955=CIRCLE ( 'NONE', #29319, 0.01499999999999995781 ) ;
#6956=CARTESIAN_POINT ( 'NONE',  ( 0.1499999999999994671, 0.5346638663566671834, 0.07572681171513505338 ) ) ;
#6963=ORIENTED_EDGE ( 'NONE', *, *, #17686, .F. ) ;
#6965=EDGE_CURVE ( 'NONE', #13311, #34957, #32843, .T. ) ;
#6970=EDGE_CURVE ( 'NONE', #25200, #27922, #34913, .T. ) ;
#6981=CARTESIAN_POINT ( 'NONE',  ( -0.02235124290213127279, -0.2417860359143738647, 0.4518977707513324171 ) ) ;
#6991=CARTESIAN_POINT ( 'NONE',  ( -0.01896968469604851451, -0.4667670904252342323, 0.2292592343991424197 ) ) ;
#7005=CARTESIAN_POINT ( 'NONE',  ( 0.05634206451479473882, -0.2613530514269480909, 0.3773282889206444057 ) ) ;
#7011=CARTESIAN_POINT ( 'NONE',  ( -0.03647060353176813374, 0.5060729159580379388, 0.07645842516612116890 ) ) ;
#7016=DIRECTION ( 'NONE',  ( 0.000000000000000000, -3.330669073875470114E-16, -1.000000000000000000 ) ) ;
#7039=CARTESIAN_POINT ( 'NONE',  ( -0.05283719472145168711, 0.03966590960886611644, 0.4666299489511758214 ) ) ;
#7052=CARTESIAN_POINT ( 'NONE',  ( -0.02869712619511913601, 0.4519224903895677770, -0.2102851490355765740 ) ) ;
#7053=CARTESIAN_POINT ( 'NONE',  ( -0.05269191099235946696, 0.004472488327044489738, 0.4686046460979745309 ) ) ;
#7064=CARTESIAN_POINT ( 'NONE',  ( -0.01548846960707545191, -0.5198120922912100594, 0.07362328916748400731 ) ) ;
#7067=ORIENTED_EDGE ( 'NONE', *, *, #876, .F. ) ;
#7080=CARTESIAN_POINT ( 'NONE',  ( -0.02872242845530505531, 0.3729171224323672984, -0.3802687114177490946 ) ) ;
#7087=CARTESIAN_POINT ( 'NONE',  ( 0.03303737228521517327, 0.4610015631984470952, -0.2426019986921478244 ) ) ;
#7089=ORIENTED_EDGE ( 'NONE', *, *, #35574, .T. ) ;
#7091=CARTESIAN_POINT ( 'NONE',  ( 0.01548846960712783535, -0.2450655194479442189, 0.4674710490748163472 ) ) ;
#7096=CARTESIAN_POINT ( 'NONE',  ( -0.01548846960707524721, 0.000000000000000000, 0.000000000000000000 ) ) ;
#7102=DIRECTION ( 'NONE',  ( 1.000000000000000000, 2.280301054154495132E-31, -1.664003471950577689E-31 ) ) ;
#7107=DIRECTION ( 'NONE',  ( -2.563099466555617214E-12, 0.9510565162951502005, -0.3090169943749580539 ) ) ;
#7114=ORIENTED_EDGE ( 'NONE', *, *, #1734, .F. ) ;
#7144=DIRECTION ( 'NONE',  ( -1.000000000000000000, -2.280301054154495132E-31, 1.664003471950577689E-31 ) ) ;
#7155=CARTESIAN_POINT ( 'NONE',  ( -0.01548846960712804005, -0.07651041855114824874, 0.5222379212567086482 ) ) ;
#7209=ORIENTED_EDGE ( 'NONE', *, *, #21595, .F. ) ;
#7219=EDGE_LOOP ( 'NONE', ( #15437, #7642, #1578 ) ) ;
#7233=CARTESIAN_POINT ( 'NONE',  ( 0.02235124290213229628, -0.4612278572487559236, -0.2234747101372517586 ) ) ;
#7234=ADVANCED_FACE ( 'NONE', ( #24588 ), #25593, .T. ) ;
#7256=CIRCLE ( 'NONE', #28949, 0.01499999999999995434 ) ;
#7264=DIRECTION ( 'NONE',  ( -1.000000000000000000, -2.280301054154495132E-31, 1.664003471950577689E-31 ) ) ;
#7267=ORIENTED_EDGE ( 'NONE', *, *, #10628, .T. ) ;
#7270=CARTESIAN_POINT ( 'NONE',  ( -0.04947837552028722108, 0.2513950290986471381, -0.4056869761633373206 ) ) ;
#7273=EDGE_CURVE ( 'NONE', #8761, #15212, #40608, .T. ) ;
#7280=DIRECTION ( 'NONE',  ( -1.416619696839556283E-11, 0.5877852522924840173, 0.8090169943749395687 ) ) ;
#7282=CARTESIAN_POINT ( 'NONE',  ( 0.02881195911414656183, 0.4889334074056470580, -0.09563129189200189617 ) ) ;
#7284=ORIENTED_EDGE ( 'NONE', *, *, #36892, .T. ) ;
#7286=CARTESIAN_POINT ( 'NONE',  ( 0.04155248107635906019, -0.2901916982059698502, 0.3701002694350353228 ) ) ;
#7287=CYLINDRICAL_SURFACE ( 'NONE', #33086, 0.1749999999999999889 ) ;
#7288=ORIENTED_EDGE ( 'NONE', *, *, #2259, .T. ) ;
#7290=DIRECTION ( 'NONE',  ( -1.000000000000000000, -2.280301054154495132E-31, 1.664003471950577689E-31 ) ) ;
#7298=DIRECTION ( 'NONE',  ( -1.000000000000000000, -2.341930812374887555E-31, 1.664003471950578127E-31 ) ) ;
#7321=CARTESIAN_POINT ( 'NONE',  ( 0.04229974373173647079, -0.4430055847546718328, 0.1530238331097731330 ) ) ;
#7326=SPHERICAL_SURFACE ( 'NONE', #40427, 0.01499999999999999944 ) ;
#7334=CARTESIAN_POINT ( 'NONE',  ( 0.03170953572518896840, 0.2433677181033278847, 0.4274019581173342242 ) ) ;
#7345=DIRECTION ( 'NONE',  ( -1.000000000000000000, -2.280301054154495132E-31, 1.664003471950577689E-31 ) ) ;
#7354=CARTESIAN_POINT ( 'NONE',  ( 0.08978098643734212791, -7.789101598130604663E-17, -0.3698489655877988391 ) ) ;
#7355=ORIENTED_EDGE ( 'NONE', *, *, #3684, .F. ) ;
#7357=ADVANCED_FACE ( 'NONE', ( #8936 ), #2732, .T. ) ;
#7360=DIRECTION ( 'NONE',  ( -0.000000000000000000, 0.8090169943749540016, 0.5877852522924639223 ) ) ;
#7397=DIRECTION ( 'NONE',  ( 1.702140497302371910E-12, 0.5877852522924655876, -0.8090169943749527803 ) ) ;
#7398=CIRCLE ( 'NONE', #30425, 0.5302738246768103902 ) ;
#7409=EDGE_LOOP ( 'NONE', ( #35700, #11546, #38204, #30505 ) ) ;
#7410=EDGE_LOOP ( 'NONE', ( #5544, #23731, #37068 ) ) ;
#7420=ORIENTED_EDGE ( 'NONE', *, *, #38297, .F. ) ;
#7426=CARTESIAN_POINT ( 'NONE',  ( 0.1499999999999989120, -0.3772621329472692908, -0.3651003739303438911 ) ) ;
#7452=CARTESIAN_POINT ( 'NONE',  ( -0.01895494625228186930, 0.4667936258712436226, -0.2292799240428185781 ) ) ;
#7470=CARTESIAN_POINT ( 'NONE',  ( -0.02238765564325672849, 0.5044129532808436789, -0.09031612285224611958 ) ) ;
#7471=ORIENTED_EDGE ( 'NONE', *, *, #20365, .T. ) ;
#7474=CIRCLE ( 'NONE', #12749, 0.01499999999999999424 ) ;
#7477=AXIS2_PLACEMENT_3D ( 'NONE', #1668, #32890, #10488 ) ;
#7486=CARTESIAN_POINT ( 'NONE',  ( -0.03171102739523436881, -0.4816844162602763602, -0.09938404130288475136 ) ) ;
#7487=ADVANCED_FACE ( 'NONE', ( #3362, #25403 ), #24798, .F. ) ;
#7488=VECTOR ( 'NONE', #3980, 39.37007874015748143 ) ;
#7496=CYLINDRICAL_SURFACE ( 'NONE', #39593, 0.01500000000000004281 ) ;
#7498=CARTESIAN_POINT ( 'NONE',  ( 0.04946288932099741908, 0.4418470831553572564, -0.1805342557390068048 ) ) ;
#7502=CARTESIAN_POINT ( 'NONE',  ( 0.03662792686184382362, -0.2484399233013401542, 0.4119056456069884464 ) ) ;
#7503=AXIS2_PLACEMENT_3D ( 'NONE', #10134, #31945, #25782 ) ;
#7504=CARTESIAN_POINT ( 'NONE',  ( -0.04211471441534227894, -0.2686849334112374477, -0.3844466239331229551 ) ) ;
#7507=FACE_OUTER_BOUND ( 'NONE', #5724, .T. ) ;
#7519=CIRCLE ( 'NONE', #37777, 0.1249999999999999584 ) ;
#7541=ORIENTED_EDGE ( 'NONE', *, *, #38924, .T. ) ;
#7544=CARTESIAN_POINT ( 'NONE',  ( 0.03170953572518595692, -0.4816881781209783608, 0.09938198567066194866 ) ) ;
#7550=DIRECTION ( 'NONE',  ( 1.000000000000000000, 2.532387540469236368E-12, 8.550494110633370620E-14 ) ) ;
#7555=B_SPLINE_CURVE_WITH_KNOTS ( 'NONE', 3,
 ( #852, #35178, #6981, #3891, #13574, #23041, #19942, #10474, #35566, #11501, #24065, #29810, #21162, #5290, #17854, #1848, #36591, #11285 ),
 .UNSPECIFIED., .F., .F.,
 ( 4, 2, 2, 2, 2, 2, 2, 2, 4 ),
 ( -0.002633528389679711239, -0.001975271857855709877, -0.001317015326031708514, -0.0006587587942077071518, -5.022623837057892116E-07, 0.0006577542694402955734, 0.001316010801264296936, 0.001974267333088298732, 0.002632523864912299661 ),
 .UNSPECIFIED. ) ;
#7557=CIRCLE ( 'NONE', #17405, 0.01500000000000002894 ) ;
#7558=CARTESIAN_POINT ( 'NONE',  ( 0.05634206451479729927, 0.2780979935378019574, 0.3651623763481127161 ) ) ;
#7567=CARTESIAN_POINT ( 'NONE',  ( -0.01548846960707524721, 0.000000000000000000, 0.000000000000000000 ) ) ;
#7568=CARTESIAN_POINT ( 'NONE',  ( -0.02872242845530498245, -0.3729171224323651890, 0.3802687114177512040 ) ) ;
#7570=ORIENTED_EDGE ( 'NONE', *, *, #2407, .F. ) ;
#7577=CARTESIAN_POINT ( 'NONE',  ( -0.05283102792148799270, 0.4315398646667473193, 0.1819478359276328061 ) ) ;
#7580=CARTESIAN_POINT ( 'NONE',  ( 0.05634301242525761172, 0.4396003943662958324, -0.1320237143668752666 ) ) ;
#7594=CARTESIAN_POINT ( 'NONE',  ( 0.01895494625228220584, 0.4667936258712425679, 0.2292799240428173291 ) ) ;
#7601=DIRECTION ( 'NONE',  ( 0.9378410757839518164, 0.1072489841977738861, 0.3300784330442475545 ) ) ;
#7617=AXIS2_PLACEMENT_3D ( 'NONE', #16179, #166, #35083 ) ;
#7620=ORIENTED_EDGE ( 'NONE', *, *, #25842, .T. ) ;
#7621=ORIENTED_EDGE ( 'NONE', *, *, #20365, .F. ) ;
#7630=ORIENTED_EDGE ( 'NONE', *, *, #29180, .T. ) ;
#7642=ORIENTED_EDGE ( 'NONE', *, *, #25092, .F. ) ;
#7655=DIRECTION ( 'NONE',  ( 1.000000000000000000, 2.280301054154495132E-31, -1.664003471950577689E-31 ) ) ;
#7675=DIRECTION ( 'NONE',  ( 0.000000000000000000, -0.8090169943749413450, 0.5877852522924816858 ) ) ;
#7678=ORIENTED_EDGE ( 'NONE', *, *, #13770, .F. ) ;
#7689=CARTESIAN_POINT ( 'NONE',  ( -0.04211471441534243160, 0.4486586774158433100, -0.1367340165256737128 ) ) ;
#7702=CARTESIAN_POINT ( 'NONE',  ( -0.04139678531769518804, -0.4420204940294896745, -0.1614859807034213779 ) ) ;
#7715=CARTESIAN_POINT ( 'NONE',  ( -0.04230258372739897216, -0.2788587125276409950, -0.3766249785157098073 ) ) ;
#7719=CARTESIAN_POINT ( 'NONE',  ( -0.03309058451312549970, 0.08822157290689555675, -0.5132714794726503937 ) ) ;
#7728=EDGE_CURVE ( 'NONE', #36370, #28193, #4523, .T. ) ;
#7734=ORIENTED_EDGE ( 'NONE', *, *, #31872, .F. ) ;
#7741=CARTESIAN_POINT ( 'NONE',  ( 0.02953079040095673430, -0.5250338024619264354, 0.07436286310882474215 ) ) ;
#7750=CARTESIAN_POINT ( 'NONE',  ( 0.03170874437002701302, -0.4481116538287146511, 0.2027256324086040840 ) ) ;
#7770=CARTESIAN_POINT ( 'NONE',  ( -0.05268850283020223846, -0.2791746226943827569, 0.3764045485075394604 ) ) ;
#7771=ORIENTED_EDGE ( 'NONE', *, *, #3625, .F. ) ;
#7793=CARTESIAN_POINT ( 'NONE',  ( 0.02231181081520686171, 0.5045902076536099568, 0.09028112709016243576 ) ) ;
#7797=CARTESIAN_POINT ( 'NONE',  ( 0.03309059653085726083, 0.08822156176787604442, -0.5132714489379864853 ) ) ;
#7799=CARTESIAN_POINT ( 'NONE',  ( 0.02953079040095700838, 0.4684706630666080063, -0.2484463060367437248 ) ) ;
#7808=CARTESIAN_POINT ( 'NONE',  ( 0.01548846960707524721, -0.09061086148575756005, -0.5171215251571035232 ) ) ;
#7811=CARTESIAN_POINT ( 'NONE',  ( -0.01548846960707524721, 0.3772621329472709006, 0.3651003739303413931 ) ) ;
#7813=ORIENTED_EDGE ( 'NONE', *, *, #20885, .F. ) ;
#7815=ORIENTED_EDGE ( 'NONE', *, *, #22056, .F. ) ;
#7824=CARTESIAN_POINT ( 'NONE',  ( -0.02869712619511821314, -0.4892154842446487240, -0.09550911579582112287 ) ) ;
#7842=CARTESIAN_POINT ( 'NONE',  ( 0.1499999999999996614, -0.09061086148574991339, 0.5171215251571054106 ) ) ;
#7854=LINE ( 'NONE', #4169, #31766 ) ;
#7867=CARTESIAN_POINT ( 'NONE',  ( 0.05082294681498966682, -0.04864283519431490677, -0.4711332289091952896 ) ) ;
#7870=CARTESIAN_POINT ( 'NONE',  ( -0.05269191099235458198, 0.4442874273374661787, -0.1490603884548157565 ) ) ;
#7882=ORIENTED_EDGE ( 'NONE', *, *, #16675, .F. ) ;
#7889=CARTESIAN_POINT ( 'NONE',  ( -0.02881329448201269683, -0.4889301291947605321, -0.09563270201326828923 ) ) ;
#7902=CARTESIAN_POINT ( 'NONE',  ( -0.05634304521267782806, -0.01028134608267022333, -0.4588823192046730948 ) ) ;
#7903=CARTESIAN_POINT ( 'NONE',  ( -0.05252359774140143156, -0.2829835766811571451, -0.3741004571325397543 ) ) ;
#7912=DIRECTION ( 'NONE',  ( 1.000000000000000000, 2.341930812374887555E-31, -1.664003471950578127E-31 ) ) ;
#7914=DIRECTION ( 'NONE',  ( 0.000000000000000000, 3.330669073875470114E-16, 1.000000000000000000 ) ) ;
#7932=DIRECTION ( 'NONE',  ( 0.000000000000000000, -0.9510565162951566398, -0.3090169943749374593 ) ) ;
#7937=CARTESIAN_POINT ( 'NONE',  ( 0.03303737228521656105, -0.4610015631984417106, 0.2426019986921502947 ) ) ;
#7944=CARTESIAN_POINT ( 'NONE',  ( 0.04293324258486896916, -0.07181764475132801362, 0.4893676133895067393 ) ) ;
#7947=EDGE_CURVE ( 'NONE', #3369, #5616, #19099, .T. ) ;
#7948=CARTESIAN_POINT ( 'NONE',  ( 0.03868649100028154209, -0.2522293598345311527, -0.4043344736883377477 ) ) ;
#7955=CARTESIAN_POINT ( 'NONE',  ( -0.05562144613422700945, 0.4316454521248592191, -0.1615915407302009887 ) ) ;
#7959=DIRECTION ( 'NONE',  ( -1.000000000000000000, -2.280301054154495132E-31, 1.664003471950577689E-31 ) ) ;
#7960=CARTESIAN_POINT ( 'NONE',  ( -0.05543910610525103894, -0.2873579635174355329, 0.3608851239303187408 ) ) ;
#7963=EDGE_LOOP ( 'NONE', ( #27393, #22287 ) ) ;
#7965=CIRCLE ( 'NONE', #13231, 0.5400000000000019229 ) ;
#7976=DIRECTION ( 'NONE',  ( 1.000000000000000000, 2.341930812374887555E-31, -1.664003471950578127E-31 ) ) ;
#7988=CARTESIAN_POINT ( 'NONE',  ( 0.03868649100028150045, 0.4417196792138944339, 0.1788567627196042398 ) ) ;
#7998=AXIS2_PLACEMENT_3D ( 'NONE', #12939, #38022, #18483 ) ;
#8005=EDGE_CURVE ( 'NONE', #12964, #38697, #8876, .T. ) ;
#8049=DIRECTION ( 'NONE',  ( 1.000000000000000000, 2.341930812374887555E-31, -1.664003471950578127E-31 ) ) ;
#8057=CIRCLE ( 'NONE', #888, 0.01500000000000006016 ) ;
#8060=CIRCLE ( 'NONE', #35648, 0.5302738246768091690 ) ;
#8073=LINE ( 'NONE', #16943, #17953 ) ;
#8075=ORIENTED_EDGE ( 'NONE', *, *, #6970, .T. ) ;
#8076=EDGE_LOOP ( 'NONE', ( #20147, #33956, #34296, #8797 ) ) ;
#8096=CARTESIAN_POINT ( 'NONE',  ( 0.05634301242525739661, -0.4332457820339863930, -0.1515812001271571730 ) ) ;
#8098=AXIS2_PLACEMENT_3D ( 'NONE', #27864, #29016, #501 ) ;
#8099=CARTESIAN_POINT ( 'NONE',  ( -0.03478556507500174533, 0.2420934825333293239, -0.4561854036929720024 ) ) ;
#8100=DIRECTION ( 'NONE',  ( -1.000000000000000000, -2.341930812374887555E-31, 1.664003471950578127E-31 ) ) ;
#8113=CARTESIAN_POINT ( 'NONE',  ( -0.05543910610525095567, -0.2544236545520495163, -0.3848133000241401036 ) ) ;
#8115=VECTOR ( 'NONE', #7345, 39.37007874015748143 ) ;
#8119=ADVANCED_FACE ( 'NONE', ( #22422 ), #37482, .T. ) ;
#8128=FACE_OUTER_BOUND ( 'NONE', #28519, .T. ) ;
#8139=EDGE_CURVE ( 'NONE', #28193, #28482, #38801, .T. ) ;
#8149=CARTESIAN_POINT ( 'NONE',  ( 0.04575106512774491235, -0.4390484599015547218, 0.2110503898921168298 ) ) ;
#8158=VECTOR ( 'NONE', #8993, 39.37007874015748143 ) ;
#8164=CARTESIAN_POINT ( 'NONE',  ( 0.04575106512774668177, 0.3363942840372686205, 0.3523417416125865231 ) ) ;
#8167=CARTESIAN_POINT ( 'NONE',  ( -0.04582889109739281958, 0.4389390569944021658, -0.2108010426992259212 ) ) ;
#8180=AXIS2_PLACEMENT_3D ( 'NONE', #34654, #3183, #9960 ) ;
#8184=DIRECTION ( 'NONE',  ( 0.3468893892380644495, 0.7396492646828584094, -0.5767033179097805773 ) ) ;
#8192=ORIENTED_EDGE ( 'NONE', *, *, #27855, .F. ) ;
#8197=DIRECTION ( 'NONE',  ( -1.000000000000000000, -2.280301054154495132E-31, 1.664003471950577689E-31 ) ) ;
#8199=ORIENTED_EDGE ( 'NONE', *, *, #13739, .T. ) ;
#8202=CARTESIAN_POINT ( 'NONE',  ( 0.03662792686184341423, 0.4685177067346131263, 0.1089945633920604146 ) ) ;
#8213=DIRECTION ( 'NONE',  ( 2.532366176626899733E-12, -0.3090169943749382364, 0.9510565162951566398 ) ) ;
#8222=LINE ( 'NONE', #26949, #13369 ) ;
#8231=CARTESIAN_POINT ( 'NONE',  ( 0.1499999999999996336, 0.3232818887608630010, 0.4449593469062194107 ) ) ;
#8240=DIRECTION ( 'NONE',  ( 0.000000000000000000, -0.5877852522924371659, 0.8090169943749736525 ) ) ;
#8260=CARTESIAN_POINT ( 'NONE',  ( -0.01548846960707524721, -0.4638115001430989648, 0.2459753896937853235 ) ) ;
#8266=AXIS2_PLACEMENT_3D ( 'NONE', #34963, #18942, #13149 ) ;
#8279=CARTESIAN_POINT ( 'NONE',  ( 0.05269111014006781779, 0.009103832413167858503, -0.4686064687114369631 ) ) ;
#8291=EDGE_LOOP ( 'NONE', ( #4586, #21774, #2832, #1051 ) ) ;
#8294=DIRECTION ( 'NONE',  ( 0.3468893892380655042, -0.2594111197898628651, 0.9013177145509854160 ) ) ;
#8297=CARTESIAN_POINT ( 'NONE',  ( -0.03478556507500055878, 0.4639967941986962163, -0.2267627654641953261 ) ) ;
#8300=CIRCLE ( 'NONE', #32606, 0.01499999999999994393 ) ;
#8305=CARTESIAN_POINT ( 'NONE',  ( -0.01548846960688968731, -0.4638115001435005325, -0.2459753896940882756 ) ) ;
#8310=CARTESIAN_POINT ( 'NONE',  ( 0.04582889109739239630, -0.4389390569944004450, -0.2108010426992268926 ) ) ;
#8315=DIRECTION ( 'NONE',  ( 1.000000000000000000, 0.000000000000000000, 0.000000000000000000 ) ) ;
#8327=CARTESIAN_POINT ( 'NONE',  ( -0.02242905165739169857, -0.3548958552285863544, -0.3695186750059928360 ) ) ;
#8337=CARTESIAN_POINT ( 'NONE',  ( 0.02242828275838827656, -0.06992002095336109779, 0.5075510395145186315 ) ) ;
#8341=CARTESIAN_POINT ( 'NONE',  ( 0.05076541221973829288, 0.4633004642377209215, 0.09914728473420074406 ) ) ;
#8352=DIRECTION ( 'NONE',  ( -1.355854680848614260E-31, 3.330669073875470114E-16, 1.000000000000000000 ) ) ;
#8368=CARTESIAN_POINT ( 'NONE',  ( 0.03478489236951365360, 0.2420938338887054231, 0.4561872437641242839 ) ) ;
#8380=SPHERICAL_SURFACE ( 'NONE', #22421, 0.01499999999999999944 ) ;
#8382=LINE ( 'NONE', #11274, #6179 ) ;
#8387=ORIENTED_EDGE ( 'NONE', *, *, #34382, .T. ) ;
#8388=CARTESIAN_POINT ( 'NONE',  ( 0.1499999999999996059, -0.2306506793134098787, -0.4716198300880303784 ) ) ;
#8395=ORIENTED_EDGE ( 'NONE', *, *, #38297, .T. ) ;
#8396=ORIENTED_EDGE ( 'NONE', *, *, #20114, .T. ) ;
#8398=ORIENTED_EDGE ( 'NONE', *, *, #3854, .F. ) ;
#8404=ADVANCED_FACE ( 'NONE', ( #23235 ), #23452, .T. ) ;
#8406=EDGE_CURVE ( 'NONE', #32833, #17796, #26345, .T. ) ;
#8410=CARTESIAN_POINT ( 'NONE',  ( 0.05562144613422612127, 0.4316454521248598297, 0.1615915407302006557 ) ) ;
#8417=ADVANCED_FACE ( 'NONE', ( #23639 ), #36195, .T. ) ;
#8436=FACE_OUTER_BOUND ( 'NONE', #36805, .T. ) ;
#8439=CARTESIAN_POINT ( 'NONE',  ( -0.03662792686184387220, -0.4431041838557909784, -0.1872093443778377886 ) ) ;
#8463=DIRECTION ( 'NONE',  ( -1.000000000000000000, -2.280301054154495132E-31, 1.664003471950577689E-31 ) ) ;
#8474=CARTESIAN_POINT ( 'NONE',  ( 0.03171861681795883070, 0.07587220456997828544, -0.5191007718638542823 ) ) ;
#8491=CARTESIAN_POINT ( 'NONE',  ( -0.03171893264487601199, 0.4702476704888088332, -0.2325692314474739619 ) ) ;
#8500=ORIENTED_EDGE ( 'NONE', *, *, #1739, .T. ) ;
#8508=CARTESIAN_POINT ( 'NONE',  ( 0.1499999999999993561, 0.000000000000000000, 0.000000000000000000 ) ) ;
#8518=CARTESIAN_POINT ( 'NONE',  ( 0.02953079040095690777, -0.4684706630666085614, 0.2484463060367459175 ) ) ;
#8520=LINE ( 'NONE', #34220, #1570 ) ;
#8524=CARTESIAN_POINT ( 'NONE',  ( -0.02872242845530507266, 0.07817994906157174628, -0.5268390348591137640 ) ) ;
#8529=CARTESIAN_POINT ( 'NONE',  ( 0.02953079040094720373, -0.4684706630666299887, -0.2484463060367549936 ) ) ;
#8531=CARTESIAN_POINT ( 'NONE',  ( 0.04945776359514829357, 0.4635931069071551058, 0.1136454792236781391 ) ) ;
#8534=CARTESIAN_POINT ( 'NONE',  ( 0.01899496522503133639, -0.3622296354306509536, -0.3730445619378164324 ) ) ;
#8536=CARTESIAN_POINT ( 'NONE',  ( -0.02953079040095707777, -0.5250338024619264354, 0.07436286310882474215 ) ) ;
#8540=CARTESIAN_POINT ( 'NONE',  ( -0.04293701532779559127, -0.4875995331660226695, 0.08291810260646308162 ) ) ;
#8552=AXIS2_PLACEMENT_3D ( 'NONE', #645, #19335, #32070 ) ;
#8553=FACE_OUTER_BOUND ( 'NONE', #20243, .T. ) ;
#8554=LINE ( 'NONE', #24221, #15474 ) ;
#8564=ORIENTED_EDGE ( 'NONE', *, *, #34894, .F. ) ;
#8569=ORIENTED_EDGE ( 'NONE', *, *, #20978, .F. ) ;
#8575=CONICAL_SURFACE ( 'NONE', #26979, 0.5399999999999999245, 1.211529128687673262 ) ;
#8603=DIRECTION ( 'NONE',  ( -1.000000000000000000, -2.280301054154495132E-31, 1.664003471950577689E-31 ) ) ;
#8607=AXIS2_PLACEMENT_3D ( 'NONE', #31638, #9824, #19098 ) ;
#8612=DIRECTION ( 'NONE',  ( -1.000000000000000000, -2.280301054154495132E-31, 1.664003471950577689E-31 ) ) ;
#8617=ORIENTED_EDGE ( 'NONE', *, *, #2259, .F. ) ;
#8619=ORIENTED_EDGE ( 'NONE', *, *, #30344, .F. ) ;
#8628=ORIENTED_EDGE ( 'NONE', *, *, #15204, .T. ) ;
#8632=CARTESIAN_POINT ( 'NONE',  ( -0.04154009738085474857, -0.4416556227939096302, -0.1617111092119922766 ) ) ;
#8642=CARTESIAN_POINT ( 'NONE',  ( -0.04229883635637818329, -0.4470233673486266324, 0.1406638142521413615 ) ) ;
#8646=EDGE_CURVE ( 'NONE', #36862, #33486, #30937, .T. ) ;
#8648=DIRECTION ( 'NONE',  ( -0.9378410757839560352, 0.2807814858886596987, 0.2039996905746388478 ) ) ;
#8659=VECTOR ( 'NONE', #15126, 39.37007874015748143 ) ;
#8660=CARTESIAN_POINT ( 'NONE',  ( 0.03643058821096618188, -0.2291047292463120055, 0.4577947064495202500 ) ) ;
#8666=CARTESIAN_POINT ( 'NONE',  ( 0.02881195911414601712, 0.06013796869038309789, -0.4945549975361969719 ) ) ;
#8687=CARTESIAN_POINT ( 'NONE',  ( -0.02881329448201502830, 0.4517642754607751887, -0.2100174381953940073 ) ) ;
#8688=ORIENTED_EDGE ( 'NONE', *, *, #11422, .F. ) ;
#8692=CARTESIAN_POINT ( 'NONE',  ( -0.01548846960707504251, -0.09061086148575973886, 0.5171215251571027460 ) ) ;
#8696=EDGE_LOOP ( 'NONE', ( #10598, #697, #23032 ) ) ;
#8717=CARTESIAN_POINT ( 'NONE',  ( -0.02953079040095591551, -0.3810518745593868273, -0.3687679460475801196 ) ) ;
#8718=EDGE_CURVE ( 'NONE', #4225, #35619, #34257, .T. ) ;
#8721=CARTESIAN_POINT ( 'NONE',  ( -0.05078493045283998669, -0.2374933143169552507, 0.4099093267371753391 ) ) ;
#8723=EDGE_CURVE ( 'NONE', #13846, #10925, #19156, .T. ) ;
#8726=CARTESIAN_POINT ( 'NONE',  ( -0.05634115714581353074, 0.005221855766568654980, -0.4588864551388210922 ) ) ;
#8733=CARTESIAN_POINT ( 'NONE',  ( 0.05634402396114680800, -0.01030784378588360008, 0.4588801752140554968 ) ) ;
#8745=AXIS2_PLACEMENT_3D ( 'NONE', #25688, #3077, #38027 ) ;
#8761=VERTEX_POINT ( 'NONE', #25651 ) ;
#8762=DIRECTION ( 'NONE',  ( 0.000000000000000000, 0.5877852522924840173, 0.8090169943749395687 ) ) ;
#8770=CARTESIAN_POINT ( 'NONE',  ( -0.04947837552028187119, 0.3081459059633598341, 0.3644550506195312067 ) ) ;
#8775=CARTESIAN_POINT ( 'NONE',  ( 0.03158843595483482730, 0.3316344853930308645, -0.3635668653053517052 ) ) ;
#8791=CARTESIAN_POINT ( 'NONE',  ( 0.05268932808079795915, 0.2680477706051491715, -0.3844863582443084349 ) ) ;
#8797=ORIENTED_EDGE ( 'NONE', *, *, #8718, .F. ) ;
#8801=CARTESIAN_POINT ( 'NONE',  ( -0.02869942827333593627, 0.3396431753871648751, -0.3648167270360638814 ) ) ;
#8807=DIRECTION ( 'NONE',  ( -0.9378410757839568124, -0.2807814858886553133, 0.2039996905746412070 ) ) ;
#8829=DIRECTION ( 'NONE',  ( 1.000000000000000000, 2.280301054154495132E-31, -1.664003471950577689E-31 ) ) ;
#8831=CIRCLE ( 'NONE', #15388, 0.01500000000000003761 ) ;
#8848=CARTESIAN_POINT ( 'NONE',  ( 0.04229956186878620211, 0.4483852441756290275, -0.1364680347311786890 ) ) ;
#8858=ORIENTED_EDGE ( 'NONE', *, *, #23412, .F. ) ;
#8876=B_SPLINE_CURVE_WITH_KNOTS ( 'NONE', 3,
 ( #12342, #3090, #15632, #3483, #22228, #28788, #25505, #28590, #22845, #19337, #13347, #16640, #6550, #35552, #10061, #13561, #35365, #7155 ),
 .UNSPECIFIED., .F., .F.,
 ( 4, 2, 2, 2, 2, 2, 2, 2, 4 ),
 ( -0.002633528389679722082, -0.001975271857855721153, -0.001317015326031719790, -0.0006587587942077184275, -5.022623837174985950E-07, 0.0006577542694402834303, 0.001316010801264285227, 0.001974267333088286155, 0.002632523864912287084 ),
 .UNSPECIFIED. ) ;
#8895=ORIENTED_EDGE ( 'NONE', *, *, #1929, .T. ) ;
#8908=FACE_OUTER_BOUND ( 'NONE', #23544, .T. ) ;
#8920=CARTESIAN_POINT ( 'NONE',  ( 0.000000000000000000, 0.000000000000000000, 0.000000000000000000 ) ) ;
#8922=EDGE_CURVE ( 'NONE', #15637, #10835, #28332, .T. ) ;
#8924=ADVANCED_FACE ( 'NONE', ( #8128 ), #14524, .T. ) ;
#8936=FACE_OUTER_BOUND ( 'NONE', #12440, .T. ) ;
#8940=CARTESIAN_POINT ( 'NONE',  ( -0.05544444631433741166, -0.02030017825816498797, -0.4608552147122320641 ) ) ;
#8945=CARTESIAN_POINT ( 'NONE',  ( 0.03875673594170349345, -0.03328920108826790430, 0.4752375706209726602 ) ) ;
#8947=CARTESIAN_POINT ( 'NONE',  ( 0.01548846960706570797, -0.4730347584886935852, -0.2341461249029953284 ) ) ;
#8951=CARTESIAN_POINT ( 'NONE',  ( 0.04230258372739759826, 0.4443637212174459394, 0.1488268768076428383 ) ) ;
#8953=CARTESIAN_POINT ( 'NONE',  ( 0.02881408050861044082, -0.3393437137871890275, -0.3647498010034141425 ) ) ;
#8971=CARTESIAN_POINT ( 'NONE',  ( -0.04229956186878639640, 0.4483852441756294160, 0.1364680347311792996 ) ) ;
#8979=CARTESIAN_POINT ( 'NONE',  ( -0.04047161733259624361, 0.3430572239576530902, 0.3654812350069518434 ) ) ;
#8982=EDGE_CURVE ( 'NONE', #40212, #35830, #28305, .T. ) ;
#8985=CARTESIAN_POINT ( 'NONE',  ( 0.02953079040094807803, 0.2329676531120586647, 0.4763574306556516702 ) ) ;
#8993=DIRECTION ( 'NONE',  ( -1.000000000000000000, -2.341930812374887555E-31, 1.664003471950578127E-31 ) ) ;
#9004=CARTESIAN_POINT ( 'NONE',  ( 0.03170953572518810798, 0.3312786565686240969, -0.3635309226454341291 ) ) ;
#9016=( BOUNDED_SURFACE ( )  B_SPLINE_SURFACE ( 3, 2, ( 
 ( #14722, #39602, #24811 ),
 ( #8534, #21318, #5658 ),
 ( #18214, #30760, #15116 ),
 ( #8953, #2783, #15332 ),
 ( #27888, #9144, #21708 ),
 ( #12856, #12437, #19443 ),
 ( #28884, #19231, #3590 ),
 ( #25199, #15543, #40621 ),
 ( #6458, #10173, #31773 ),
 ( #12633, #3376, #28094 ),
 ( #25417, #9759, #6052 ),
 ( #15932, #22529, #24990 ),
 ( #37741, #141, #19029 ),
 ( #21924, #18839, #28694 ),
 ( #745, #22742, #25819 ),
 ( #38340, #3793, #18620 ),
 ( #22329, #37521, #28479 ),
 ( #31178, #31381, #34848 ) ),
 .UNSPECIFIED., .F., .F., .T. ) 
 B_SPLINE_SURFACE_WITH_KNOTS ( ( 4, 2, 2, 2, 2, 2, 2, 2, 4 ),
 ( 3, 3 ),
 ( -0.001532620576208848376, -0.0007637936630077624307, 5.033250193323623133E-06, 0.0007738601633944096770, 0.001542687076595495622, 0.002311513989796581785, 0.003080340902997667513, 0.003849167816198753242, 0.004617994729399839404 ),
 ( 0.000000000000000000, 1.000000000000000000 ),
 .UNSPECIFIED. ) 
 GEOMETRIC_REPRESENTATION_ITEM ( )  RATIONAL_B_SPLINE_SURFACE ( (
 ( 1.000000000000000000, 0.7283825911960419841, 1.000000000000000000),
 ( 1.000000000000000000, 0.7404385082114082195, 1.000000000000000000),
 ( 1.000000000000000000, 0.7521504257738304000, 1.000000000000000000),
 ( 1.000000000000000000, 0.7744497410761531642, 1.000000000000000000),
 ( 1.000000000000000000, 0.7845654757373292654, 1.000000000000000000),
 ( 1.000000000000000000, 0.8022083990892909799, 1.000000000000000000),
 ( 1.000000000000000000, 0.8094167424697321644, 1.000000000000000000),
 ( 1.000000000000000000, 0.8194491993618630010, 1.000000000000000000),
 ( 1.000000000000000000, 0.8220634900780660059, 1.000000000000000000),
 ( 1.000000000000000000, 0.8220705070823303151, 1.000000000000000000),
 ( 1.000000000000000000, 0.8194468812480828479, 1.000000000000000000),
 ( 1.000000000000000000, 0.8094220769839568508, 1.000000000000000000),
 ( 1.000000000000000000, 0.8022659121986730479, 1.000000000000000000),
 ( 1.000000000000000000, 0.7845681159034245677, 1.000000000000000000),
 ( 1.000000000000000000, 0.7744426415185311496, 1.000000000000000000),
 ( 1.000000000000000000, 0.7522890290928635482, 1.000000000000000000),
 ( 1.000000000000000000, 0.7403540167215398871, 1.000000000000000000),
 ( 1.000000000000000000, 0.7283825911960186694, 1.000000000000000000) ) ) 
 REPRESENTATION_ITEM ( '' )  SURFACE ( )  );
#9035=CARTESIAN_POINT ( 'NONE',  ( 0.03309057659885121516, 0.3730661755626903942, -0.3633900220890659005 ) ) ;
#9050=ORIENTED_EDGE ( 'NONE', *, *, #933, .T. ) ;
#9057=CARTESIAN_POINT ( 'NONE',  ( 0.01895494625228211910, 0.5124113341948440814, -0.08888305413160359214 ) ) ;
#9071=CARTESIAN_POINT ( 'NONE',  ( 0.01548846960707528191, -0.4638115001430989648, 0.2459753896937853235 ) ) ;
#9075=FACE_BOUND ( 'NONE', #22530, .T. ) ;
#9085=CARTESIAN_POINT ( 'NONE',  ( 0.03309057659885152047, -0.3730661755626882292, 0.3633900220890675103 ) ) ;
#9112=DIRECTION ( 'NONE',  ( 0.000000000000000000, 1.000000000000000000, -3.330669073875470607E-16 ) ) ;
#9123=CARTESIAN_POINT ( 'NONE',  ( -0.03474824846560347485, -0.07233741238826779663, 0.5114535313566185293 ) ) ;
#9129=CARTESIAN_POINT ( 'NONE',  ( -0.03171102739523230796, -0.05432883045314854803, -0.4888204606144185282 ) ) ;
#9133=ADVANCED_FACE ( 'NONE', ( #2184 ), #9016, .T. ) ;
#9140=FACE_OUTER_BOUND ( 'NONE', #22892, .T. ) ;
#9144=CARTESIAN_POINT ( 'NONE',  ( 0.04308558661661592015, -0.3346374335304956316, -0.3638133228716434187 ) ) ;
#9145=ORIENTED_EDGE ( 'NONE', *, *, #34325, .T. ) ;
#9162=CARTESIAN_POINT ( 'NONE',  ( -0.04230188431063472421, 0.4429734639576320965, 0.1531098457317267014 ) ) ;
#9169=CARTESIAN_POINT ( 'NONE',  ( -0.03874953289575077536, 0.2523958943867715687, 0.4040664878102117052 ) ) ;
#9175=CARTESIAN_POINT ( 'NONE',  ( 0.02953079040095700838, 0.2329676531120518090, 0.4763574306556300764 ) ) ;
#9187=CARTESIAN_POINT ( 'NONE',  ( 0.04229974373173431973, 0.2684538943183510384, -0.3841910309321978079 ) ) ;
#9193=EDGE_LOOP ( 'NONE', ( #19286, #18984, #3595, #15158 ) ) ;
#9203=ORIENTED_EDGE ( 'NONE', *, *, #19251, .T. ) ;
#9214=CARTESIAN_POINT ( 'NONE',  ( 0.02953079040095728247, 0.000000000000000000, 0.000000000000000000 ) ) ;
#9236=TOROIDAL_SURFACE ( 'NONE', #30266, 0.5250000000000000222, 0.01499999999999999944 ) ;
#9237=ADVANCED_FACE ( 'NONE', ( #38551 ), #3236, .T. ) ;
#9239=CARTESIAN_POINT ( 'NONE',  ( 0.01548846960706677829, 0.3772621329472856666, -0.3651003739303602669 ) ) ;
#9240=ORIENTED_EDGE ( 'NONE', *, *, #1446, .T. ) ;
#9247=ADVANCED_FACE ( 'NONE', ( #27836 ), #11787, .T. ) ;
#9255=CARTESIAN_POINT ( 'NONE',  ( -0.05138886601527748593, -0.4416142869301858398, 0.1669109982969966266 ) ) ;
#9267=EDGE_CURVE ( 'NONE', #4624, #3966, #7965, .T. ) ;
#9272=CARTESIAN_POINT ( 'NONE',  ( 0.04308558661660950168, -0.2425983775171404733, 0.4306836113028234547 ) ) ;
#9280=CARTESIAN_POINT ( 'NONE',  ( 0.05083665881508999534, -0.3162195626321993580, 0.3525671453250093235 ) ) ;
#9296=CARTESIAN_POINT ( 'NONE',  ( 0.02953079040095700838, 0.4684706630666080063, -0.2484463060367437248 ) ) ;
#9315=CARTESIAN_POINT ( 'NONE',  ( -0.01548846960707524721, 0.000000000000000000, 0.000000000000000000 ) ) ;
#9323=AXIS2_PLACEMENT_3D ( 'NONE', #37473, #28226, #93 ) ;
#9324=ORIENTED_EDGE ( 'NONE', *, *, #17176, .F. ) ;
#9326=CARTESIAN_POINT ( 'NONE',  ( -0.05616044724337281718, 0.01023656896654763504, 0.4592816919116773922 ) ) ;
#9332=CARTESIAN_POINT ( 'NONE',  ( -0.02238765564325250618, 0.06997643758149711679, -0.5076344429488346410 ) ) ;
#9337=ORIENTED_EDGE ( 'NONE', *, *, #6784, .F. ) ;
#9340=DIRECTION ( 'NONE',  ( -1.000000000000000000, -2.280301054154495132E-31, 1.664003471950577689E-31 ) ) ;
#9342=CARTESIAN_POINT ( 'NONE',  ( 0.03171893264485862313, 0.4702476704888156056, 0.2325692314474981925 ) ) ;
#9362=CARTESIAN_POINT ( 'NONE',  ( -0.05252049209742703367, 0.2830365943384567373, -0.3740706778132397714 ) ) ;
#9364=DIRECTION ( 'NONE',  ( 1.000000000000000000, 1.681422630952712846E-11, -5.294072836416825871E-12 ) ) ;
#9370=CARTESIAN_POINT ( 'NONE',  ( -0.03171893264487805203, 0.3665010048041807411, 0.3753642664049919864 ) ) ;
#9372=ADVANCED_FACE ( 'NONE', ( #20660 ), #21476, .T. ) ;
#9377=EDGE_CURVE ( 'NONE', #19775, #30304, #39510, .T. ) ;
#9383=FACE_OUTER_BOUND ( 'NONE', #28032, .T. ) ;
#9389=ORIENTED_EDGE ( 'NONE', *, *, #38323, .T. ) ;
#9392=LINE ( 'NONE', #31610, #17113 ) ;
#9425=CYLINDRICAL_SURFACE ( 'NONE', #29201, 0.1249999999999999584 ) ;
#9426=CARTESIAN_POINT ( 'NONE',  ( 0.04582889109739302080, 0.3361233334070958811, -0.3523147457849521991 ) ) ;
#9448=DIRECTION ( 'NONE',  ( -1.416619696839552082E-11, 0.9510565162951502005, -0.3090169943749580539 ) ) ;
#9449=CARTESIAN_POINT ( 'NONE',  ( 0.01548846960721252282, 0.2450655194478999765, 0.4674710490746267211 ) ) ;
#9456=ORIENTED_EDGE ( 'NONE', *, *, #6182, .T. ) ;
#9457=AXIS2_PLACEMENT_3D ( 'NONE', #4966, #17324, #30081 ) ;
#9479=CIRCLE ( 'NONE', #25920, 0.01500000000000001159 ) ;
#9492=CARTESIAN_POINT ( 'NONE',  ( -0.03170874437002482032, 0.4481116538287114315, 0.2027256324086049999 ) ) ;
#9497=ORIENTED_EDGE ( 'NONE', *, *, #40301, .F. ) ;
#9498=CARTESIAN_POINT ( 'NONE',  ( 0.01548846960707511190, -0.5346638663566677385, -0.07572681171513533094 ) ) ;
#9503=VERTEX_POINT ( 'NONE', #31726 ) ;
#9512=LINE ( 'NONE', #19935, #32244 ) ;
#9534=CIRCLE ( 'NONE', #5561, 0.01500000000000003587 ) ;
#9540=SHAPE_DEFINITION_REPRESENTATION ( #20986, #30390 ) ;
#9547=CARTESIAN_POINT ( 'NONE',  ( -0.04047076529493080083, -0.06272252650431732468, 0.4973259435627372382 ) ) ;
#9565=VECTOR ( 'NONE', #25217, 39.37007874015748854 ) ;
#9573=DIRECTION ( 'NONE',  ( 0.000000000000000000, -2.275957200481562704E-14, 1.000000000000000000 ) ) ;
#9580=CARTESIAN_POINT ( 'NONE',  ( -0.05634115714581183765, 0.2739512608647006742, -0.3681776108866004482 ) ) ;
#9582=CARTESIAN_POINT ( 'NONE',  ( -0.03303708955568357419, -0.4610021654188251605, -0.2426024699083967617 ) ) ;
#9586=CARTESIAN_POINT ( 'NONE',  ( -0.04762200653274744483, 0.3170437565186472462, 0.3633076762442032370 ) ) ;
#9590=CIRCLE ( 'NONE', #12887, 0.5400000000000007017 ) ;
#9623=ORIENTED_EDGE ( 'NONE', *, *, #11931, .T. ) ;
#9630=DIRECTION ( 'NONE',  ( 1.000000000000000000, 0.000000000000000000, 0.000000000000000000 ) ) ;
#9631=DIRECTION ( 'NONE',  ( 0.3468893892380796040, 0.3199132558029604834, -0.8816593788961709643 ) ) ;
#9655=ORIENTED_EDGE ( 'NONE', *, *, #37754, .F. ) ;
#9660=CARTESIAN_POINT ( 'NONE',  ( -0.05083665881508995371, -0.4630607685881625857, -0.09936361682460898015 ) ) ;
#9682=DIRECTION ( 'NONE',  ( 0.000000000000000000, 1.000000000000000000, -3.330669073875470607E-16 ) ) ;
#9689=PLANE ( 'NONE',  #13321 ) ;
#9695=CARTESIAN_POINT ( 'NONE',  ( 0.01548846960706648165, -0.3688619771573060646, 0.3775276577327108529 ) ) ;
#9699=CARTESIAN_POINT ( 'NONE',  ( -0.04157078424165206593, 0.4522175634759015850, 0.1290209392672064526 ) ) ;
#9730=CARTESIAN_POINT ( 'NONE',  ( 0.06980746140711582837, 0.000000000000000000, 0.000000000000000000 ) ) ;
#9734=DIRECTION ( 'NONE',  ( 0.000000000000000000, -0.9510565162951585272, 0.3090169943749324633 ) ) ;
#9736=CARTESIAN_POINT ( 'NONE',  ( 0.01895494625228212604, -0.4667936258712412911, -0.2292799240428205210 ) ) ;
#9737=DIRECTION ( 'NONE',  ( 1.000000000000000000, 2.341930812374887555E-31, -1.664003471950578127E-31 ) ) ;
#9742=CARTESIAN_POINT ( 'NONE',  ( -0.04945776359514338083, -0.03517487494623300348, 0.4760216296475739406 ) ) ;
#9745=DIRECTION ( 'NONE',  ( -1.000000000000000000, -2.280301054154496446E-31, -1.355854680848613603E-31 ) ) ;
#9752=FACE_OUTER_BOUND ( 'NONE', #12585, .T. ) ;
#9754=DIRECTION ( 'NONE',  ( -1.000000000000000000, -2.280301054154495132E-31, 1.664003471950577689E-31 ) ) ;
#9759=CARTESIAN_POINT ( 'NONE',  ( 0.05201782277453038256, -0.2617104306118866464, -0.3909705171288733738 ) ) ;
#9761=CARTESIAN_POINT ( 'NONE',  ( -0.03159140494780148661, 0.3316214887069900419, -0.3635694333040939141 ) ) ;
#9762=VERTEX_POINT ( 'NONE', #29862 ) ;
#9775=CARTESIAN_POINT ( 'NONE',  ( -0.02953079040095687308, 0.3810518745593911571, 0.3687679460475725701 ) ) ;
#9777=CARTESIAN_POINT ( 'NONE',  ( -0.03474824846561417463, -0.4640677240217945809, -0.2268448004460654477 ) ) ;
#9780=SPHERICAL_SURFACE ( 'NONE', #6267, 0.01499999999999999944 ) ;
#9781=EDGE_CURVE ( 'NONE', #21164, #28482, #32961, .T. ) ;
#9785=CARTESIAN_POINT ( 'NONE',  ( 0.05268932808079793140, 0.4428506128075155868, -0.1535014714533980418 ) ) ;
#9790=ORIENTED_EDGE ( 'NONE', *, *, #29588, .T. ) ;
#9795=CARTESIAN_POINT ( 'NONE',  ( -0.05634304521267749499, -0.01028123094841905914, 0.4588823192046724841 ) ) ;
#9800=CARTESIAN_POINT ( 'NONE',  ( 0.1499999999999993561, 0.09061086148575100974, -0.5171215251571038563 ) ) ;
#9817=ORIENTED_EDGE ( 'NONE', *, *, #21009, .T. ) ;
#9819=DIRECTION ( 'NONE',  ( 5.546678239835219551E-32, 0.9849933812516251663, -0.1725921171157328571 ) ) ;
#9824=DIRECTION ( 'NONE',  ( 1.000000000000000000, 2.280301054154495132E-31, -1.664003471950577689E-31 ) ) ;
#9828=DIRECTION ( 'NONE',  ( 0.000000000000000000, 0.7185945389471846134, 0.6954292836768403152 ) ) ;
#9832=CARTESIAN_POINT ( 'NONE',  ( 0.01548846960703768524, -0.5198120922912046193, 0.07362328916749273644 ) ) ;
#9833=CARTESIAN_POINT ( 'NONE',  ( -0.01548846960707463312, 0.3772621329472714558, -0.3651003739303419482 ) ) ;
#9848=CARTESIAN_POINT ( 'NONE',  ( 0.03654364704248821982, -0.2290829176602880712, -0.4574690890339243587 ) ) ;
#9849=ORIENTED_EDGE ( 'NONE', *, *, #19596, .T. ) ;
#9854=FACE_OUTER_BOUND ( 'NONE', #3492, .T. ) ;
#9870=CARTESIAN_POINT ( 'NONE',  ( -0.02869942827333608198, 0.06034320897027863062, -0.4947801815387833924 ) ) ;
#9872=FACE_OUTER_BOUND ( 'NONE', #26427, .T. ) ;
#9892=CARTESIAN_POINT ( 'NONE',  ( -0.04285427992854486112, 0.4878399728613377340, 0.08281491827193812605 ) ) ;
#9894=EDGE_CURVE ( 'NONE', #25917, #30159, #263, .T. ) ;
#9922=TOROIDAL_SURFACE ( 'NONE', #23104, 0.5250000000000000222, 0.01499999999999999944 ) ;
#9932=LINE ( 'NONE', #6838, #15262 ) ;
#9938=AXIS2_PLACEMENT_3D ( 'NONE', #18065, #30616, #2443 ) ;
#9942=CARTESIAN_POINT ( 'NONE',  ( -0.04047161733259035249, 0.06271464429810597041, 0.4973245071804685558 ) ) ;
#9945=DIRECTION ( 'NONE',  ( 0.000000000000000000, -0.5877852522925116618, -0.8090169943749194736 ) ) ;
#9956=ORIENTED_EDGE ( 'NONE', *, *, #12398, .F. ) ;
#9959=DIRECTION ( 'NONE',  ( 1.000000000000000000, 0.000000000000000000, 0.000000000000000000 ) ) ;
#9960=DIRECTION ( 'NONE',  ( 0.9378410757839558132, -0.3470650033817763158, 0.000000000000000000 ) ) ;
#9975=CIRCLE ( 'NONE', #36895, 0.01499999999999994914 ) ;
#9979=CARTESIAN_POINT ( 'NONE',  ( -0.04085667396267339546, 0.2941474082995404471, -0.3688418229621439060 ) ) ;
#9990=CARTESIAN_POINT ( 'NONE',  ( 0.03672447062657550193, 0.4430265621404723686, -0.1868507191434661263 ) ) ;
#9994=FACE_OUTER_BOUND ( 'NONE', #6656, .T. ) ;
#10029=ORIENTED_EDGE ( 'NONE', *, *, #6965, .T. ) ;
#10032=LINE ( 'NONE', #25272, #22355 ) ;
#10044=AXIS2_PLACEMENT_3D ( 'NONE', #39265, #5095, #23648 ) ;
#10052=CIRCLE ( 'NONE', #36320, 0.2149999999999999967 ) ;
#10061=CARTESIAN_POINT ( 'NONE',  ( -0.02869942827333604035, -0.06034320897027634772, 0.4947801815387837809 ) ) ;
#10069=AXIS2_PLACEMENT_3D ( 'NONE', #15622, #12333, #39898 ) ;
#10074=CARTESIAN_POINT ( 'NONE',  ( -0.03868649100028027227, -0.4417196792138980421, 0.1788567627196056276 ) ) ;
#10080=DIRECTION ( 'NONE',  ( 0.000000000000000000, -0.7185945389471800615, -0.6954292836768448671 ) ) ;
#10083=CARTESIAN_POINT ( 'NONE',  ( -0.02953079040095533611, -0.4684706630666171101, 0.2484463060367359533 ) ) ;
#10090=CARTESIAN_POINT ( 'NONE',  ( 0.1499999999999993561, -3.685538980774209949E-17, -0.1750000000000000167 ) ) ;
#10092=CARTESIAN_POINT ( 'NONE',  ( -0.01548846960688927792, 0.5198120922917062181, -0.07362328916747552798 ) ) ;
#10096=CARTESIAN_POINT ( 'NONE',  ( 0.02953079040094797741, -0.3810518745594024259, 0.3687679460475924431 ) ) ;
#10102=DIRECTION ( 'NONE',  ( -9.860761315262614725E-32, -0.9849933812516262766, 0.1725921171157263345 ) ) ;
#10104=CARTESIAN_POINT ( 'NONE',  ( -0.04762035657659158955, 0.4700462218748341914, 0.1075639008184042372 ) ) ;
#10106=CIRCLE ( 'NONE', #8098, 0.01500000000000005322 ) ;
#10121=AXIS2_PLACEMENT_3D ( 'NONE', #12904, #29351, #23185 ) ;
#10130=CARTESIAN_POINT ( 'NONE',  ( -0.06980746140711623082, 0.000000000000000000, 0.000000000000000000 ) ) ;
#10134=CARTESIAN_POINT ( 'NONE',  ( 0.01548846960706735942, 0.4638115001431208362, 0.2459753896937896811 ) ) ;
#10142=DIRECTION ( 'NONE',  ( 1.000000000000000000, 2.341930812374887555E-31, -1.664003471950578127E-31 ) ) ;
#10150=AXIS2_PLACEMENT_3D ( 'NONE', #14105, #21098, #33430 ) ;
#10153=CARTESIAN_POINT ( 'NONE',  ( -0.03170752374382829891, -0.05433200130546726042, 0.4888275802721887553 ) ) ;
#10166=VERTEX_POINT ( 'NONE', #6063 ) ;
#10167=CYLINDRICAL_SURFACE ( 'NONE', #35617, 0.01500000000000000291 ) ;
#10173=CARTESIAN_POINT ( 'NONE',  ( 0.05268932808079675872, -0.2828369400135328227, -0.3737413977152367894 ) ) ;
#10176=ADVANCED_FACE ( 'NONE', ( #16553 ), #6877, .F. ) ;
#10186=ORIENTED_EDGE ( 'NONE', *, *, #17003, .F. ) ;
#10188=EDGE_CURVE ( 'NONE', #35163, #34957, #4679, .T. ) ;
#10189=EDGE_CURVE ( 'NONE', #33895, #37954, #40213, .T. ) ;
#10194=CARTESIAN_POINT ( 'NONE',  ( -0.05634307799789452925, 0.2614070397638449950, 0.3772863199289416825 ) ) ;
#10201=DIRECTION ( 'NONE',  ( 0.3468893892380809363, -0.3199132558029670337, 0.8816593788961679667 ) ) ;
#10205=CARTESIAN_POINT ( 'NONE',  ( 0.05561310505366643536, 0.4442420632723487195, -0.1228816621031056378 ) ) ;
#10209=CARTESIAN_POINT ( 'NONE',  ( 0.03664605387828149402, -0.3149102792626756742, 0.3635688186731572125 ) ) ;
#10211=ORIENTED_EDGE ( 'NONE', *, *, #23752, .F. ) ;
#10216=AXIS2_PLACEMENT_3D ( 'NONE', #36449, #11147, #33354 ) ;
#10228=EDGE_LOOP ( 'NONE', ( #6587, #33583, #10876, #35490 ) ) ;
#10230=CIRCLE ( 'NONE', #33215, 0.2526340763130724976 ) ;
#10239=EDGE_CURVE ( 'NONE', #2531, #16637, #30360, .T. ) ;
#10245=CARTESIAN_POINT ( 'NONE',  ( 0.01548846960707524721, 0.000000000000000000, 0.000000000000000000 ) ) ;
#10269=VECTOR ( 'NONE', #38572, 39.37007874015748143 ) ;
#10270=DIRECTION ( 'NONE',  ( 1.000000000000000000, 2.341930812374887555E-31, -1.664003471950578127E-31 ) ) ;
#10277=ORIENTED_EDGE ( 'NONE', *, *, #4610, .F. ) ;
#10293=CARTESIAN_POINT ( 'NONE',  ( -0.03159140494780162539, -0.4819881711443532168, 0.09921162977303668584 ) ) ;
#10310=CARTESIAN_POINT ( 'NONE',  ( 0.1499999999999994671, 0.5203207976467930651, -0.08861466064782039243 ) ) ;
#10315=CARTESIAN_POINT ( 'NONE',  ( 0.02242828275838585836, -0.3548975010106722450, 0.3695194593235500702 ) ) ;
#10321=FACE_OUTER_BOUND ( 'NONE', #11694, .T. ) ;
#10322=DIRECTION ( 'NONE',  ( 1.000000000000000000, -1.195566832711449733E-12, 1.235392033522785979E-12 ) ) ;
#10376=CARTESIAN_POINT ( 'NONE',  ( -0.04574984450155356736, 0.4792536329485947433, -0.08732079948164463146 ) ) ;
#10385=ORIENTED_EDGE ( 'NONE', *, *, #12398, .T. ) ;
#10389=CARTESIAN_POINT ( 'NONE',  ( -0.02953079040095560326, -0.4684706630666131133, -0.2484463060367418652 ) ) ;
#10391=CIRCLE ( 'NONE', #16972, 0.1749999999999999889 ) ;
#10398=CARTESIAN_POINT ( 'NONE',  ( 0.03868649100028107024, -0.03360400204099643628, 0.4753701585314249467 ) ) ;
#10400=CARTESIAN_POINT ( 'NONE',  ( -0.01548846960707416301, -0.2450655194479855747, -0.4674710490749294234 ) ) ;
#10402=VERTEX_POINT ( 'NONE', #40332 ) ;
#10403=DIRECTION ( 'NONE',  ( -1.000000000000000000, -2.280301054154495132E-31, 1.664003471950577689E-31 ) ) ;
#10407=DIRECTION ( 'NONE',  ( 0.000000000000000000, -1.000000000000000000, 3.330669073875470607E-16 ) ) ;
#10411=CARTESIAN_POINT ( 'NONE',  ( -0.03159140494780058456, -0.2432984029592178132, -0.4277399113045173284 ) ) ;
#10429=ORIENTED_EDGE ( 'NONE', *, *, #20141, .F. ) ;
#10434=CARTESIAN_POINT ( 'NONE',  ( 0.05078310099560627566, -0.4632425114130950261, 0.09919524461158438222 ) ) ;
#10436=ORIENTED_EDGE ( 'NONE', *, *, #29594, .F. ) ;
#10442=CARTESIAN_POINT ( 'NONE',  ( 0.01548846960707497486, -0.2306506793133962230, 0.4716198300880369287 ) ) ;
#10445=CARTESIAN_POINT ( 'NONE',  ( 0.05279905671744913181, 0.2420693533014125209, 0.4010177630757486011 ) ) ;
#10473=CYLINDRICAL_SURFACE ( 'NONE', #33151, 0.1749999999999999889 ) ;
#10474=CARTESIAN_POINT ( 'NONE',  ( -0.04155248107635971938, -0.2623121065566123566, 0.3903559784317158776 ) ) ;
#10478=DIMENSIONAL_EXPONENTS ( 1.000000000000000000, 0.000000000000000000, 0.000000000000000000, 0.000000000000000000, 0.000000000000000000, 0.000000000000000000, 0.000000000000000000 ) ;
#10481=B_SPLINE_CURVE_WITH_KNOTS ( 'NONE', 3,
 ( #23754, #27034, #20880, #23967, #26844, #36274, #14681, #36696, #30728, #8096, #32989, #29926, #30121, #8310, #2143, #21067, #17763, #1952 ),
 .UNSPECIFIED., .F., .F.,
 ( 4, 2, 2, 2, 2, 2, 2, 2, 4 ),
 ( -0.003133633995111093605, -0.002350221109836652788, -0.001566808224562211971, -0.0007833953392877711537, 1.754598666966339371E-08, 0.0007834304312611109142, 0.001566843316535551298, 0.002350256201809991681, 0.003133669087084432932 ),
 .UNSPECIFIED. ) ;
#10488=DIRECTION ( 'NONE',  ( 0.000000000000000000, 0.9510565162951636342, 0.3090169943749164205 ) ) ;
#10489=DIRECTION ( 'NONE',  ( -1.000000000000000000, -2.280301054154495132E-31, 1.664003471950577689E-31 ) ) ;
#10496=ORIENTED_EDGE ( 'NONE', *, *, #17547, .F. ) ;
#10500=CARTESIAN_POINT ( 'NONE',  ( -0.01548846960707538425, 0.09319974324248773978, -0.5318964258758787089 ) ) ;
#10511=ORIENTED_EDGE ( 'NONE', *, *, #5434, .F. ) ;
#10515=DIRECTION ( 'NONE',  ( 0.9378410757839510392, -0.3470650033817896385, 0.000000000000000000 ) ) ;
#10531=CARTESIAN_POINT ( 'NONE',  ( -0.03309059653085701797, 0.08822156176788366333, 0.5132714489379847089 ) ) ;
#10538=DIRECTION ( 'NONE',  ( -0.000000000000000000, 0.8090169943749540016, 0.5877852522924639223 ) ) ;
#10566=CARTESIAN_POINT ( 'NONE',  ( -0.04229883635637986250, 0.4470233673486225245, -0.1406638142521441093 ) ) ;
#10572=DIRECTION ( 'NONE',  ( 1.787262988391355310E-31, 0.4685245517978617324, -0.8834504764629497187 ) ) ;
#10581=CARTESIAN_POINT ( 'NONE',  ( -0.05279185365593355023, -0.4315575715699441206, -0.1821760513485178312 ) ) ;
#10584=B_SPLINE_CURVE_WITH_KNOTS ( 'NONE', 3,
 ( #15122, #28487, #34663, #30963, #27680, #25204, #34457, #37747, #5849, #31182 ),
 .UNSPECIFIED., .F., .F.,
 ( 4, 2, 2, 2, 4 ),
 ( -0.003133633995111221975, -0.002350225496333395447, -0.001566816997555568487, -0.0007834084987777415257, 8.586881206085195117E-17 ),
 .UNSPECIFIED. ) ;
#10593=CARTESIAN_POINT ( 'NONE',  ( 0.04575106512774645279, 0.4390484599015499478, -0.2110503898921174404 ) ) ;
#10597=CARTESIAN_POINT ( 'NONE',  ( -0.05076541221973714102, -0.2374623881706939277, -0.4099867295868578343 ) ) ;
#10598=ORIENTED_EDGE ( 'NONE', *, *, #24589, .T. ) ;
#10606=CARTESIAN_POINT ( 'NONE',  ( -0.03868649100028244414, -0.3066017772948799180, -0.3648306000529315529 ) ) ;
#10607=CARTESIAN_POINT ( 'NONE',  ( 0.02238826743733661473, 0.06997574608431179899, 0.5076331681966321785 ) ) ;
#10608=CARTESIAN_POINT ( 'NONE',  ( 0.02881408050861775094, -0.4889293851945573643, -0.09562755728437868918 ) ) ;
#10619=CIRCLE ( 'NONE', #3499, 0.01499999999999999251 ) ;
#10628=EDGE_CURVE ( 'NONE', #26041, #21164, #38059, .T. ) ;
#10629=ADVANCED_FACE ( 'NONE', ( #9872 ), #13159, .T. ) ;
#10634=CARTESIAN_POINT ( 'NONE',  ( 0.03478489236951123886, -0.5086709597375885794, 0.08927530733452980483 ) ) ;
#10638=CARTESIAN_POINT ( 'NONE',  ( -0.1399999999999997358, 0.000000000000000000, 0.000000000000000000 ) ) ;
#10646=CARTESIAN_POINT ( 'NONE',  ( 0.02881408050861337250, 0.3393437137871819775, 0.3647498010034102567 ) ) ;
#10651=AXIS2_PLACEMENT_3D ( 'NONE', #1461, #10489, #13974 ) ;
#10652=EDGE_CURVE ( 'NONE', #15491, #5909, #20528, .T. ) ;
#10656=AXIS2_PLACEMENT_3D ( 'NONE', #38546, #19826, #38132 ) ;
#10659=CARTESIAN_POINT ( 'NONE',  ( -0.04047076529493409680, -0.3430644450807453505, 0.3654777640200593813 ) ) ;
#10663=ORIENTED_EDGE ( 'NONE', *, *, #19006, .F. ) ;
#10675=DIRECTION ( 'NONE',  ( 1.000000000000000000, 2.280301054154495132E-31, -1.664003471950577689E-31 ) ) ;
#10677=CARTESIAN_POINT ( 'NONE',  ( 0.01548846960707292615, -0.4638115001430591078, -0.2459753896938795814 ) ) ;
#10682=DIRECTION ( 'NONE',  ( -1.355854680848614260E-31, 3.330669073875470114E-16, 1.000000000000000000 ) ) ;
#10689=AXIS2_PLACEMENT_3D ( 'NONE', #1250, #16864, #36371 ) ;
#10691=DIRECTION ( 'NONE',  ( 1.664003471950577032E-31, 3.330669073875470607E-16, 1.000000000000000000 ) ) ;
#10698=CARTESIAN_POINT ( 'NONE',  ( -0.01548846960707531660, -0.09061086148575756005, -0.5171215251571035232 ) ) ;
#10705=CARTESIAN_POINT ( 'NONE',  ( -0.02953079040095693900, -0.09152108205202422186, -0.5223162075576424090 ) ) ;
#10710=B_SPLINE_CURVE_WITH_KNOTS ( 'NONE', 3,
 ( #927, #9736, #7233, #26004, #32341, #28669, #35247, #4162, #31534, #38525, #25392, #22919, #3347, #29279, #1128, #34818, #15906, #28451 ),
 .UNSPECIFIED., .F., .F.,
 ( 4, 2, 2, 2, 2, 2, 2, 2, 4 ),
 ( 0.0003425652276237726654, 0.001007165397454292104, 0.001671765567284811543, 0.002336365737115330982, 0.003000965906945850421, 0.003665566076776368993, 0.004330166246606887565, 0.004994766416437405702, 0.005659366586267923840 ),
 .UNSPECIFIED. ) ;
#10721=ORIENTED_EDGE ( 'NONE', *, *, #12441, .F. ) ;
#10726=CARTESIAN_POINT ( 'NONE',  ( 0.02953079040094790803, 0.4684706630666300442, 0.2484463060367509413 ) ) ;
#10741=EDGE_CURVE ( 'NONE', #2376, #10925, #34317, .T. ) ;
#10744=ADVANCED_FACE ( 'NONE', ( #16025 ), #25489, .T. ) ;
#10756=CIRCLE ( 'NONE', #33736, 0.2149999999999999967 ) ;
#10770=CARTESIAN_POINT ( 'NONE',  ( 0.01548846960707524721, -0.4770632572900511681, -0.2530032579707427454 ) ) ;
#10780=CARTESIAN_POINT ( 'NONE',  ( 0.03650577977170433447, -0.08362514765351604373, -0.5048437183011801332 ) ) ;
#10783=CARTESIAN_POINT ( 'NONE',  ( -0.05634490452572885749, 0.4348542811545068609, -0.1466173361067412140 ) ) ;
#10795=EDGE_CURVE ( 'NONE', #28660, #24301, #15941, .T. ) ;
#10798=EDGE_CURVE ( 'NONE', #28193, #20390, #28675, .T. ) ;
#10800=CARTESIAN_POINT ( 'NONE',  ( -0.05615703521555148736, -0.4336255412628354233, -0.1517287855096114135 ) ) ;
#10802=CARTESIAN_POINT ( 'NONE',  ( 0.01548846960707511190, 0.09319974324248773978, -0.5318964258758787089 ) ) ;
#10810=EDGE_CURVE ( 'NONE', #30304, #19775, #21932, .T. ) ;
#10815=CIRCLE ( 'NONE', #15424, 0.01499999999999997169 ) ;
#10818=CIRCLE ( 'NONE', #8745, 0.01499999999999994046 ) ;
#10819=EDGE_LOOP ( 'NONE', ( #6934, #40583, #10211 ) ) ;
#10826=CARTESIAN_POINT ( 'NONE',  ( -0.03868264068766667785, -0.2522289290439768683, -0.4043438810462546273 ) ) ;
#10827=CYLINDRICAL_SURFACE ( 'NONE', #25011, 0.01500000000000001506 ) ;
#10833=CARTESIAN_POINT ( 'NONE',  ( 0.01548846960707524721, 0.000000000000000000, 0.000000000000000000 ) ) ;
#10835=VERTEX_POINT ( 'NONE', #5071 ) ;
#10864=CARTESIAN_POINT ( 'NONE',  ( 0.01548846960707344483, 0.3688619771572954620, 0.3775276577326994176 ) ) ;
#10869=CARTESIAN_POINT ( 'NONE',  ( 0.01548846960721255751, -0.07651041855108323131, 0.5222379212565277928 ) ) ;
#10873=CARTESIAN_POINT ( 'NONE',  ( -0.04285561529641291473, -0.2295129201144956999, 0.4383679482630353785 ) ) ;
#10876=ORIENTED_EDGE ( 'NONE', *, *, #3904, .T. ) ;
#10888=CARTESIAN_POINT ( 'NONE',  ( 0.01548846960707524721, 0.000000000000000000, 0.000000000000000000 ) ) ;
#10896=ORIENTED_EDGE ( 'NONE', *, *, #12441, .T. ) ;
#10900=CARTESIAN_POINT ( 'NONE',  ( 0.03664605387828129279, 0.4430871221163660278, 0.1871485295462630150 ) ) ;
#10923=ORIENTED_EDGE ( 'NONE', *, *, #4471, .F. ) ;
#10925=VERTEX_POINT ( 'NONE', #32846 ) ;
#10930=B_SPLINE_CURVE_WITH_KNOTS ( 'NONE', 3,
 ( #1149, #19828, #10780, #23138, #10994, #7867, #26416, #4779, #4187, #17354 ),
 .UNSPECIFIED., .F., .F.,
 ( 4, 2, 2, 2, 4 ),
 ( -0.003133633995111182076, -0.002350225496333364222, -0.001566816997555546803, -0.0007834084987777293826, 8.760353553682875827E-17 ),
 .UNSPECIFIED. ) ;
#10931=EDGE_CURVE ( 'NONE', #26041, #35420, #17929, .T. ) ;
#10936=ADVANCED_FACE ( 'NONE', ( #20128 ), #23621, .T. ) ;
#10949=EDGE_LOOP ( 'NONE', ( #21003, #12426, #24899 ) ) ;
#10967=LENGTH_MEASURE_WITH_UNIT ( LENGTH_MEASURE( 0.02539999999999999897 ), #38919 );
#10993=ORIENTED_EDGE ( 'NONE', *, *, #6921, .T. ) ;
#10994=CARTESIAN_POINT ( 'NONE',  ( 0.04582705327698207570, -0.06484491888962944095, -0.4826014279685457153 ) ) ;
#10995=CARTESIAN_POINT ( 'NONE',  ( -0.01548846960712804005, -0.3688619771571925998, 0.3775276577326319161 ) ) ;
#10996=CARTESIAN_POINT ( 'NONE',  ( -0.05138886601527934556, 0.4416142869301819540, -0.1669109982970012063 ) ) ;
#11007=DIRECTION ( 'NONE',  ( 1.000000000000000000, 2.341930812374887555E-31, -1.664003471950578127E-31 ) ) ;
#11013=CARTESIAN_POINT ( 'NONE',  ( -0.05491348488830681551, -0.4472107100395448231, -0.1187682108873645004 ) ) ;
#11020=FACE_OUTER_BOUND ( 'NONE', #29635, .T. ) ;
#11021=CARTESIAN_POINT ( 'NONE',  ( 0.02953079040095728247, 0.000000000000000000, 0.000000000000000000 ) ) ;
#11023=CARTESIAN_POINT ( 'NONE',  ( -0.04047076529492847630, -0.2415772653364916533, -0.4392125161515710863 ) ) ;
#11024=ORIENTED_EDGE ( 'NONE', *, *, #14163, .F. ) ;
#11026=LINE ( 'NONE', #33011, #33122 ) ;
#11027=EDGE_CURVE ( 'NONE', #30248, #23130, #6083, .T. ) ;
#11031=CARTESIAN_POINT ( 'NONE',  ( 0.03309057659885129149, 0.2303206601891112093, 0.4671007096900143818 ) ) ;
#11032=CARTESIAN_POINT ( 'NONE',  ( -0.02953079040095652960, 0.2329676531120518090, 0.4763574306556300764 ) ) ;
#11039=ORIENTED_EDGE ( 'NONE', *, *, #8139, .F. ) ;
#11048=ADVANCED_FACE ( 'NONE', ( #30489 ), #7496, .T. ) ;
#11049=ORIENTED_EDGE ( 'NONE', *, *, #23932, .F. ) ;
#11050=EDGE_CURVE ( 'NONE', #10402, #14366, #19905, .T. ) ;
#11056=CARTESIAN_POINT ( 'NONE',  ( 0.04047043078436388108, -0.4923670751789738786, 0.09403524049742623125 ) ) ;
#11061=CYLINDRICAL_SURFACE ( 'NONE', #11557, 0.1249999999999999584 ) ;
#11064=CARTESIAN_POINT ( 'NONE',  ( 0.02953079040095494406, 0.3810518745593893808, 0.3687679460475793425 ) ) ;
#11066=CARTESIAN_POINT ( 'NONE',  ( 0.01895494625228227870, 0.3623053290766983792, -0.3730957266516553017 ) ) ;
#11072=CARTESIAN_POINT ( 'NONE',  ( -0.04308449196698653505, -0.3346410801914496691, 0.3638139224395113280 ) ) ;
#11074=B_SPLINE_CURVE_WITH_KNOTS ( 'NONE', 3,
 ( #35702, #7719, #20285, #1574, #4607, #20086, #17183, #14097, #26670, #23174 ),
 .UNSPECIFIED., .F., .F.,
 ( 4, 2, 2, 2, 4 ),
 ( 1.080346398583096594E-17, 0.0007746574062662946875, 0.001549314812532578750, 0.002323972218798862812, 0.003098629625065147525 ),
 .UNSPECIFIED. ) ;
#11085=FACE_OUTER_BOUND ( 'NONE', #20498, .T. ) ;
#11086=ORIENTED_EDGE ( 'NONE', *, *, #32300, .F. ) ;
#11094=EDGE_LOOP ( 'NONE', ( #32919, #30811, #32205, #33081 ) ) ;
#11097=CARTESIAN_POINT ( 'NONE',  ( 0.03868264068766623376, 0.4624969084406955200, 0.1149348357506039670 ) ) ;
#11105=CARTESIAN_POINT ( 'NONE',  ( 0.01548846960707524721, 0.000000000000000000, 0.000000000000000000 ) ) ;
#11116=CARTESIAN_POINT ( 'NONE',  ( 0.01548846960707528191, 0.2372406987223596164, -0.4850946823762614102 ) ) ;
#11117=ORIENTED_EDGE ( 'NONE', *, *, #19080, .F. ) ;
#11118=ORIENTED_EDGE ( 'NONE', *, *, #17176, .T. ) ;
#11132=CARTESIAN_POINT ( 'NONE',  ( 0.1499999999999993561, 0.000000000000000000, 0.000000000000000000 ) ) ;
#11147=DIRECTION ( 'NONE',  ( 1.000000000000000000, 2.280301054154495132E-31, -1.664003471950577689E-31 ) ) ;
#11148=EDGE_CURVE ( 'NONE', #34957, #3966, #21891, .T. ) ;
#11154=FACE_OUTER_BOUND ( 'NONE', #28594, .T. ) ;
#11180=CARTESIAN_POINT ( 'NONE',  ( -0.03474824846560887331, 0.5087747035359508896, -0.08925086559848302570 ) ) ;
#11190=ORIENTED_EDGE ( 'NONE', *, *, #20978, .T. ) ;
#11204=AXIS2_PLACEMENT_3D ( 'NONE', #27670, #15326, #1976 ) ;
#11205=CARTESIAN_POINT ( 'NONE',  ( 0.03171861681797973065, 0.5171399723077767518, -0.08825220573713646322 ) ) ;
#11207=SPHERICAL_SURFACE ( 'NONE', #18189, 0.01499999999999999944 ) ;
#11209=CARTESIAN_POINT ( 'NONE',  ( -0.05491348488830606611, -0.2919908616877284202, -0.3589493610278738922 ) ) ;
#11217=CARTESIAN_POINT ( 'NONE',  ( -0.03159140494780109804, 0.2432984029592196173, 0.4277399113045149415 ) ) ;
#11219=CARTESIAN_POINT ( 'NONE',  ( 0.01899496522503167292, -0.5123200228845833371, -0.08888615261743730567 ) ) ;
#11226=DIRECTION ( 'NONE',  ( 1.000000000000000000, 0.000000000000000000, 0.000000000000000000 ) ) ;
#11240=CARTESIAN_POINT ( 'NONE',  ( 0.04575185649130646820, -0.4792489163483505399, 0.08731931755211817803 ) ) ;
#11252=CARTESIAN_POINT ( 'NONE',  ( 0.03158843595483436933, -0.2432919444504229867, -0.4277514783322127201 ) ) ;
#11256=CARTESIAN_POINT ( 'NONE',  ( 0.03174060074380782165, 0.3664546090234515607, 0.3753288017716206459 ) ) ;
#11267=CARTESIAN_POINT ( 'NONE',  ( -0.05281452789367974132, -0.2421206024358327213, 0.4009379267244617684 ) ) ;
#11269=ORIENTED_EDGE ( 'NONE', *, *, #32755, .T. ) ;
#11270=CARTESIAN_POINT ( 'NONE',  ( 0.01548846960707278911, -0.5198120922912308206, 0.07362328916738182516 ) ) ;
#11271=AXIS2_PLACEMENT_3D ( 'NONE', #34000, #5805, #33195 ) ;
#11274=CARTESIAN_POINT ( 'NONE',  ( -1.694818351060767551E-32, 4.163336342344336410E-17, 0.1249999999999999584 ) ) ;
#11276=CARTESIAN_POINT ( 'NONE',  ( -0.05562144613422686373, 0.4441896308501013801, 0.1229845283801401928 ) ) ;
#11285=CARTESIAN_POINT ( 'NONE',  ( -0.01548846960712804005, -0.3688619771571925998, 0.3775276577326319161 ) ) ;
#11302=VECTOR ( 'NONE', #20370, 39.37007874015748143 ) ;
#11309=CARTESIAN_POINT ( 'NONE',  ( 0.02869942827333354235, -0.4519168387192312175, 0.2102852866807465304 ) ) ;
#11318=VERTEX_POINT ( 'NONE', #17876 ) ;
#11330=CARTESIAN_POINT ( 'NONE',  ( -0.01548846960721259221, -0.5203207976464859774, -0.08861466064783186936 ) ) ;
#11364=CARTESIAN_POINT ( 'NONE',  ( 0.01548846960707350381, -0.07651041855118986823, -0.5222379212568243334 ) ) ;
#11370=AXIS2_PLACEMENT_3D ( 'NONE', #5204, #16961, #17758 ) ;
#11382=CARTESIAN_POINT ( 'NONE',  ( -0.04575334816098172719, 0.4390433668671429590, -0.2110480141057351211 ) ) ;
#11399=( GEOMETRIC_REPRESENTATION_CONTEXT ( 3 ) GLOBAL_UNCERTAINTY_ASSIGNED_CONTEXT ( ( #15737 ) ) GLOBAL_UNIT_ASSIGNED_CONTEXT ( ( #1126, #26195, #23112 ) ) REPRESENTATION_CONTEXT ( 'NONE', 'WORKASPACE' ) );
#11403=CARTESIAN_POINT ( 'NONE',  ( -0.05543910610524967891, -0.4320206429437797868, -0.1617740274009885904 ) ) ;
#11415=DIRECTION ( 'NONE',  ( 1.000000000000000000, 2.280301054154495132E-31, -1.664003471950577689E-31 ) ) ;
#11416=CARTESIAN_POINT ( 'NONE',  ( -0.03877220711930252917, -0.3061923002804363692, -0.3649281646214425634 ) ) ;
#11417=AXIS2_PLACEMENT_3D ( 'NONE', #30743, #17985, #40191 ) ;
#11418=AXIS2_PLACEMENT_3D ( 'NONE', #3487, #25508, #26131 ) ;
#11420=CARTESIAN_POINT ( 'NONE',  ( -0.02953079040095639429, 0.4684706630666118365, 0.2484463060367366194 ) ) ;
#11422=EDGE_CURVE ( 'NONE', #1137, #8761, #8057, .T. ) ;
#11426=EDGE_CURVE ( 'NONE', #4682, #24540, #7398, .T. ) ;
#11427=CARTESIAN_POINT ( 'NONE',  ( 0.05283102792148739596, 0.3063958269170706794, 0.3541938269410513374 ) ) ;
#11470=DIRECTION ( 'NONE',  ( -1.000000000000000000, -2.280301054154495132E-31, 1.664003471950577689E-31 ) ) ;
#11473=CARTESIAN_POINT ( 'NONE',  ( -0.02953079040095639429, 0.4684706630666080063, -0.2484463060367437248 ) ) ;
#11479=CIRCLE ( 'NONE', #34470, 0.5302738246768086139 ) ;
#11481=ADVANCED_FACE ( 'NONE', ( #37008 ), #24531, .T. ) ;
#11487=FACE_OUTER_BOUND ( 'NONE', #11493, .T. ) ;
#11493=EDGE_LOOP ( 'NONE', ( #39667, #39222, #3138, #15996 ) ) ;
#11496=CYLINDRICAL_SURFACE ( 'NONE', #3999, 0.01500000000000004628 ) ;
#11498=CARTESIAN_POINT ( 'NONE',  ( -0.01548846960712810944, 0.3688619771571925998, -0.3775276577326300287 ) ) ;
#11501=CARTESIAN_POINT ( 'NONE',  ( -0.04230188431063459237, -0.2825024449121562586, 0.3739792551055085568 ) ) ;
#11512=EDGE_CURVE ( 'NONE', #22691, #3242, #29120, .T. ) ;
#11517=CARTESIAN_POINT ( 'NONE',  ( 0.01548846960707511190, 0.09061086148575973886, 0.5171215251571029681 ) ) ;
#11529=DIRECTION ( 'NONE',  ( 2.532366176626898522E-12, 0.8090169943749566661, 0.5877852522924604806 ) ) ;
#11533=VERTEX_POINT ( 'NONE', #18705 ) ;
#11546=ORIENTED_EDGE ( 'NONE', *, *, #17472, .F. ) ;
#11557=AXIS2_PLACEMENT_3D ( 'NONE', #33261, #17631, #27314 ) ;
#11562=DIRECTION ( 'NONE',  ( 1.000000000000000000, 2.280301054154495132E-31, -1.664003471950577689E-31 ) ) ;
#11570=CARTESIAN_POINT ( 'NONE',  ( 0.01548846960707528191, -0.3880410510314710182, 0.3755318131855027719 ) ) ;
#11571=TOROIDAL_SURFACE ( 'NONE', #18111, 0.5250000000000000222, 0.01499999999999999944 ) ;
#11572=CIRCLE ( 'NONE', #14176, 0.5400000000000017009 ) ;
#11581=CARTESIAN_POINT ( 'NONE',  ( 0.03474878377840812799, -0.07233677907409617747, -0.5114521822558271147 ) ) ;
#11590=ORIENTED_EDGE ( 'NONE', *, *, #30818, .T. ) ;
#11599=ORIENTED_EDGE ( 'NONE', *, *, #19073, .F. ) ;
#11609=ORIENTED_EDGE ( 'NONE', *, *, #1221, .T. ) ;
#11615=CARTESIAN_POINT ( 'NONE',  ( 0.04582713223189361501, -0.4389429380065721364, 0.2108029774974868320 ) ) ;
#11621=B_SPLINE_CURVE_WITH_KNOTS ( 'NONE', 3,
 ( #34763, #22656, #28401, #861, #19148, #35191, #6779, #31685, #19562, #32092, #25722, #29210, #28612, #3899, #9870, #16662, #22443, #19359 ),
 .UNSPECIFIED., .F., .F.,
 ( 4, 2, 2, 2, 2, 2, 2, 2, 4 ),
 ( -0.002633528389679716444, -0.001975271857855715081, -0.001317015326031713285, -0.0006587587942077119223, -5.022623837101260202E-07, 0.0006577542694402916702, 0.001316010801264292599, 0.001974267333088294395, 0.002632523864912296192 ),
 .UNSPECIFIED. ) ;
#11624=DIRECTION ( 'NONE',  ( -0.9378410757839558132, -0.3470650033817760383, 1.707404996040169097E-15 ) ) ;
#11627=LINE ( 'NONE', #33418, #18859 ) ;
#11633=CARTESIAN_POINT ( 'NONE',  ( -0.03647137243074970170, -0.08366781003817859441, -0.5049290013155085521 ) ) ;
#11638=CARTESIAN_POINT ( 'NONE',  ( 0.03301162916267817715, -0.4610563966203419795, -0.2426449039644940076 ) ) ;
#11656=CARTESIAN_POINT ( 'NONE',  ( 0.01548846960707524721, 0.3880410510314737382, -0.3755318131855000519 ) ) ;
#11667=EDGE_CURVE ( 'NONE', #36888, #14981, #4787, .T. ) ;
#11671=EDGE_CURVE ( 'NONE', #5331, #38334, #31654, .T. ) ;
#11685=CARTESIAN_POINT ( 'NONE',  ( -0.03650581953630684107, 0.3643937567481969619, -0.3592734714612021429 ) ) ;
#11687=DIRECTION ( 'NONE',  ( 1.000000000000000000, 1.998486013202558684E-12, 1.557674999835062714E-12 ) ) ;
#11693=CARTESIAN_POINT ( 'NONE',  ( -0.04229956186878654906, 0.2683474741743145375, -0.3842687663629381079 ) ) ;
#11694=EDGE_LOOP ( 'NONE', ( #36625, #27985, #40625, #26777 ) ) ;
#11700=ORIENTED_EDGE ( 'NONE', *, *, #4205, .T. ) ;
#11720=CARTESIAN_POINT ( 'NONE',  ( 0.01548846960707511190, -0.5198120922912221609, 0.07362328916738264395 ) ) ;
#11727=EDGE_CURVE ( 'NONE', #10166, #22691, #35156, .T. ) ;
#11733=DIRECTION ( 'NONE',  ( 0.9378410757839521494, 0.2807814858886644171, -0.2039996905746503109 ) ) ;
#11735=ORIENTED_EDGE ( 'NONE', *, *, #17502, .T. ) ;
#11743=DIRECTION ( 'NONE',  ( 0.000000000000000000, -0.9510565162951422069, 0.3090169943749823678 ) ) ;
#11747=CARTESIAN_POINT ( 'NONE',  ( -0.04139678531769439007, -0.4525211694413290853, 0.1291682248591894677 ) ) ;
#11759=CARTESIAN_POINT ( 'NONE',  ( -0.02953079040095707777, -0.5250338024619269905, -0.07436286310882420092 ) ) ;
#11762=CARTESIAN_POINT ( 'NONE',  ( 0.01899496522504870444, -0.2428513482851170358, 0.4597779644694723333 ) ) ;
#11764=CARTESIAN_POINT ( 'NONE',  ( 0.1499999999999994671, 0.3772621329472654605, -0.3651003739303476658 ) ) ;
#11768=CARTESIAN_POINT ( 'NONE',  ( 0.02872242845529800886, 0.07817994906157710311, -0.5268390348591307504 ) ) ;
#11787=SPHERICAL_SURFACE ( 'NONE', #40156, 0.01499999999999999944 ) ;
#11790=CARTESIAN_POINT ( 'NONE',  ( -0.01548846960707524721, 0.3772621329472709006, 0.3651003739303413931 ) ) ;
#11795=VERTEX_POINT ( 'NONE', #27104 ) ;
#11797=CARTESIAN_POINT ( 'NONE',  ( -0.01548846960707524721, 0.000000000000000000, 0.000000000000000000 ) ) ;
#11803=EDGE_CURVE ( 'NONE', #1288, #13846, #27194, .T. ) ;
#11811=CARTESIAN_POINT ( 'NONE',  ( -0.04285561529641390005, -0.3459893009864985491, -0.3537429040513713763 ) ) ;
#11817=CARTESIAN_POINT ( 'NONE',  ( -0.04762200653274617501, -0.04294689284307315336, -0.4802757286814972049 ) ) ;
#11821=CARTESIAN_POINT ( 'NONE',  ( 0.03309060444528774680, 0.3730661130945450155, 0.3633899800202370911 ) ) ;
#11824=CARTESIAN_POINT ( 'NONE',  ( 0.05269111014006322424, -0.4428579967164673614, -0.1534656216456658784 ) ) ;
#11828=CARTESIAN_POINT ( 'NONE',  ( 0.05615703521555099470, 0.4399943745474645951, 0.1321275321584946816 ) ) ;
#11854=CARTESIAN_POINT ( 'NONE',  ( -0.05489899477340535322, 0.2510719788555840215, 0.3887182106515215674 ) ) ;
#11872=AXIS2_PLACEMENT_3D ( 'NONE', #37083, #8294, #17745 ) ;
#11876=VERTEX_POINT ( 'NONE', #9175 ) ;
#11883=( BOUNDED_SURFACE ( )  B_SPLINE_SURFACE ( 3, 2, ( 
 ( #10400, #22962, #16983 ),
 ( #39201, #20474, #13872 ),
 ( #23580, #26246, #13682 ),
 ( #29523, #11023, #4223 ),
 ( #29336, #36293, #26667 ),
 ( #39389, #32612, #10597 ),
 ( #5031, #26447, #17596 ),
 ( #29725, #23170, #38983 ),
 ( #35698, #14094, #8113 ),
 ( #7504, #4422, #1363 ),
 ( #17388, #23390, #35906 ),
 ( #7715, #20281, #32802 ),
 ( #36098, #7903, #4603 ),
 ( #1569, #20693, #29946 ),
 ( #1784, #14299, #11209 ),
 ( #11416, #36516, #21689 ),
 ( #6034, #15098, #33420 ),
 ( #39990, #23988, #33837 ),
 ( #5639, #1968, #11811 ),
 ( #8327, #20899, #5228 ),
 ( #14704, #40405, #17778 ),
 ( #27271, #24582, #8717 ) ),
 .UNSPECIFIED., .F., .F., .T. ) 
 B_SPLINE_SURFACE_WITH_KNOTS ( ( 4, 2, 2, 2, 2, 2, 2, 2, 2, 2, 4 ),
 ( 3, 3 ),
 ( 0.002013519961495850892, 0.002780892266055758240, 0.003548264570615666021, 0.004315636875175573803, 0.004699323027455527477, 0.005083009179735481151, 0.005466695332015434824, 0.005850381484295388498, 0.006617753788855296714, 0.007385126093415204929, 0.008152498397975112276 ),
 ( 0.000000000000000000, 1.000000000000000000 ),
 .UNSPECIFIED. ) 
 GEOMETRIC_REPRESENTATION_ITEM ( )  RATIONAL_B_SPLINE_SURFACE ( (
 ( 1.000000000000000000, 0.7283825911960389865, 1.000000000000000000),
 ( 1.000000000000000000, 0.7404375345927034502, 1.000000000000000000),
 ( 1.000000000000000000, 0.7521483142435980707, 1.000000000000000000),
 ( 1.000000000000000000, 0.7744460733776445949, 1.000000000000000000),
 ( 1.000000000000000000, 0.7845612039382956482, 1.000000000000000000),
 ( 1.000000000000000000, 0.8022035258261175361, 1.000000000000000000),
 ( 1.000000000000000000, 0.8093965293321856436, 1.000000000000000000),
 ( 1.000000000000000000, 0.8169028692725391894, 1.000000000000000000),
 ( 1.000000000000000000, 0.8188329634863381612, 1.000000000000000000),
 ( 1.000000000000000000, 0.8214004505363993180, 1.000000000000000000),
 ( 1.000000000000000000, 0.8220602406261371398, 1.000000000000000000),
 ( 1.000000000000000000, 0.8220736605435244870, 1.000000000000000000),
 ( 1.000000000000000000, 0.8214126668415641097, 1.000000000000000000),
 ( 1.000000000000000000, 0.8188520474558359519, 1.000000000000000000),
 ( 1.000000000000000000, 0.8169545908333891715, 1.000000000000000000),
 ( 1.000000000000000000, 0.8094771004220669974, 1.000000000000000000),
 ( 1.000000000000000000, 0.8022723753808039815, 1.000000000000000000),
 ( 1.000000000000000000, 0.7845733350636995285, 1.000000000000000000),
 ( 1.000000000000000000, 0.7744472902493304556, 1.000000000000000000),
 ( 1.000000000000000000, 0.7522916829163448504, 1.000000000000000000),
 ( 1.000000000000000000, 0.7403553004665824888, 1.000000000000000000),
 ( 1.000000000000000000, 0.7283825911960383204, 1.000000000000000000) ) ) 
 REPRESENTATION_ITEM ( '' )  SURFACE ( )  );
#11890=ORIENTED_EDGE ( 'NONE', *, *, #36841, .T. ) ;
#11908=AXIS2_PLACEMENT_3D ( 'NONE', #22982, #1801, #11226 ) ;
#11911=CARTESIAN_POINT ( 'NONE',  ( 0.01548846960712800709, -0.4730347584885825629, 0.2341461249029146152 ) ) ;
#11916=DIRECTION ( 'NONE',  ( 0.000000000000000000, -0.8834504764630435325, -0.4685245517976845409 ) ) ;
#11930=CARTESIAN_POINT ( 'NONE',  ( 0.02869712619511918458, 0.4892154842446461149, -0.09550911579581898569 ) ) ;
#11931=EDGE_CURVE ( 'NONE', #3966, #32833, #34075, .T. ) ;
#11932=ORIENTED_EDGE ( 'NONE', *, *, #38924, .F. ) ;
#11946=CARTESIAN_POINT ( 'NONE',  ( -0.05615703521554993999, -0.4399943745474717560, 0.1321275321584853002 ) ) ;
#11955=DIRECTION ( 'NONE',  ( 2.341930812374876608E-31, 0.6954292836768424246, -0.7185945389471826150 ) ) ;
#11970=CARTESIAN_POINT ( 'NONE',  ( 0.04047043078435642177, 0.06271696546453996157, -0.4973274026419952643 ) ) ;
#11973=ORIENTED_EDGE ( 'NONE', *, *, #32320, .T. ) ;
#11975=ORIENTED_EDGE ( 'NONE', *, *, #11803, .F. ) ;
#11980=DIRECTION ( 'NONE',  ( 1.000000000000000000, 2.280301054154496446E-31, 1.355854680848613603E-31 ) ) ;
#11983=EDGE_LOOP ( 'NONE', ( #35805, #15396, #16946, #28837 ) ) ;
#11991=VERTEX_POINT ( 'NONE', #24641 ) ;
#11996=DIRECTION ( 'NONE',  ( 0.000000000000000000, -0.3090169943749375148, 0.9510565162951567508 ) ) ;
#12006=AXIS2_PLACEMENT_3D ( 'NONE', #32392, #35294, #4216 ) ;
#12012=CIRCLE ( 'NONE', #10044, 0.01499999999999995087 ) ;
#12027=CARTESIAN_POINT ( 'NONE',  ( -0.03647137243075283808, -0.2291011402249958639, 0.4576748478490594296 ) ) ;
#12031=CARTESIAN_POINT ( 'NONE',  ( -0.01896968469605126578, -0.07379952543979935442, -0.5147668824877623672 ) ) ;
#12037=CIRCLE ( 'NONE', #25193, 0.2526340763130724976 ) ;
#12038=CARTESIAN_POINT ( 'NONE',  ( 0.04230170315644469353, -0.008603754326271256456, 0.4686066795590708711 ) ) ;
#12039=CARTESIAN_POINT ( 'NONE',  ( 0.01896931156525832537, -0.4667677622193532327, -0.2292597581959257558 ) ) ;
#12043=CARTESIAN_POINT ( 'NONE',  ( 0.05186792262756725197, 0.4530091620765404059, 0.1282979832840893120 ) ) ;
#12054=DIRECTION ( 'NONE',  ( -0.000000000000000000, 0.3090169943749569437, 0.9510565162951504226 ) ) ;
#12072=CARTESIAN_POINT ( 'NONE',  ( -0.04230258372739956890, 0.2788587125276416057, 0.3766249785157091967 ) ) ;
#12081=EDGE_LOOP ( 'NONE', ( #18203, #22132, #34395, #39538 ) ) ;
#12089=CARTESIAN_POINT ( 'NONE',  ( 0.03643058821096709782, 0.2291047292463132268, -0.4577947064495169194 ) ) ;
#12099=CARTESIAN_POINT ( 'NONE',  ( -0.04230188431063500870, 0.2825024449121532055, -0.3739792551055095005 ) ) ;
#12114=DIRECTION ( 'NONE',  ( 1.000000000000000000, 0.000000000000000000, 0.000000000000000000 ) ) ;
#12136=( BOUNDED_SURFACE ( )  B_SPLINE_SURFACE ( 3, 2, ( 
 ( #1399, #16825, #23814 ),
 ( #33254, #23614, #7937 ),
 ( #13908, #30172, #22994 ),
 ( #26891, #26481, #4260 ),
 ( #7750, #17423, #8149 ),
 ( #23426, #20119, #20312 ),
 ( #29370, #35943, #32835 ),
 ( #4640, #27087, #17216 ),
 ( #7321, #13714, #5064 ),
 ( #29760, #17625, #39421 ),
 ( #1603, #26282, #35730 ),
 ( #14131, #26701, #20726 ),
 ( #39234, #2000, #10434 ),
 ( #7544, #29979, #11240 ),
 ( #36127, #11056, #20512 ),
 ( #33046, #10634, #36332 ),
 ( #35516, #38800, #19898 ),
 ( #32434, #1213, #23206 ) ),
 .UNSPECIFIED., .F., .F., .T. ) 
 B_SPLINE_SURFACE_WITH_KNOTS ( ( 4, 2, 2, 2, 2, 2, 2, 2, 4 ),
 ( 3, 3 ),
 ( -0.001532620576208883721, -0.0007637936630077779348, 5.033250193327851521E-06, 0.0007738601633944336379, 0.001542687076595539424, 0.002311513989796645102, 0.003080340902997751214, 0.003849167816198856892, 0.004617994729399962570 ),
 ( 0.000000000000000000, 1.000000000000000000 ),
 .UNSPECIFIED. ) 
 GEOMETRIC_REPRESENTATION_ITEM ( )  RATIONAL_B_SPLINE_SURFACE ( (
 ( 1.000000000000000000, 0.7283825911960434274, 1.000000000000000000),
 ( 1.000000000000000000, 0.7404385082112715510, 1.000000000000000000),
 ( 1.000000000000000000, 0.7521504257740206922, 1.000000000000000000),
 ( 1.000000000000000000, 0.7744497410759673128, 1.000000000000000000),
 ( 1.000000000000000000, 0.7845654757376588906, 1.000000000000000000),
 ( 1.000000000000000000, 0.8022083990889582461, 1.000000000000000000),
 ( 1.000000000000000000, 0.8094167424698768265, 1.000000000000000000),
 ( 1.000000000000000000, 0.8194491993617196712, 1.000000000000000000),
 ( 1.000000000000000000, 0.8220634900780805498, 1.000000000000000000),
 ( 1.000000000000000000, 0.8220705070823159932, 1.000000000000000000),
 ( 1.000000000000000000, 0.8194468812480130149, 1.000000000000000000),
 ( 1.000000000000000000, 0.8094220769840309027, 1.000000000000000000),
 ( 1.000000000000000000, 0.8022659121987061326, 1.000000000000000000),
 ( 1.000000000000000000, 0.7845681159033996988, 1.000000000000000000),
 ( 1.000000000000000000, 0.7744426415183223167, 1.000000000000000000),
 ( 1.000000000000000000, 0.7522890290930832613, 1.000000000000000000),
 ( 1.000000000000000000, 0.7403540167213815693, 1.000000000000000000),
 ( 1.000000000000000000, 0.7283825911960234434, 1.000000000000000000) ) ) 
 REPRESENTATION_ITEM ( '' )  SURFACE ( )  );
#12145=CARTESIAN_POINT ( 'NONE',  ( 0.03158843595483479261, 0.4819971762524422609, -0.09920191295802893716 ) ) ;
#12155=ORIENTED_EDGE ( 'NONE', *, *, #24619, .T. ) ;
#12157=DIRECTION ( 'NONE',  ( 0.000000000000000000, 0.9510565162951525320, -0.3090169943749502268 ) ) ;
#12159=CARTESIAN_POINT ( 'NONE',  ( -0.05491348488830374852, -0.4316112672892422064, 0.1667783590291052331 ) ) ;
#12182=AXIS2_PLACEMENT_3D ( 'NONE', #1310, #26190, #38714 ) ;
#12184=EDGE_CURVE ( 'NONE', #22691, #31970, #3523, .T. ) ;
#12185=CARTESIAN_POINT ( 'NONE',  ( 0.04230170315644469353, 0.008603754326275107542, -0.4686066795590708711 ) ) ;
#12186=DIRECTION ( 'NONE',  ( 1.000000000000000000, 2.280301054154495132E-31, -1.664003471950577689E-31 ) ) ;
#12208=FACE_OUTER_BOUND ( 'NONE', #39181, .T. ) ;
#12238=CARTESIAN_POINT ( 'NONE',  ( -0.05252359774140243770, -0.009047791085682871728, -0.4689872004378276005 ) ) ;
#12245=ADVANCED_FACE ( 'NONE', ( #17179 ), #7287, .T. ) ;
#12250=CARTESIAN_POINT ( 'NONE',  ( 0.05137569054208863950, 0.4554428576827989628, 0.1244487204292523824 ) ) ;
#12258=DIRECTION ( 'NONE',  ( 0.000000000000000000, 0.000000000000000000, 1.000000000000000000 ) ) ;
#12271=CARTESIAN_POINT ( 'NONE',  ( -0.01548846960712763066, 0.4730347584885825629, 0.2341461249029053171 ) ) ;
#12277=CARTESIAN_POINT ( 'NONE',  ( -0.04574984450155029914, 0.2311445325521691019, 0.4288136795716618876 ) ) ;
#12287=ADVANCED_FACE ( 'NONE', ( #20082 ), #11883, .T. ) ;
#12311=DIRECTION ( 'NONE',  ( 1.000000000000000000, 2.341930812374887555E-31, -1.664003471950578127E-31 ) ) ;
#12313=DIRECTION ( 'NONE',  ( 0.000000000000000000, -0.4393346272636262095, -0.8983234858819681978 ) ) ;
#12333=DIRECTION ( 'NONE',  ( 1.000000000000000000, -2.410886674703095109E-13, 1.702189702233165782E-12 ) ) ;
#12342=CARTESIAN_POINT ( 'NONE',  ( -0.01548846960721204577, 0.07651041855109251555, 0.5222379212565261275 ) ) ;
#12347=EDGE_LOOP ( 'NONE', ( #39647, #8688, #21988 ) ) ;
#12349=ORIENTED_EDGE ( 'NONE', *, *, #5238, .T. ) ;
#12355=EDGE_CURVE ( 'NONE', #36780, #15637, #8520, .T. ) ;
#12361=CARTESIAN_POINT ( 'NONE',  ( -0.05269191099235791265, -0.4442874273374651239, 0.1490603884548177271 ) ) ;
#12379=CARTESIAN_POINT ( 'NONE',  ( 0.05283710938261042267, -0.3063690517300490246, 0.3541964274677651403 ) ) ;
#12394=EDGE_LOOP ( 'NONE', ( #7678, #7114, #14666, #4132 ) ) ;
#12396=EDGE_CURVE ( 'NONE', #1288, #26954, #19304, .T. ) ;
#12398=EDGE_CURVE ( 'NONE', #20386, #16145, #23918, .T. ) ;
#12399=DIRECTION ( 'NONE',  ( -2.563099466555623676E-12, 0.5877852522924655876, -0.8090169943749527803 ) ) ;
#12405=ADVANCED_FACE ( 'NONE', ( #2563 ), #28721, .T. ) ;
#12421=CARTESIAN_POINT ( 'NONE',  ( -0.04211471441534238996, -0.008601378579327368865, 0.4689528935642813812 ) ) ;
#12426=ORIENTED_EDGE ( 'NONE', *, *, #15258, .F. ) ;
#12427=CARTESIAN_POINT ( 'NONE',  ( -0.03674260963082680992, -0.04074834683009077863, -0.4790483961530569990 ) ) ;
#12431=CARTESIAN_POINT ( 'NONE',  ( 0.01548846960707511190, -0.3772621329472763962, -0.3651003739303386730 ) ) ;
#12437=CARTESIAN_POINT ( 'NONE',  ( 0.04760578872586663374, -0.3171112559587725976, -0.3633058139840105172 ) ) ;
#12440=EDGE_LOOP ( 'NONE', ( #32024, #40601, #34033, #24006 ) ) ;
#12441=EDGE_CURVE ( 'NONE', #2376, #13090, #20625, .T. ) ;
#12455=CARTESIAN_POINT ( 'NONE',  ( -0.04582889109739283345, 0.3361233334070998779, 0.3523147457849521436 ) ) ;
#12461=CARTESIAN_POINT ( 'NONE',  ( -0.04308745346420277816, 0.3346348984074301591, 0.3638093623074960536 ) ) ;
#12479=DIRECTION ( 'NONE',  ( -1.000000000000000000, -2.280301054154495132E-31, 1.664003471950577689E-31 ) ) ;
#12480=CARTESIAN_POINT ( 'NONE',  ( 0.05201840200954559873, 0.2617120493658921521, -0.3909676859878664090 ) ) ;
#12504=ORIENTED_EDGE ( 'NONE', *, *, #14200, .F. ) ;
#12510=EDGE_CURVE ( 'NONE', #5283, #13008, #7854, .T. ) ;
#12517=DIRECTION ( 'NONE',  ( 1.000000000000000000, 2.280301054154495132E-31, -1.664003471950577689E-31 ) ) ;
#12519=ADVANCED_FACE ( 'NONE', ( #36664 ), #19814, .T. ) ;
#12533=DIRECTION ( 'NONE',  ( -1.416619696839557898E-11, 0.000000000000000000, 1.000000000000000000 ) ) ;
#12536=CARTESIAN_POINT ( 'NONE',  ( -0.05283102792148778454, -0.4315398646667463756, -0.1819478359276366641 ) ) ;
#12539=DIRECTION ( 'NONE',  ( 0.000000000000000000, 0.5877852522924701395, -0.8090169943749495607 ) ) ;
#12540=VERTEX_POINT ( 'NONE', #33985 ) ;
#12541=ORIENTED_EDGE ( 'NONE', *, *, #19080, .T. ) ;
#12562=DIRECTION ( 'NONE',  ( -1.000000000000000000, -2.280301054154495132E-31, 1.664003471950577689E-31 ) ) ;
#12569=DIRECTION ( 'NONE',  ( 1.000000000000000000, 2.341930812374887555E-31, -1.664003471950578127E-31 ) ) ;
#12573=CARTESIAN_POINT ( 'NONE',  ( -0.04575106512774497480, 0.4390484599015530565, 0.2110503898921227695 ) ) ;
#12575=CARTESIAN_POINT ( 'NONE',  ( 0.02953079040095704308, -0.3810518745593846068, 0.3687679460475796756 ) ) ;
#12585=EDGE_LOOP ( 'NONE', ( #35546, #14941, #9240, #15760 ) ) ;
#12608=LINE ( 'NONE', #3770, #30627 ) ;
#12617=CARTESIAN_POINT ( 'NONE',  ( -0.05281452789367579309, 0.03978571835447197030, 0.4666805157975088547 ) ) ;
#12631=CARTESIAN_POINT ( 'NONE',  ( 0.05544444631433361609, 0.4320262549500614169, 0.1617187101067886490 ) ) ;
#12633=CARTESIAN_POINT ( 'NONE',  ( 0.04230170315644249390, -0.2684795119051844869, -0.3841679273482348500 ) ) ;
#12651=CARTESIAN_POINT ( 'NONE',  ( -0.05186792262756997896, 0.2910804482542271310, -0.3700673534428220446 ) ) ;
#12653=FACE_OUTER_BOUND ( 'NONE', #36417, .T. ) ;
#12654=DIRECTION ( 'NONE',  ( 0.000000000000000000, 0.5877852522924830181, 0.8090169943749403458 ) ) ;
#12658=CARTESIAN_POINT ( 'NONE',  ( -0.05252359774140260423, 0.2829835766811606979, 0.3741004571325340922 ) ) ;
#12663=EDGE_CURVE ( 'NONE', #17796, #3309, #6543, .T. ) ;
#12671=CARTESIAN_POINT ( 'NONE',  ( -0.01548846960707517956, -0.3772621329472692908, -0.3651003739303438911 ) ) ;
#12679=EDGE_CURVE ( 'NONE', #34509, #28442, #15666, .T. ) ;
#12683=( GEOMETRIC_REPRESENTATION_CONTEXT ( 3 ) GLOBAL_UNCERTAINTY_ASSIGNED_CONTEXT ( ( #30969 ) ) GLOBAL_UNIT_ASSIGNED_CONTEXT ( ( #14030, #29274, #19800 ) ) REPRESENTATION_CONTEXT ( 'NONE', 'WORKASPACE' ) );
#12686=CARTESIAN_POINT ( 'NONE',  ( 0.04760578872586526678, 0.2475315945985601951, -0.4138583970464100315 ) ) ;
#12706=ORIENTED_EDGE ( 'NONE', *, *, #10189, .F. ) ;
#12713=SPHERICAL_SURFACE ( 'NONE', #13337, 0.01499999999999999944 ) ;
#12729=( BOUNDED_SURFACE ( )  B_SPLINE_SURFACE ( 3, 2, ( 
 ( #17246, #29796, #1639 ),
 ( #23640, #14353, #26728 ),
 ( #39257, #31422, #12089 ),
 ( #24439, #193, #22183 ),
 ( #21369, #28135, #27721 ),
 ( #15987, #12686, #27934 ),
 ( #36972, #15588, #34291 ),
 ( #34696, #12480, #40257 ),
 ( #9187, #8791, #19074 ),
 ( #5892, #40647, #37186 ),
 ( #33907, #40474, #31612 ),
 ( #5704, #3428, #37788 ),
 ( #30806, #15773, #37571 ),
 ( #9004, #21756, #28319 ),
 ( #18261, #24855, #28532 ),
 ( #25246, #31005, #37375 ),
 ( #18883, #34500, #6503 ),
 ( #21566, #2627, #15162 ) ),
 .UNSPECIFIED., .F., .F., .T. ) 
 B_SPLINE_SURFACE_WITH_KNOTS ( ( 4, 2, 2, 2, 2, 2, 2, 2, 4 ),
 ( 3, 3 ),
 ( -0.001532620576208849244, -0.0007637936630077626476, 5.033250193323839973E-06, 0.0007738601633944103275, 0.001542687076595496923, 0.002311513989796583519, 0.003080340902997669682, 0.003849167816198756278, 0.004617994729399842874 ),
 ( 0.000000000000000000, 1.000000000000000000 ),
 .UNSPECIFIED. ) 
 GEOMETRIC_REPRESENTATION_ITEM ( )  RATIONAL_B_SPLINE_SURFACE ( (
 ( 1.000000000000000000, 0.7283825911960446486, 1.000000000000000000),
 ( 1.000000000000000000, 0.7404385082112820982, 1.000000000000000000),
 ( 1.000000000000000000, 0.7521504257740054822, 1.000000000000000000),
 ( 1.000000000000000000, 0.7744497410759803024, 1.000000000000000000),
 ( 1.000000000000000000, 0.7845654757373869970, 1.000000000000000000),
 ( 1.000000000000000000, 0.8022083990892319161, 1.000000000000000000),
 ( 1.000000000000000000, 0.8094167424698467395, 1.000000000000000000),
 ( 1.000000000000000000, 0.8194491993617468717, 1.000000000000000000),
 ( 1.000000000000000000, 0.8220634900780513510, 1.000000000000000000),
 ( 1.000000000000000000, 0.8220705070823443039, 1.000000000000000000),
 ( 1.000000000000000000, 0.8194468812481126019, 1.000000000000000000),
 ( 1.000000000000000000, 0.8094220769839290952, 1.000000000000000000),
 ( 1.000000000000000000, 0.8022659121984873076, 1.000000000000000000),
 ( 1.000000000000000000, 0.7845681159036136387, 1.000000000000000000),
 ( 1.000000000000000000, 0.7744426415186176360, 1.000000000000000000),
 ( 1.000000000000000000, 0.7522890290927783941, 1.000000000000000000),
 ( 1.000000000000000000, 0.7403540167216061674, 1.000000000000000000),
 ( 1.000000000000000000, 0.7283825911960206678, 1.000000000000000000) ) ) 
 REPRESENTATION_ITEM ( '' )  SURFACE ( )  );
#12739=TOROIDAL_SURFACE ( 'NONE', #35731, 0.5250000000000000222, 0.01499999999999999944 ) ;
#12742=CARTESIAN_POINT ( 'NONE',  ( 0.04293317454820601980, -0.2295413494973341795, -0.4381202835071938417 ) ) ;
#12745=CARTESIAN_POINT ( 'NONE',  ( 0.02235124290213170994, 0.2417860359143765847, 0.4518977707513289754 ) ) ;
#12749=AXIS2_PLACEMENT_3D ( 'NONE', #23393, #35910, #4227 ) ;
#12759=ADVANCED_FACE ( 'NONE', ( #20752 ), #12739, .T. ) ;
#12766=CARTESIAN_POINT ( 'NONE',  ( -0.04308745346419785849, -0.4494111352305510398, 0.2058334250444107671 ) ) ;
#12772=AXIS2_PLACEMENT_3D ( 'NONE', #39885, #5914, #24459 ) ;
#12773=AXIS2_PLACEMENT_3D ( 'NONE', #1140, #23724, #4176 ) ;
#12788=CARTESIAN_POINT ( 'NONE',  ( -0.05279905671745363516, 0.4561941007107723212, 0.1063003320160429144 ) ) ;
#12825=CARTESIAN_POINT ( 'NONE',  ( 0.01548846960707582834, 0.4638115001430508921, 0.2459753896938730033 ) ) ;
#12827=CARTESIAN_POINT ( 'NONE',  ( 0.04293317454820586021, -0.4876093284570336417, 0.08292018301452548645 ) ) ;
#12840=CARTESIAN_POINT ( 'NONE',  ( -0.04285561529640979223, 0.07198636226547958095, 0.4895514295879622169 ) ) ;
#12853=CARTESIAN_POINT ( 'NONE',  ( 0.04575334816097070129, 0.4390433668671658296, 0.2110480141057521908 ) ) ;
#12856=CARTESIAN_POINT ( 'NONE',  ( 0.03672447062657707012, -0.3146083306767501475, -0.3636032511890223695 ) ) ;
#12859=CIRCLE ( 'NONE', #437, 0.01500000000000004975 ) ;
#12864=ORIENTED_EDGE ( 'NONE', *, *, #24109, .F. ) ;
#12877=CARTESIAN_POINT ( 'NONE',  ( -0.03874953289575409909, 0.3062954455724236635, -0.3649061716334326411 ) ) ;
#12887=AXIS2_PLACEMENT_3D ( 'NONE', #4553, #29670, #23114 ) ;
#12894=FACE_BOUND ( 'NONE', #38850, .T. ) ;
#12898=DIRECTION ( 'NONE',  ( 1.000000000000000000, 0.000000000000000000, 0.000000000000000000 ) ) ;
#12900=ORIENTED_EDGE ( 'NONE', *, *, #21821, .F. ) ;
#12904=CARTESIAN_POINT ( 'NONE',  ( -0.01548846960707524721, 0.3772621329472709006, 0.3651003739303413931 ) ) ;
#12924=EDGE_LOOP ( 'NONE', ( #25576, #18892, #27737 ) ) ;
#12927=EDGE_CURVE ( 'NONE', #20390, #27640, #30800, .T. ) ;
#12934=DIRECTION ( 'NONE',  ( -2.563099466555618426E-12, 0.9510565162951575280, 0.3090169943749354053 ) ) ;
#12939=CARTESIAN_POINT ( 'NONE',  ( 0.01548846960707292615, 0.09061086148586355860, -0.5171215251570915328 ) ) ;
#12960=CARTESIAN_POINT ( 'NONE',  ( 0.03159140494780116742, 0.3316214887069901529, 0.3635694333040935811 ) ) ;
#12964=VERTEX_POINT ( 'NONE', #595 ) ;
#12977=CARTESIAN_POINT ( 'NONE',  ( -0.04047161733260044858, -0.4536038223829735871, 0.2133268955647525666 ) ) ;
#12978=ADVANCED_FACE ( 'NONE', ( #25454 ), #38585, .T. ) ;
#12983=DIRECTION ( 'NONE',  ( 1.000000000000000000, 2.280301054154495132E-31, -1.664003471950577689E-31 ) ) ;
#12996=EDGE_CURVE ( 'NONE', #23581, #16603, #17342, .T. ) ;
#12998=CARTESIAN_POINT ( 'NONE',  ( -0.04308611741967801473, 0.4845711164928901971, 0.09763251765261002357 ) ) ;
#13008=VERTEX_POINT ( 'NONE', #26067 ) ;
#13031=DIRECTION ( 'NONE',  ( -1.000000000000000000, -2.280301054154495132E-31, 1.664003471950577689E-31 ) ) ;
#13041=CARTESIAN_POINT ( 'NONE',  ( -0.01548846960707442669, 0.07651041855119183888, 0.5222379212568223350 ) ) ;
#13052=DIRECTION ( 'NONE',  ( 1.702140497302367265E-12, -0.9510565162951545304, -0.3090169943749443426 ) ) ;
#13054=CARTESIAN_POINT ( 'NONE',  ( 0.05138886601527578590, 0.4416142869301781793, 0.1669109982970058137 ) ) ;
#13073=CARTESIAN_POINT ( 'NONE',  ( -0.03309060444528674066, 0.2303206394830028259, 0.4671006372792929073 ) ) ;
#13074=DIRECTION ( 'NONE',  ( 1.000000000000000000, 2.341930812374887555E-31, -1.664003471950578127E-31 ) ) ;
#13079=CARTESIAN_POINT ( 'NONE',  ( 0.04157078424165153163, 0.4522175634759060814, -0.1290209392671970434 ) ) ;
#13090=VERTEX_POINT ( 'NONE', #23585 ) ;
#13107=ORIENTED_EDGE ( 'NONE', *, *, #10931, .F. ) ;
#13108=VERTEX_POINT ( 'NONE', #1575 ) ;
#13117=DIRECTION ( 'NONE',  ( -1.000000000000000000, -2.341930812374887555E-31, 1.664003471950578127E-31 ) ) ;
#13124=CARTESIAN_POINT ( 'NONE',  ( -0.06980746140711623082, 0.000000000000000000, 0.000000000000000000 ) ) ;
#13139=CYLINDRICAL_SURFACE ( 'NONE', #11418, 0.08139150547213655496 ) ;
#13149=DIRECTION ( 'NONE',  ( 1.000000000000000000, 0.000000000000000000, 0.000000000000000000 ) ) ;
#13156=CARTESIAN_POINT ( 'NONE',  ( -0.04762200653275133755, -0.4434980416368527467, 0.1892582844414182897 ) ) ;
#13159=SPHERICAL_SURFACE ( 'NONE', #4731, 0.01499999999999999944 ) ;
#13165=CARTESIAN_POINT ( 'NONE',  ( 0.02953079040095687308, 0.5250338024619264354, 0.07436286310882474215 ) ) ;
#13167=CIRCLE ( 'NONE', #15788, 0.01499999999999999424 ) ;
#13168=CARTESIAN_POINT ( 'NONE',  ( 0.05268932808079999225, -0.2680477706051425102, 0.3844863582443106553 ) ) ;
#13176=CARTESIAN_POINT ( 'NONE',  ( -0.01899496522503853549, 0.4667215747137464787, 0.2292237458735913169 ) ) ;
#13195=ORIENTED_EDGE ( 'NONE', *, *, #6197, .F. ) ;
#13204=AXIS2_PLACEMENT_3D ( 'NONE', #32464, #4074, #1052 ) ;
#13210=CARTESIAN_POINT ( 'NONE',  ( -0.02953079040095693900, -0.2329676531120430660, 0.4763574306556350169 ) ) ;
#13221=DIRECTION ( 'NONE',  ( 0.000000000000000000, 3.330669073875470114E-16, 1.000000000000000000 ) ) ;
#13227=LINE ( 'NONE', #16935, #26733 ) ;
#13231=AXIS2_PLACEMENT_3D ( 'NONE', #30718, #2539, #5196 ) ;
#13247=ORIENTED_EDGE ( 'NONE', *, *, #6965, .F. ) ;
#13272=CARTESIAN_POINT ( 'NONE',  ( -0.02872242845530464245, -0.4768947642620179339, -0.2371557650701917319 ) ) ;
#13291=ADVANCED_FACE ( 'NONE', ( #34228 ), #2979, .T. ) ;
#13293=CARTESIAN_POINT ( 'NONE',  ( -0.04230188431063468257, -0.2683773510969740261, -0.3842417364743036523 ) ) ;
#13300=DIRECTION ( 'NONE',  ( 0.000000000000000000, -0.4393346272634560679, -0.8983234858820514646 ) ) ;
#13311=VERTEX_POINT ( 'NONE', #40195 ) ;
#13315=EDGE_LOOP ( 'NONE', ( #26519, #36105, #36220, #38941 ) ) ;
#13320=DIRECTION ( 'NONE',  ( 1.664003471950577032E-31, 3.330669073875470114E-16, 1.000000000000000000 ) ) ;
#13321=AXIS2_PLACEMENT_3D ( 'NONE', #28407, #21639, #25534 ) ;
#13333=CARTESIAN_POINT ( 'NONE',  ( 0.01548846960707511190, 0.09061086148576739940, 0.5171215251571016358 ) ) ;
#13337=AXIS2_PLACEMENT_3D ( 'NONE', #30077, #30258, #39731 ) ;
#13341=CARTESIAN_POINT ( 'NONE',  ( 0.03654364704248871248, -0.3642884434512947966, 0.3592365245254307560 ) ) ;
#13345=CARTESIAN_POINT ( 'NONE',  ( 0.05634301242525747294, -0.2614060064472272793, -0.3772872482281126039 ) ) ;
#13347=CARTESIAN_POINT ( 'NONE',  ( -0.04154009738085497061, -0.01731731106881116700, 0.4700109389422703066 ) ) ;
#13369=VECTOR ( 'NONE', #32710, 39.37007874015748143 ) ;
#13377=DIRECTION ( 'NONE',  ( 1.000000000000000000, 8.054771744420843492E-13, 1.518808759990554105E-12 ) ) ;
#13378=DIRECTION ( 'NONE',  ( -1.540743955509782771E-31, -0.9849933812515921927, -0.1725921171159214562 ) ) ;
#13381=CARTESIAN_POINT ( 'NONE',  ( 0.05078310099560401358, -0.3164655623698865439, 0.3525377550955086092 ) ) ;
#13385=CIRCLE ( 'NONE', #31132, 0.1749999999999999889 ) ;
#13389=CYLINDRICAL_SURFACE ( 'NONE', #29735, 0.01499999999999999424 ) ;
#13414=CIRCLE ( 'NONE', #16712, 0.01500000000000005669 ) ;
#13429=CIRCLE ( 'NONE', #7477, 0.5400000000000018119 ) ;
#13455=CIRCLE ( 'NONE', #22672, 0.5400000000000001465 ) ;
#13464=CARTESIAN_POINT ( 'NONE',  ( -0.03642997641689546540, 0.5061875831641691192, -0.07642488348723255887 ) ) ;
#13478=CARTESIAN_POINT ( 'NONE',  ( -0.02953079040095640123, 0.2329676531120523086, -0.4763574306556315752 ) ) ;
#13490=DIRECTION ( 'NONE',  ( 1.000000000000000000, 2.341930812374887555E-31, -1.664003471950578127E-31 ) ) ;
#13491=CARTESIAN_POINT ( 'NONE',  ( 0.05634206451479474576, 0.4332270636364591865, -0.1516455289248239691 ) ) ;
#13494=CARTESIAN_POINT ( 'NONE',  ( 0.02869712619511882029, -0.3396447909410097998, 0.3648221446286689651 ) ) ;
#13501=CIRCLE ( 'NONE', #14138, 0.01500000000000001332 ) ;
#13510=DIRECTION ( 'NONE',  ( 0.3468893892380798261, -0.9373665302208751271, -0.03180785525163549315 ) ) ;
#13513=DIRECTION ( 'NONE',  ( -1.000000000000000000, -2.280301054154495132E-31, 1.664003471950577689E-31 ) ) ;
#13520=VERTEX_POINT ( 'NONE', #10770 ) ;
#13541=CARTESIAN_POINT ( 'NONE',  ( 0.02231181081520646273, -0.3551561381230135539, -0.3696296485972559998 ) ) ;
#13545=CARTESIAN_POINT ( 'NONE',  ( 0.02872242845530408734, 0.3729171224323689082, 0.3802687114177492056 ) ) ;
#13555=EDGE_CURVE ( 'NONE', #23581, #38697, #23308, .T. ) ;
#13559=CARTESIAN_POINT ( 'NONE',  ( 0.03309057659885102087, -0.2303206601891079897, -0.4671007096900161581 ) ) ;
#13561=CARTESIAN_POINT ( 'NONE',  ( -0.02231181081520790255, -0.07006449514257452604, 0.5077922075898742005 ) ) ;
#13574=CARTESIAN_POINT ( 'NONE',  ( -0.03158843595483515343, -0.2432919444504221540, 0.4277514783322121650 ) ) ;
#13579=DIRECTION ( 'NONE',  ( -2.218671295934093951E-31, -0.6954292836768477537, 0.7185945389471773970 ) ) ;
#13582=CARTESIAN_POINT ( 'NONE',  ( -0.01548846960707477016, 0.3880410510314737382, -0.3755318131855000519 ) ) ;
#13598=LINE ( 'NONE', #20377, #15976 ) ;
#13612=ORIENTED_EDGE ( 'NONE', *, *, #27855, .T. ) ;
#13637=ORIENTED_EDGE ( 'NONE', *, *, #38119, .T. ) ;
#13652=CARTESIAN_POINT ( 'NONE',  ( -0.05615703521554947508, 0.4399943745474728107, -0.1321275321584859941 ) ) ;
#13666=CARTESIAN_POINT ( 'NONE',  ( -0.04047161733260026123, 0.2415827978909600438, -0.4392067210493235119 ) ) ;
#13670=CARTESIAN_POINT ( 'NONE',  ( -0.04211471441534220955, -0.4433427331037121388, -0.1530948108196634461 ) ) ;
#13677=CARTESIAN_POINT ( 'NONE',  ( 0.04229974373173322338, 0.4430055847546675585, -0.1530238331097760751 ) ) ;
#13682=CARTESIAN_POINT ( 'NONE',  ( -0.03642997641689347393, -0.2291049489869416145, -0.4577964116453033805 ) ) ;
#13690=ORIENTED_EDGE ( 'NONE', *, *, #36768, .T. ) ;
#13693=CARTESIAN_POINT ( 'NONE',  ( 0.01899496522504069002, 0.07377983897468347319, 0.5147126279162671514 ) ) ;
#13703=ORIENTED_EDGE ( 'NONE', *, *, #876, .T. ) ;
#13714=CARTESIAN_POINT ( 'NONE',  ( 0.05268932808080010327, -0.4428506128075276882, 0.1535014714533977642 ) ) ;
#13720=CARTESIAN_POINT ( 'NONE',  ( 0.05634304521267756438, -0.01028134608269219187, 0.4588823192046725397 ) ) ;
#13726=CARTESIAN_POINT ( 'NONE',  ( 0.04229974373173651936, 0.2824305679197209873, 0.3740363831607525502 ) ) ;
#13729=CARTESIAN_POINT ( 'NONE',  ( -0.02953079040095652960, 0.5250338024619264354, -0.07436286310882528339 ) ) ;
#13733=B_SPLINE_CURVE_WITH_KNOTS ( 'NONE', 3,
 ( #32811, #14305, #17189, #27062, #20484, #26676, #2378, #27475, #17787, #33018, #24194, #33232, #40000, #11217, #5040, #36717, #14920, #4823 ),
 .UNSPECIFIED., .F., .F.,
 ( 4, 2, 2, 2, 2, 2, 2, 2, 4 ),
 ( -0.002633528389679732490, -0.001975271857855729826, -0.001317015326031727163, -0.0006587587942077244990, -5.022623837218354037E-07, 0.0006577542694402808282, 0.001316010801264283492, 0.001974267333088286155, 0.002632523864912288819 ),
 .UNSPECIFIED. ) ;
#13735=CARTESIAN_POINT ( 'NONE',  ( -0.02238765564325098656, -0.3549921663302747499, 0.3695537732572988232 ) ) ;
#13737=VERTEX_POINT ( 'NONE', #4510 ) ;
#13739=EDGE_CURVE ( 'NONE', #4078, #22774, #25951, .T. ) ;
#13746=CARTESIAN_POINT ( 'NONE',  ( -0.05283710938261119983, 0.4560492058803807813, 0.1064717188025598449 ) ) ;
#13750=CARTESIAN_POINT ( 'NONE',  ( 0.03654364704248846962, 0.5058694728073472868, -0.07650507870001040100 ) ) ;
#13757=DIRECTION ( 'NONE',  ( 1.000000000000000000, 0.000000000000000000, 0.000000000000000000 ) ) ;
#13760=ORIENTED_EDGE ( 'NONE', *, *, #24119, .T. ) ;
#13770=EDGE_CURVE ( 'NONE', #13940, #2287, #26587, .T. ) ;
#13773=CARTESIAN_POINT ( 'NONE',  ( 0.05283102792148713922, 0.4560693389104583662, 0.1064538768721982470 ) ) ;
#13783=FACE_OUTER_BOUND ( 'NONE', #5446, .T. ) ;
#13784=CARTESIAN_POINT ( 'NONE',  ( 0.02869712619511936846, 0.06034133159976078770, -0.4947855140619924486 ) ) ;
#13787=ORIENTED_EDGE ( 'NONE', *, *, #34096, .T. ) ;
#13798=EDGE_LOOP ( 'NONE', ( #23684, #22743, #33044 ) ) ;
#13800=CARTESIAN_POINT ( 'NONE',  ( 0.05252359774140119564, 0.4432374118283801123, 0.1535299757497397000 ) ) ;
#13841=AXIS2_PLACEMENT_3D ( 'NONE', #22580, #13510, #22790 ) ;
#13844=AXIS2_PLACEMENT_3D ( 'NONE', #8692, #11996, #33588 ) ;
#13845=CARTESIAN_POINT ( 'NONE',  ( -0.05634115714581326706, 0.4380405955734048007, -0.1368374331724235560 ) ) ;
#13846=VERTEX_POINT ( 'NONE', #30437 ) ;
#13854=ORIENTED_EDGE ( 'NONE', *, *, #25287, .T. ) ;
#13858=DIRECTION ( 'NONE',  ( 1.000000000000000000, 2.280301054154495132E-31, -1.664003471950577689E-31 ) ) ;
#13872=CARTESIAN_POINT ( 'NONE',  ( -0.03303708955568313704, -0.2303604322856099840, -0.4672397951413049255 ) ) ;
#13883=EDGE_CURVE ( 'NONE', #34509, #17498, #16074, .T. ) ;
#13885=CARTESIAN_POINT ( 'NONE',  ( 0.01548846960707388198, -0.5203207976467953966, -0.08861466064782426433 ) ) ;
#13887=DIRECTION ( 'NONE',  ( -0.3468893892380665034, -0.3199132558031917983, -0.8816593788960922495 ) ) ;
#13889=AXIS2_PLACEMENT_3D ( 'NONE', #37864, #9682, #31683 ) ;
#13904=DIRECTION ( 'NONE',  ( 0.9378410757839558132, 0.3470650033817763158, 0.000000000000000000 ) ) ;
#13907=CARTESIAN_POINT ( 'NONE',  ( 0.01548846960707524721, 0.5346638663566671834, 0.07572681171513505338 ) ) ;
#13908=CARTESIAN_POINT ( 'NONE',  ( 0.02238826743732968277, -0.4611641377668557196, 0.2234181651772608468 ) ) ;
#13918=DIRECTION ( 'NONE',  ( -2.218671295934093951E-31, -0.6954292836768477537, 0.7185945389471773970 ) ) ;
#13924=B_SPLINE_CURVE_WITH_KNOTS ( 'NONE', 3,
 ( #1611, #13720, #4459, #20731, #20320, #17629, #7944, #20518, #23212, #39023 ),
 .UNSPECIFIED., .F., .F.,
 ( 4, 2, 2, 2, 4 ),
 ( 8.597723227810050162E-17, 0.0007834172717712229415, 0.001566834543542360448, 0.002350251815313497521, 0.003133669087084634593 ),
 .UNSPECIFIED. ) ;
#13927=CARTESIAN_POINT ( 'NONE',  ( -0.01548846960707477016, 0.2372406987223678043, 0.4850946823762586901 ) ) ;
#13928=EDGE_CURVE ( 'NONE', #5083, #36014, #38395, .T. ) ;
#13935=AXIS2_PLACEMENT_3D ( 'NONE', #347, #15108, #18397 ) ;
#13938=CARTESIAN_POINT ( 'NONE',  ( -0.03171102739523559005, -0.2433685106468572723, 0.4273977451499074154 ) ) ;
#13940=VERTEX_POINT ( 'NONE', #10869 ) ;
#13954=DIRECTION ( 'NONE',  ( 1.000000000000000000, 1.609192080950324210E-13, -1.762723797404872045E-11 ) ) ;
#13957=CARTESIAN_POINT ( 'NONE',  ( -0.01895884884825285027, -0.5124024296374548593, 0.08888335629179863751 ) ) ;
#13968=CARTESIAN_POINT ( 'NONE',  ( -0.02953079040095700838, 0.09152108205202039160, -0.5223162075576429642 ) ) ;
#13969=AXIS2_PLACEMENT_3D ( 'NONE', #28185, #14827, #2680 ) ;
#13974=DIRECTION ( 'NONE',  ( -1.355854680848614260E-31, 3.330669073875470114E-16, 1.000000000000000000 ) ) ;
#13979=ADVANCED_FACE ( 'NONE', ( #9383 ), #31213, .F. ) ;
#14012=EDGE_LOOP ( 'NONE', ( #3886, #36272, #25424, #3053 ) ) ;
#14020=AXIS2_PLACEMENT_3D ( 'NONE', #20860, #29905, #1143 ) ;
#14024=AXIS2_PLACEMENT_3D ( 'NONE', #30550, #2368, #14909 ) ;
#14030=( CONVERSION_BASED_UNIT ( 'INCH', #33166 ) LENGTH_UNIT ( ) NAMED_UNIT ( #10478 ) );
#14039=AXIS2_PLACEMENT_3D ( 'NONE', #38479, #13377, #18956 ) ;
#14046=EDGE_CURVE ( 'NONE', #4078, #33332, #2936, .T. ) ;
#14063=CARTESIAN_POINT ( 'NONE',  ( -0.05279185365593402207, 0.4562178057548016419, -0.1062796545748909277 ) ) ;
#14070=VECTOR ( 'NONE', #23054, 39.37007874015748143 ) ;
#14078=CARTESIAN_POINT ( 'NONE',  ( -0.04047161733259348887, -0.4923636041515490613, -0.09403655331106135218 ) ) ;
#14085=CIRCLE ( 'NONE', #27868, 0.2526340763130724976 ) ;
#14091=DIRECTION ( 'NONE',  ( -1.000000000000000000, -2.280301054154495132E-31, 1.664003471950577689E-31 ) ) ;
#14094=CARTESIAN_POINT ( 'NONE',  ( -0.05186792262756985405, -0.2620061627190611864, -0.3911910583554863430 ) ) ;
#14097=CARTESIAN_POINT ( 'NONE',  ( -0.05561170715395123004, 0.02038383341412555033, -0.4604752114371309935 ) ) ;
#14102=CARTESIAN_POINT ( 'NONE',  ( 0.02953079040095704308, 0.3810518745593911571, 0.3687679460475725701 ) ) ;
#14105=CARTESIAN_POINT ( 'NONE',  ( -0.01548846960707463312, 0.2306506793134060762, 0.4716198300880322658 ) ) ;
#14122=LINE ( 'NONE', #1807, #30960 ) ;
#14125=ORIENTED_EDGE ( 'NONE', *, *, #22971, .F. ) ;
#14128=ORIENTED_EDGE ( 'NONE', *, *, #18352, .T. ) ;
#14131=CARTESIAN_POINT ( 'NONE',  ( 0.03875673594170155750, -0.4622647171927982135, 0.1151965740700821167 ) ) ;
#14138=AXIS2_PLACEMENT_3D ( 'NONE', #35782, #36179, #32885 ) ;
#14141=CARTESIAN_POINT ( 'NONE',  ( 0.03875673594170226527, 0.2524061059367339599, 0.4040421724581182983 ) ) ;
#14144=CARTESIAN_POINT ( 'NONE',  ( -0.04582713223189551627, 0.4790191777205496382, -0.08746099429787626556 ) ) ;
#14157=DIRECTION ( 'NONE',  ( 1.000000000000000000, 0.000000000000000000, 0.000000000000000000 ) ) ;
#14160=CARTESIAN_POINT ( 'NONE',  ( -0.03654364704248907331, 0.5058694728073477309, 0.07650507870001060917 ) ) ;
#14163=EDGE_CURVE ( 'NONE', #5331, #27640, #4878, .T. ) ;
#14166=CARTESIAN_POINT ( 'NONE',  ( 0.02953079040095700838, 0.2329676531120452587, -0.4763574306556336291 ) ) ;
#14175=CLOSED_SHELL ( 'NONE', ( #24895, #33771, #40099, #16279, #2554, #27287, #17526, #12245, #33590, #38588, #14220, #32602, #7487, #35837, #27852, #21879, #30413, #29280, #2715, #23000, #21714, #2845, #1038, #15189, #27430, #34568, #20808, #19238, #24833, #9237, #21368, #11481, #28807, #26178, #19307, #25738, #4590, #17480, #20035, #13979, #16323, #33066, #2964, #29583, #29641, #5152, #24564, #4369, #10744, #11048, #9247, #1256, #2604, #8417, #32323, #24366, #12519, #33036, #32270, #29441, #33367, #29845, #17733, #26144, #40643, #12759, #12287, #24123, #9133, #25510, #25044, #30127, #32128, #25304, #8404, #25170, #20313, #16238, #40591, #22625, #8924, #13291, #31641, #10936, #3915, #15758, #5217, #10176, #15060, #18916, #2374, #36656, #2750, #12978, #16525, #5962, #9372, #31520, #15236, #20513, #20459, #27335, #7234, #19296, #34160, #34035, #40441, #40068, #14835, #27356, #37874, #23855, #39825, #23295, #12405, #391, #24610, #15667, #28898, #30526, #22310, #32796, #2623, #32388, #37346, #8119, #38614, #22337, #34560, #19011, #36148, #17619, #30024, #21768, #1948, #17235, #5953, #7357, #29779, #18083, #10629, #16561, #26614, #32845 ) ) ;
#14176=AXIS2_PLACEMENT_3D ( 'NONE', #9315, #31952, #9734 ) ;
#14180=CARTESIAN_POINT ( 'NONE',  ( 0.04229956186878608415, 0.4429651807893710269, 0.1531492745855134174 ) ) ;
#14200=EDGE_CURVE ( 'NONE', #14410, #1288, #11479, .T. ) ;
#14220=ADVANCED_FACE ( 'NONE', ( #7507, #12894 ), #29340, .F. ) ;
#14251=ORIENTED_EDGE ( 'NONE', *, *, #31872, .T. ) ;
#14268=CARTESIAN_POINT ( 'NONE',  ( -0.05543910610525212834, 0.4446004295725625166, -0.1230574251923853557 ) ) ;
#14282=CARTESIAN_POINT ( 'NONE',  ( -0.04575334816098036717, 0.2311426348461442515, -0.4288046462019702854 ) ) ;
#14284=CARTESIAN_POINT ( 'NONE',  ( -0.04575334816098059615, -0.4792444552800824153, -0.08732178612071218871 ) ) ;
#14298=CARTESIAN_POINT ( 'NONE',  ( -0.02953079040095693900, -0.09152108205202422186, -0.5223162075576424090 ) ) ;
#14299=CARTESIAN_POINT ( 'NONE',  ( -0.05138886601528206560, -0.2952081121918937456, -0.3684218102521223392 ) ) ;
#14305=CARTESIAN_POINT ( 'NONE',  ( -0.01895494625228195951, 0.3623053290767001000, 0.3730957266516555793 ) ) ;
#14306=CARTESIAN_POINT ( 'NONE',  ( 0.03170874437002779017, 0.05432941731172492156, 0.4888251740112576349 ) ) ;
#14308=CARTESIAN_POINT ( 'NONE',  ( -0.01548846960707490547, 0.09061086148575973886, 0.5171215251571029681 ) ) ;
#14325=CARTESIAN_POINT ( 'NONE',  ( 0.1499999999999993561, 0.000000000000000000, 0.000000000000000000 ) ) ;
#14328=EDGE_LOOP ( 'NONE', ( #9956, #18315, #13612, #9849 ) ) ;
#14330=DIRECTION ( 'NONE',  ( -1.000000000000000000, -2.341930812374887555E-31, 1.664003471950578127E-31 ) ) ;
#14337=DIRECTION ( 'NONE',  ( 0.000000000000000000, -0.8090169943749496717, -0.5877852522924700285 ) ) ;
#14339=CARTESIAN_POINT ( 'NONE',  ( 0.05076679145662137127, 0.3165345149637581734, 0.3525336044145316872 ) ) ;
#14347=CARTESIAN_POINT ( 'NONE',  ( -0.04947837552028283570, -0.2513950290986461944, 0.4056869761633379867 ) ) ;
#14348=ORIENTED_EDGE ( 'NONE', *, *, #35406, .T. ) ;
#14351=ORIENTED_EDGE ( 'NONE', *, *, #30010, .F. ) ;
#14353=CARTESIAN_POINT ( 'NONE',  ( 0.03174060074383010938, 0.2437182008228720997, -0.4645020220639604069 ) ) ;
#14355=CARTESIAN_POINT ( 'NONE',  ( -0.05634307799789435578, 0.4332460723641307077, 0.1515798417490766270 ) ) ;
#14360=DIRECTION ( 'NONE',  ( -1.416619696839553375E-11, -0.5877852522924736922, -0.8090169943749470072 ) ) ;
#14366=VERTEX_POINT ( 'NONE', #11420 ) ;
#14369=CARTESIAN_POINT ( 'NONE',  ( 0.04230188431063428012, 0.4483687697007492923, 0.1365048020681075280 ) ) ;
#14375=CARTESIAN_POINT ( 'NONE',  ( 0.04582713223189471136, 0.2312054150958161580, -0.4285473768184981935 ) ) ;
#14380=CARTESIAN_POINT ( 'NONE',  ( 0.03664605387828124422, -0.4684681574363452339, 0.1090337349854996613 ) ) ;
#14393=CYLINDRICAL_SURFACE ( 'NONE', #25634, 0.08139150547213666598 ) ;
#14410=VERTEX_POINT ( 'NONE', #17781 ) ;
#14422=CARTESIAN_POINT ( 'NONE',  ( 0.1499999999999993561, 0.000000000000000000, 0.000000000000000000 ) ) ;
#14428=B_SPLINE_CURVE_WITH_KNOTS ( 'NONE', 3,
 ( #40391, #33210, #5016, #2150, #11615, #24175, #17583, #25579, #25168, #15511, #534, #40589, #28859, #22108, #12827, #25786, #37708, #38109 ),
 .UNSPECIFIED., .F., .F.,
 ( 4, 2, 2, 2, 2, 2, 2, 2, 4 ),
 ( -0.003133633995111274450, -0.002350221109836769448, -0.001566808224562264446, -0.0007833953392877594443, 1.754598674555754578E-08, 0.0007834304312612518605, 0.001566843316535758163, 0.002350256201810264466, 0.003133669087084770769 ),
 .UNSPECIFIED. ) ;
#14437=CARTESIAN_POINT ( 'NONE',  ( 0.05561310505367213913, 0.02041094169100532082, -0.4604718309744556537 ) ) ;
#14439=SPHERICAL_SURFACE ( 'NONE', #32252, 0.01499999999999999944 ) ;
#14467=DIRECTION ( 'NONE',  ( 0.000000000000000000, 0.5877852522924910117, -0.8090169943749343506 ) ) ;
#14484=CARTESIAN_POINT ( 'NONE',  ( -0.05562150110511283885, -0.02029635476683529227, -0.4604536315446556838 ) ) ;
#14490=AXIS2_PLACEMENT_3D ( 'NONE', #3238, #15784, #34511 ) ;
#14494=LINE ( 'NONE', #30556, #31006 ) ;
#14496=CARTESIAN_POINT ( 'NONE',  ( 0.05561375719525353534, 0.02040745343124195435, 0.4604703763991767618 ) ) ;
#14498=CARTESIAN_POINT ( 'NONE',  ( 0.04285640132274045472, -0.4878352195310067252, -0.08281044837501300160 ) ) ;
#14522=DIRECTION ( 'NONE',  ( 0.000000000000000000, 0.000000000000000000, -1.000000000000000000 ) ) ;
#14524=( BOUNDED_SURFACE ( )  B_SPLINE_SURFACE ( 3, 2, ( 
 ( #13885, #20486, #33023 ),
 ( #11219, #36306, #33235 ),
 ( #5042, #26261, #38778 ),
 ( #10608, #30149, #14498 ),
 ( #27064, #23184, #5840 ),
 ( #21097, #2575, #33622 ),
 ( #5235, #17789, #18401 ),
 ( #34237, #15327, #40002 ),
 ( #5435, #39813, #15111 ),
 ( #30558, #11824, #14717 ),
 ( #21703, #17999, #27671 ),
 ( #40203, #30347, #30953 ),
 ( #6047, #33850, #18207 ),
 ( #34039, #2381, #14922 ),
 ( #37134, #36719, #33429 ),
 ( #21312, #24599, #2178 ),
 ( #12039, #27280, #11638 ),
 ( #8947, #24196, #8529 ) ),
 .UNSPECIFIED., .F., .F., .T. ) 
 B_SPLINE_SURFACE_WITH_KNOTS ( ( 4, 2, 2, 2, 2, 2, 2, 2, 4 ),
 ( 3, 3 ),
 ( -0.001532620576208818235, -0.0007637936630077494203, 5.033250193319503164E-06, 0.0007738601633943884266, 0.001542687076595457242, 0.002311513989796526274, 0.003080340902997595089, 0.003849167816198663904, 0.004617994729399732719 ),
 ( 0.000000000000000000, 1.000000000000000000 ),
 .UNSPECIFIED. ) 
 GEOMETRIC_REPRESENTATION_ITEM ( )  RATIONAL_B_SPLINE_SURFACE ( (
 ( 1.000000000000000000, 0.7283825911960469801, 1.000000000000000000),
 ( 1.000000000000000000, 0.7404385082113237315, 1.000000000000000000),
 ( 1.000000000000000000, 0.7521504257739495269, 1.000000000000000000),
 ( 1.000000000000000000, 0.7744497410760391443, 1.000000000000000000),
 ( 1.000000000000000000, 0.7845654757373858867, 1.000000000000000000),
 ( 1.000000000000000000, 0.8022083990892294736, 1.000000000000000000),
 ( 1.000000000000000000, 0.8094167424699034719, 1.000000000000000000),
 ( 1.000000000000000000, 0.8194491993616881409, 1.000000000000000000),
 ( 1.000000000000000000, 0.8220634900780661170, 1.000000000000000000),
 ( 1.000000000000000000, 0.8220705070823304261, 1.000000000000000000),
 ( 1.000000000000000000, 0.8194468812481864317, 1.000000000000000000),
 ( 1.000000000000000000, 0.8094220769838590401, 1.000000000000000000),
 ( 1.000000000000000000, 0.8022659121987882891, 1.000000000000000000),
 ( 1.000000000000000000, 0.7845681159033097707, 1.000000000000000000),
 ( 1.000000000000000000, 0.7744426415185602375, 1.000000000000000000),
 ( 1.000000000000000000, 0.7522890290928357926, 1.000000000000000000),
 ( 1.000000000000000000, 0.7403540167215585388, 1.000000000000000000),
 ( 1.000000000000000000, 0.7283825911960204458, 1.000000000000000000) ) ) 
 REPRESENTATION_ITEM ( '' )  SURFACE ( )  );
#14541=CARTESIAN_POINT ( 'NONE',  ( -0.03309057659885111802, 0.4608882367397823532, -0.2425133248664002594 ) ) ;
#14545=AXIS2_PLACEMENT_3D ( 'NONE', #22047, #6172, #12157 ) ;
#14552=CARTESIAN_POINT ( 'NONE',  ( -0.05283710938261127615, 0.2421875768565603382, -0.4008269984734620928 ) ) ;
#14553=CIRCLE ( 'NONE', #23128, 0.01500000000000006536 ) ;
#14558=ORIENTED_EDGE ( 'NONE', *, *, #13883, .F. ) ;
#14559=EDGE_CURVE ( 'NONE', #4225, #1885, #31863, .T. ) ;
#14570=ORIENTED_EDGE ( 'NONE', *, *, #3854, .T. ) ;
#14572=DIRECTION ( 'NONE',  ( -2.563099466555620041E-12, 0.5877852522924830181, 0.8090169943749403458 ) ) ;
#14576=DIRECTION ( 'NONE',  ( 1.000000000000000000, 1.195566832711459831E-12, -1.235392033522776487E-12 ) ) ;
#14583=DIRECTION ( 'NONE',  ( 1.000000000000000000, 8.638708177629562344E-13, -2.382021192243037336E-12 ) ) ;
#14585=CIRCLE ( 'NONE', #15913, 0.5302738246768103902 ) ;
#14593=CARTESIAN_POINT ( 'NONE',  ( 0.03664605387828146627, 0.04106737781738913767, -0.4792329708773127583 ) ) ;
#14595=ORIENTED_EDGE ( 'NONE', *, *, #30344, .T. ) ;
#14599=TOROIDAL_SURFACE ( 'NONE', #22527, 0.6154198107346402491, 0.7750185148639454624 ) ;
#14600=FACE_OUTER_BOUND ( 'NONE', #2976, .T. ) ;
#14614=AXIS2_PLACEMENT_3D ( 'NONE', #36632, #21001, #40102 ) ;
#14644=CARTESIAN_POINT ( 'NONE',  ( 0.05268932808079344193, -0.009140209359764809791, -0.4686105243965638656 ) ) ;
#14645=AXIS2_PLACEMENT_3D ( 'NONE', #19322, #6346, #3864 ) ;
#14655=CARTESIAN_POINT ( 'NONE',  ( 0.01895884884825209393, 0.3622979475331369326, 0.3730907371368772929 ) ) ;
#14657=ORIENTED_EDGE ( 'NONE', *, *, #3341, .T. ) ;
#14666=ORIENTED_EDGE ( 'NONE', *, *, #5882, .T. ) ;
#14670=EDGE_CURVE ( 'NONE', #13846, #13090, #37782, .T. ) ;
#14681=CARTESIAN_POINT ( 'NONE',  ( 0.05283102792148691718, -0.4560693389104585882, -0.1064538768722001622 ) ) ;
#14684=VECTOR ( 'NONE', #39793, 39.37007874015748143 ) ;
#14686=AXIS2_PLACEMENT_3D ( 'NONE', #7842, #8049, #1510 ) ;
#14704=CARTESIAN_POINT ( 'NONE',  ( -0.01896968469605425645, -0.3622774521524859126, -0.3730768833943127749 ) ) ;
#14713=ORIENTED_EDGE ( 'NONE', *, *, #6921, .F. ) ;
#14714=CARTESIAN_POINT ( 'NONE',  ( 0.05083665881508980799, 0.2375940621857689505, 0.4096919151850463847 ) ) ;
#14716=CARTESIAN_POINT ( 'NONE',  ( 0.04946426091937060343, -0.03515176265874975226, 0.4760065386269228260 ) ) ;
#14717=CARTESIAN_POINT ( 'NONE',  ( 0.05634402396114716882, -0.4332356819307869866, -0.1516051145244172449 ) ) ;
#14722=CARTESIAN_POINT ( 'NONE',  ( 0.01548846960707271452, -0.3688619771572954065, -0.3775276577327018046 ) ) ;
#14723=ORIENTED_EDGE ( 'NONE', *, *, #26252, .F. ) ;
#14743=VECTOR ( 'NONE', #23189, 39.37007874015748143 ) ;
#14745=DIRECTION ( 'NONE',  ( 0.000000000000000000, 0.9901182710308658041, 0.1402348365095101024 ) ) ;
#14748=VECTOR ( 'NONE', #33402, 39.37007874015748143 ) ;
#14766=AXIS2_PLACEMENT_3D ( 'NONE', #36398, #14583, #8213 ) ;
#14776=ORIENTED_EDGE ( 'NONE', *, *, #38648, .F. ) ;
#14792=FACE_OUTER_BOUND ( 'NONE', #24338, .T. ) ;
#14801=CARTESIAN_POINT ( 'NONE',  ( 0.05283710938261071410, 0.3063690517300499683, -0.3541964274677632529 ) ) ;
#14827=DIRECTION ( 'NONE',  ( 1.000000000000000000, 2.280301054154495132E-31, -1.664003471950577689E-31 ) ) ;
#14830=CARTESIAN_POINT ( 'NONE',  ( -0.02869942827333538810, -0.4519168387192256664, -0.2102852866807496113 ) ) ;
#14833=CARTESIAN_POINT ( 'NONE',  ( 0.01548846960707511190, 0.09061086148575973886, 0.5171215251571029681 ) ) ;
#14835=ADVANCED_FACE ( 'NONE', ( #4768 ), #14439, .T. ) ;
#14846=CARTESIAN_POINT ( 'NONE',  ( -0.01548846960707524721, 0.000000000000000000, 0.000000000000000000 ) ) ;
#14856=CARTESIAN_POINT ( 'NONE',  ( 0.02872242845530403876, -0.2464193076120092529, 0.4721747535844879051 ) ) ;
#14865=CARTESIAN_POINT ( 'NONE',  ( 0.05279755784604349411, -0.03988345070377457419, -0.4667183143801711398 ) ) ;
#14878=CARTESIAN_POINT ( 'NONE',  ( 0.1499999999999996336, -0.09061086148575810129, -0.5171215251571033011 ) ) ;
#14909=DIRECTION ( 'NONE',  ( 0.000000000000000000, 2.106022274728121591E-16, 1.000000000000000000 ) ) ;
#14910=CIRCLE ( 'NONE', #29720, 0.01499999999999995955 ) ;
#14916=CARTESIAN_POINT ( 'NONE',  ( -0.05616044724337275473, -0.01023656896654600613, -0.4592816919116775587 ) ) ;
#14920=CARTESIAN_POINT ( 'NONE',  ( -0.01895884884825269415, 0.2428741539084925405, 0.4598572020609172362 ) ) ;
#14921=CARTESIAN_POINT ( 'NONE',  ( 0.05268932808079455909, 0.009140209359766384919, 0.4686105243965638656 ) ) ;
#14922=CARTESIAN_POINT ( 'NONE',  ( 0.04575185649130682902, -0.4390455249589713116, -0.2110526333698215518 ) ) ;
#14927=CARTESIAN_POINT ( 'NONE',  ( -0.03654364704248898310, -0.3642884434512972947, -0.3592365245254302009 ) ) ;
#14937=DIRECTION ( 'NONE',  ( 1.000000000000000000, 0.000000000000000000, 0.000000000000000000 ) ) ;
#14941=ORIENTED_EDGE ( 'NONE', *, *, #16235, .F. ) ;
#14946=CARTESIAN_POINT ( 'NONE',  ( -0.01548846960721204577, 0.5203207976464816475, 0.08861466064783131424 ) ) ;
#14952=CARTESIAN_POINT ( 'NONE',  ( -0.05078493045284410146, 0.3164574661091585361, 0.3525385122722583531 ) ) ;
#14961=DIRECTION ( 'NONE',  ( -0.9378410757839563683, -0.2807814858886553133, -0.2039996905746434552 ) ) ;
#14975=ORIENTED_EDGE ( 'NONE', *, *, #34844, .F. ) ;
#14981=VERTEX_POINT ( 'NONE', #40145 ) ;
#14992=ORIENTED_EDGE ( 'NONE', *, *, #1175, .F. ) ;
#14994=CARTESIAN_POINT ( 'NONE',  ( -0.01548846960707517956, -0.2306506793134055211, -0.4716198300880352634 ) ) ;
#15005=CARTESIAN_POINT ( 'NONE',  ( 0.03868649100028075105, -0.4624880946332521336, 0.1149381524902348961 ) ) ;
#15010=DIRECTION ( 'NONE',  ( 1.972152263052529514E-31, 0.4685245517976875940, -0.8834504764630422002 ) ) ;
#15041=DIRECTION ( 'NONE',  ( -0.9378410757839558132, 0.3470650033817760383, -5.691349986800563656E-16 ) ) ;
#15060=ADVANCED_FACE ( 'NONE', ( #85 ), #25551, .T. ) ;
#15063=CARTESIAN_POINT ( 'NONE',  ( 0.02953079040095728247, 0.000000000000000000, 0.000000000000000000 ) ) ;
#15098=CARTESIAN_POINT ( 'NONE',  ( -0.04762200653274584888, -0.3170437565186433049, -0.3633076762442132845 ) ) ;
#15099=VERTEX_POINT ( 'NONE', #9498 ) ;
#15101=CARTESIAN_POINT ( 'NONE',  ( -0.05616044724337315719, -0.2616774468955898048, 0.3775835982344368791 ) ) ;
#15102=VECTOR ( 'NONE', #24072, 39.37007874015748143 ) ;
#15104=CARTESIAN_POINT ( 'NONE',  ( -0.04087116408467048739, -0.02106952151319366195, -0.4712677373718183738 ) ) ;
#15108=DIRECTION ( 'NONE',  ( 0.000000000000000000, -0.3090169943749375148, 0.9510565162951567508 ) ) ;
#15110=CARTESIAN_POINT ( 'NONE',  ( 0.03170953572519026598, -0.05433194795445580455, 0.4888234031312632122 ) ) ;
#15111=CARTESIAN_POINT ( 'NONE',  ( 0.05634206451479344818, -0.4396230623831607343, -0.1319606688783178661 ) ) ;
#15116=CARTESIAN_POINT ( 'NONE',  ( 0.03643058821097030359, -0.3645913838654561978, -0.3593578898915239517 ) ) ;
#15122=CARTESIAN_POINT ( 'NONE',  ( 0.02953079040095687308, 0.09152108205202803826, 0.5223162075576412988 ) ) ;
#15124=CARTESIAN_POINT ( 'NONE',  ( -0.03309057659885162456, -0.4608882367397833524, 0.2425133248664026742 ) ) ;
#15126=DIRECTION ( 'NONE',  ( -1.000000000000000000, -2.341930812374887555E-31, 1.664003471950578127E-31 ) ) ;
#15129=CARTESIAN_POINT ( 'NONE',  ( -0.02953079040095693900, -0.3810518745593889922, -0.3687679460475752902 ) ) ;
#15137=AXIS2_PLACEMENT_3D ( 'NONE', #30051, #26956, #39489 ) ;
#15142=CARTESIAN_POINT ( 'NONE',  ( -0.02238765564325659319, 0.2417679119117849829, 0.4518160092940282091 ) ) ;
#15158=ORIENTED_EDGE ( 'NONE', *, *, #1219, .F. ) ;
#15162=CARTESIAN_POINT ( 'NONE',  ( 0.02953079040094806068, 0.3810518745594044798, -0.3687679460475901116 ) ) ;
#15189=ADVANCED_FACE ( 'NONE', ( #19385, #6590 ), #26511, .F. ) ;
#15195=CARTESIAN_POINT ( 'NONE',  ( 0.04293317454820642920, 0.3457449726441622073, -0.3536934093827128756 ) ) ;
#15204=EDGE_CURVE ( 'NONE', #2287, #4624, #20754, .T. ) ;
#15212=VERTEX_POINT ( 'NONE', #5084 ) ;
#15235=CARTESIAN_POINT ( 'NONE',  ( -0.04140212552917654776, -0.4420250499596332094, 0.1614397576335104834 ) ) ;
#15236=ADVANCED_FACE ( 'NONE', ( #2431 ), #8380, .T. ) ;
#15248=CARTESIAN_POINT ( 'NONE',  ( -0.01548846960707504251, -0.09061086148575973886, 0.5171215251571027460 ) ) ;
#15258=EDGE_CURVE ( 'NONE', #35163, #30248, #5976, .T. ) ;
#15261=AXIS2_PLACEMENT_3D ( 'NONE', #10130, #19409, #3551 ) ;
#15262=VECTOR ( 'NONE', #9737, 39.37007874015748143 ) ;
#15280=CARTESIAN_POINT ( 'NONE',  ( -0.03674260963082490866, 0.4430101671189254908, -0.1867880763203697836 ) ) ;
#15291=AXIS2_PLACEMENT_3D ( 'NONE', #25008, #5461, #8762 ) ;
#15295=CARTESIAN_POINT ( 'NONE',  ( -0.01548846960712763066, 0.2450655194479529619, 0.4674710490748108516 ) ) ;
#15319=CARTESIAN_POINT ( 'NONE',  ( -0.03874953289574976228, 0.03331175461110465197, -0.4752512399555730016 ) ) ;
#15321=ORIENTED_EDGE ( 'NONE', *, *, #16734, .T. ) ;
#15323=DIRECTION ( 'NONE',  ( -0.9378410757839562573, 0.2807814858886506504, 0.2039996905746501998 ) ) ;
#15324=VECTOR ( 'NONE', #31211, 39.37007874015748143 ) ;
#15326=DIRECTION ( 'NONE',  ( 1.000000000000000000, 2.280301054154495132E-31, -1.664003471950577689E-31 ) ) ;
#15327=CARTESIAN_POINT ( 'NONE',  ( 0.05201840200954526566, -0.4527058363063625190, -0.1280872907206782041 ) ) ;
#15332=CARTESIAN_POINT ( 'NONE',  ( 0.04285640132273934449, -0.3459922227646587412, -0.3537374076363848374 ) ) ;
#15336=CIRCLE ( 'NONE', #14645, 0.5302738246768107233 ) ;
#15339=DIRECTION ( 'NONE',  ( -0.9378410757839558132, -0.3470650033817761493, -5.691349986800565628E-16 ) ) ;
#15349=CARTESIAN_POINT ( 'NONE',  ( -0.03159140494780132702, 0.4482517543799769411, 0.2030416442520433795 ) ) ;
#15355=CIRCLE ( 'NONE', #29158, 0.01499999999999994393 ) ;
#15356=CARTESIAN_POINT ( 'NONE',  ( -0.03642997641689365435, 0.2291049489869432521, 0.4577964116453020482 ) ) ;
#15361=CARTESIAN_POINT ( 'NONE',  ( 0.04229956186878635477, 0.2825373843407185115, -0.3739591931584693718 ) ) ;
#15378=AXIS2_PLACEMENT_3D ( 'NONE', #9800, #1192, #22373 ) ;
#15388=AXIS2_PLACEMENT_3D ( 'NONE', #33909, #11687, #37377 ) ;
#15396=ORIENTED_EDGE ( 'NONE', *, *, #13928, .T. ) ;
#15398=DIRECTION ( 'NONE',  ( -1.000000000000000000, -2.341930812374887555E-31, 1.664003471950578127E-31 ) ) ;
#15424=AXIS2_PLACEMENT_3D ( 'NONE', #1164, #3994, #26652 ) ;
#15427=ORIENTED_EDGE ( 'NONE', *, *, #36315, .T. ) ;
#15431=CYLINDRICAL_SURFACE ( 'NONE', #22596, 0.5399999999999999245 ) ;
#15437=ORIENTED_EDGE ( 'NONE', *, *, #24778, .T. ) ;
#15438=DIRECTION ( 'NONE',  ( 0.000000000000000000, 0.5877852522924756906, 0.8090169943749455639 ) ) ;
#15444=CIRCLE ( 'NONE', #25285, 0.01500000000000005669 ) ;
#15446=ORIENTED_EDGE ( 'NONE', *, *, #10810, .T. ) ;
#15447=ORIENTED_EDGE ( 'NONE', *, *, #20885, .T. ) ;
#15451=CARTESIAN_POINT ( 'NONE',  ( -0.05186792262757054101, -0.4530091620765513416, 0.1282979832840831225 ) ) ;
#15460=CIRCLE ( 'NONE', #30549, 0.01500000000000000291 ) ;
#15467=EDGE_CURVE ( 'NONE', #27640, #36370, #32387, .T. ) ;
#15474=VECTOR ( 'NONE', #24832, 39.37007874015748143 ) ;
#15476=CARTESIAN_POINT ( 'NONE',  ( 0.05634307799789363413, -0.2614070397638400545, 0.3772863199289458458 ) ) ;
#15491=VERTEX_POINT ( 'NONE', #17996 ) ;
#15494=DIRECTION ( 'NONE',  ( 0.000000000000000000, -0.3090169943749375148, 0.9510565162951567508 ) ) ;
#15503=EDGE_CURVE ( 'NONE', #15646, #15099, #14494, .T. ) ;
#15511=CARTESIAN_POINT ( 'NONE',  ( 0.05634301242525654313, -0.4396003943662976643, 0.1320237143668786528 ) ) ;
#15521=CARTESIAN_POINT ( 'NONE',  ( -0.05137569054209013830, -0.02238181648184470185, 0.4716086671401685804 ) ) ;
#15523=EDGE_CURVE ( 'NONE', #24870, #3369, #13733, .T. ) ;
#15526=CARTESIAN_POINT ( 'NONE',  ( -0.01548846960707447352, -0.2450655194479842147, 0.4674710490749294789 ) ) ;
#15531=CARTESIAN_POINT ( 'NONE',  ( -0.05076541221973657203, 0.04887304573182831707, -0.4712631214448597672 ) ) ;
#15533=ORIENTED_EDGE ( 'NONE', *, *, #34325, .F. ) ;
#15536=CARTESIAN_POINT ( 'NONE',  ( 0.01548846960707528191, 0.2306506793134049660, -0.4716198300880325434 ) ) ;
#15538=EDGE_CURVE ( 'NONE', #28751, #11876, #25040, .T. ) ;
#15541=CARTESIAN_POINT ( 'NONE',  ( 0.02881302694829601663, 0.4889319715862826543, 0.09562644460326606699 ) ) ;
#15543=CARTESIAN_POINT ( 'NONE',  ( 0.05201840200954449545, -0.2909588945328518417, -0.3697186091640858319 ) ) ;
#15550=EDGE_CURVE ( 'NONE', #32833, #28034, #2795, .T. ) ;
#15561=CARTESIAN_POINT ( 'NONE',  ( -0.02869712619511932336, 0.4892154842446466700, 0.09550911579581937427 ) ) ;
#15565=TOROIDAL_SURFACE ( 'NONE', #22163, 0.5250000000000000222, 0.01499999999999999944 ) ;
#15567=CARTESIAN_POINT ( 'NONE',  ( -0.05491348488830515018, 0.2919908616877288088, 0.3589493610278767788 ) ) ;
#15573=CARTESIAN_POINT ( 'NONE',  ( 0.04154009738085474857, 0.2622554993748598684, -0.3904256972020298533 ) ) ;
#15583=EDGE_CURVE ( 'NONE', #11795, #26731, #14585, .T. ) ;
#15588=CARTESIAN_POINT ( 'NONE',  ( 0.04946288932099957708, 0.2513464261306859737, -0.4057664802068605692 ) ) ;
#15590=DIRECTION ( 'NONE',  ( 0.9378410757839553691, 0.2807814858886550913, -0.2039996905746478406 ) ) ;
#15604=ORIENTED_EDGE ( 'NONE', *, *, #5882, .F. ) ;
#15610=CARTESIAN_POINT ( 'NONE',  ( 0.01548846960706681299, -0.09061086148575756005, 0.5171215251571267268 ) ) ;
#15622=CARTESIAN_POINT ( 'NONE',  ( 0.01548846960707524721, 0.5198120922912040642, 0.07362328916749247276 ) ) ;
#15632=CARTESIAN_POINT ( 'NONE',  ( -0.02235124290213174117, 0.07000983313419843757, 0.5077112423787081275 ) ) ;
#15633=CARTESIAN_POINT ( 'NONE',  ( 0.03158843595483476485, 0.2432919444504248463, 0.4277514783322106662 ) ) ;
#15637=VERTEX_POINT ( 'NONE', #18612 ) ;
#15638=CARTESIAN_POINT ( 'NONE',  ( 0.01548846960712810944, 0.4730347584885798429, -0.2341461249029115899 ) ) ;
#15646=VERTEX_POINT ( 'NONE', #40615 ) ;
#15649=CARTESIAN_POINT ( 'NONE',  ( -0.05634490452572756686, -0.4348542811545100251, 0.1466173361067427960 ) ) ;
#15659=CARTESIAN_POINT ( 'NONE',  ( 0.04157143636675726672, -0.2624507507128635564, 0.3902120892151791365 ) ) ;
#15664=CARTESIAN_POINT ( 'NONE',  ( -0.04946288932099660030, 0.4418470831553492073, 0.1805342557390142155 ) ) ;
#15666=LINE ( 'NONE', #37675, #8115 ) ;
#15667=ADVANCED_FACE ( 'NONE', ( #5650 ), #37324, .T. ) ;
#15668=DIRECTION ( 'NONE',  ( 0.000000000000000000, 0.9901182710308679136, -0.1402348365094949756 ) ) ;
#15669=ORIENTED_EDGE ( 'NONE', *, *, #35522, .T. ) ;
#15684=ORIENTED_EDGE ( 'NONE', *, *, #9267, .T. ) ;
#15696=EDGE_CURVE ( 'NONE', #30207, #20390, #39535, .T. ) ;
#15709=CARTESIAN_POINT ( 'NONE',  ( -0.04087116408467007800, 0.02106952151319393951, 0.4712677373718177076 ) ) ;
#15716=CARTESIAN_POINT ( 'NONE',  ( -0.03301200226531962600, -0.08829440931814541704, -0.5134711413293201465 ) ) ;
#15718=EDGE_LOOP ( 'NONE', ( #1205, #29248, #18560, #20352 ) ) ;
#15719=ORIENTED_EDGE ( 'NONE', *, *, #21595, .T. ) ;
#15722=FACE_OUTER_BOUND ( 'NONE', #22532, .T. ) ;
#15730=CYLINDRICAL_SURFACE ( 'NONE', #2989, 0.01499999999999999424 ) ;
#15737=UNCERTAINTY_MEASURE_WITH_UNIT (LENGTH_MEASURE( 1.000000000000000082E-05 ), #1126, 'distance_accuracy_value', 'NONE');
#15741=CARTESIAN_POINT ( 'NONE',  ( -0.04308449196698704159, 0.3346410801914455058, -0.3638139224395092741 ) ) ;
#15744=FACE_OUTER_BOUND ( 'NONE', #11983, .T. ) ;
#15750=CARTESIAN_POINT ( 'NONE',  ( -0.01899468245560667276, 0.2428515268394236537, 0.4597785848521163676 ) ) ;
#15757=DIRECTION ( 'NONE',  ( 2.526820087036053001E-31, 0.1402348365095093807, -0.9901182710308659152 ) ) ;
#15758=ADVANCED_FACE ( 'NONE', ( #9752 ), #10167, .T. ) ;
#15760=ORIENTED_EDGE ( 'NONE', *, *, #32319, .F. ) ;
#15767=EDGE_CURVE ( 'NONE', #15491, #37479, #29715, .T. ) ;
#15770=EDGE_CURVE ( 'NONE', #15212, #26023, #38902, .T. ) ;
#15771=DIRECTION ( 'NONE',  ( 1.000000000000000000, 2.341930812374887555E-31, -1.664003471950578127E-31 ) ) ;
#15773=CARTESIAN_POINT ( 'NONE',  ( 0.04762035657659002136, 0.3170509070583803490, -0.3633072608571736861 ) ) ;
#15782=ORIENTED_EDGE ( 'NONE', *, *, #19251, .F. ) ;
#15784=DIRECTION ( 'NONE',  ( -1.000000000000000000, -2.280301054154495132E-31, 1.664003471950577689E-31 ) ) ;
#15788=AXIS2_PLACEMENT_3D ( 'NONE', #5940, #21809, #12533 ) ;
#15791=ORIENTED_EDGE ( 'NONE', *, *, #11671, .F. ) ;
#15801=EDGE_CURVE ( 'NONE', #11795, #29903, #830, .T. ) ;
#15825=CARTESIAN_POINT ( 'NONE',  ( 0.05283102792148709759, -0.3063958269170704574, -0.3541938269410525031 ) ) ;
#15826=EDGE_LOOP ( 'NONE', ( #20152, #18898, #18887, #2724 ) ) ;
#15828=CARTESIAN_POINT ( 'NONE',  ( 0.03868264068766669866, 0.3066108573455321729, 0.3648330973802347832 ) ) ;
#15829=AXIS2_PLACEMENT_3D ( 'NONE', #4197, #10572, #20260 ) ;
#15838=CARTESIAN_POINT ( 'NONE',  ( -0.01895494625228095684, -0.4667936258712473419, 0.2292799240428166629 ) ) ;
#15847=CARTESIAN_POINT ( 'NONE',  ( -0.03478556507499973999, -0.4639967941986908873, 0.2267627654641752033 ) ) ;
#15848=DIRECTION ( 'NONE',  ( 1.000000000000000000, -2.325617669281430431E-12, -1.136734431350444160E-12 ) ) ;
#15857=DIRECTION ( 'NONE',  ( 5.879757087931980518E-34, 0.5877852522924756906, 0.8090169943749455639 ) ) ;
#15858=( BOUNDED_SURFACE ( )  B_SPLINE_SURFACE ( 3, 2, ( 
 ( #31176, #37138, #2182 ),
 ( #5843, #2992, #24199 ),
 ( #40005, #18211, #30956 ),
 ( #15541, #39816, #24809 ),
 ( #40422, #36723, #18002 ),
 ( #27886, #33627, #8341 ),
 ( #2578, #8531, #20911 ),
 ( #30562, #12250, #36530 ),
 ( #2385, #12043, #37330 ),
 ( #27480, #27674, #11828 ),
 ( #24602, #21706, #28092 ),
 ( #8951, #28692, #28273 ),
 ( #17098, #13800, #28477 ),
 ( #559, #1293, #12631 ),
 ( #35823, #13054, #139 ),
 ( #25415, #25607, #34846 ),
 ( #24988, #3792, #26364 ),
 ( #28883, #25197, #12853 ),
 ( #31379, #6456, #20201 ),
 ( #16154, #32726, #16347 ),
 ( #18836, #9342, #31557 ),
 ( #38898, #4533, #10726 ) ),
 .UNSPECIFIED., .F., .F., .T. ) 
 B_SPLINE_SURFACE_WITH_KNOTS ( ( 4, 2, 2, 2, 2, 2, 2, 2, 2, 2, 4 ),
 ( 3, 3 ),
 ( 0.002013519961495849157, 0.002780892266055832833, 0.003548264570615816075, 0.004315636875175799317, 0.004699323027455791155, 0.005083009179735782992, 0.005466695332015774830, 0.005850381484295766668, 0.006617753788855749476, 0.007385126093415732285, 0.008152498397975715960 ),
 ( 0.000000000000000000, 1.000000000000000000 ),
 .UNSPECIFIED. ) 
 GEOMETRIC_REPRESENTATION_ITEM ( )  RATIONAL_B_SPLINE_SURFACE ( (
 ( 1.000000000000000000, 0.7283825911960482014, 1.000000000000000000),
 ( 1.000000000000000000, 0.7404375345927979302, 1.000000000000000000),
 ( 1.000000000000000000, 0.7521483142434933766, 1.000000000000000000),
 ( 1.000000000000000000, 0.7744460733777726036, 1.000000000000000000),
 ( 1.000000000000000000, 0.7845612039381349989, 1.000000000000000000),
 ( 1.000000000000000000, 0.8022035258263032764, 1.000000000000000000),
 ( 1.000000000000000000, 0.8093965293321971899, 1.000000000000000000),
 ( 1.000000000000000000, 0.8169028692725515128, 1.000000000000000000),
 ( 1.000000000000000000, 0.8188329634864320861, 1.000000000000000000),
 ( 1.000000000000000000, 0.8214004505363229347, 1.000000000000000000),
 ( 1.000000000000000000, 0.8220602406259858164, 1.000000000000000000),
 ( 1.000000000000000000, 0.8220736605436884670, 1.000000000000000000),
 ( 1.000000000000000000, 0.8214126668415180355, 1.000000000000000000),
 ( 1.000000000000000000, 0.8188520474558893536, 1.000000000000000000),
 ( 1.000000000000000000, 0.8169545908335051898, 1.000000000000000000),
 ( 1.000000000000000000, 0.8094771004218379584, 1.000000000000000000),
 ( 1.000000000000000000, 0.8022723753807513569, 1.000000000000000000),
 ( 1.000000000000000000, 0.7845733350637317249, 1.000000000000000000),
 ( 1.000000000000000000, 0.7744472902493032551, 1.000000000000000000),
 ( 1.000000000000000000, 0.7522916829163440733, 1.000000000000000000),
 ( 1.000000000000000000, 0.7403553004665507364, 1.000000000000000000),
 ( 1.000000000000000000, 0.7283825911960212229, 1.000000000000000000) ) ) 
 REPRESENTATION_ITEM ( '' )  SURFACE ( )  );
#15868=CARTESIAN_POINT ( 'NONE',  ( -0.03875523708677544588, 0.4416911308383500434, 0.1785246905291629493 ) ) ;
#15874=ORIENTED_EDGE ( 'NONE', *, *, #8718, .T. ) ;
#15877=CIRCLE ( 'NONE', #4698, 0.01499999999999995087 ) ;
#15890=AXIS2_PLACEMENT_3D ( 'NONE', #7096, #23176, #5176 ) ;
#15906=CARTESIAN_POINT ( 'NONE',  ( 0.01895884884825074432, -0.5124024296374576348, -0.08888335629180295350 ) ) ;
#15911=AXIS2_PLACEMENT_3D ( 'NONE', #11517, #33496, #21177 ) ;
#15913=AXIS2_PLACEMENT_3D ( 'NONE', #33848, #30754, #3370 ) ;
#15915=CARTESIAN_POINT ( 'NONE',  ( -0.02881329448201254764, 0.06013561456248567999, 0.4945523155237982471 ) ) ;
#15918=CARTESIAN_POINT ( 'NONE',  ( -0.01896968469603269383, -0.2428673116372725704, 0.4598334287537050868 ) ) ;
#15923=ORIENTED_EDGE ( 'NONE', *, *, #25352, .T. ) ;
#15932=CARTESIAN_POINT ( 'NONE',  ( 0.03875673594170320896, -0.2524061059367321280, -0.4040421724581200191 ) ) ;
#15934=CARTESIAN_POINT ( 'NONE',  ( -0.01895884884825283639, 0.3622979475331356003, -0.3730907371368774039 ) ) ;
#15941=CIRCLE ( 'NONE', #27141, 0.1249999999999999584 ) ;
#15949=CIRCLE ( 'NONE', #6742, 0.01500000000000004281 ) ;
#15953=CARTESIAN_POINT ( 'NONE',  ( -0.04139678531769484110, 0.2901741387554239715, -0.3704845587920863048 ) ) ;
#15976=VECTOR ( 'NONE', #26160, 39.37007874015748143 ) ;
#15984=AXIS2_PLACEMENT_3D ( 'NONE', #30532, #18588, #21679 ) ;
#15987=CARTESIAN_POINT ( 'NONE',  ( 0.03672447062657326761, 0.2485879206383745099, -0.4115698867982595099 ) ) ;
#15994=EDGE_CURVE ( 'NONE', #34957, #23581, #22510, .T. ) ;
#15996=ORIENTED_EDGE ( 'NONE', *, *, #687, .T. ) ;
#16001=ORIENTED_EDGE ( 'NONE', *, *, #14200, .T. ) ;
#16025=FACE_OUTER_BOUND ( 'NONE', #24803, .T. ) ;
#16034=CARTESIAN_POINT ( 'NONE',  ( 0.1399999999999994582, 0.000000000000000000, 0.000000000000000000 ) ) ;
#16050=ORIENTED_EDGE ( 'NONE', *, *, #29559, .T. ) ;
#16052=VERTEX_POINT ( 'NONE', #6813 ) ;
#16064=CARTESIAN_POINT ( 'NONE',  ( -0.03647137243075361523, -0.4543612417835832251, 0.2356044583002005754 ) ) ;
#16065=CARTESIAN_POINT ( 'NONE',  ( -0.01548846960707524721, 0.2306506793134049660, -0.4716198300880325434 ) ) ;
#16074=CIRCLE ( 'NONE', #3572, 0.2149999999999999967 ) ;
#16076=CARTESIAN_POINT ( 'NONE',  ( -0.01548846960707524721, 0.2306506793134049660, -0.4716198300880325434 ) ) ;
#16083=CARTESIAN_POINT ( 'NONE',  ( 0.1499999999999994948, 0.3772621329472714558, 0.3651003739303416706 ) ) ;
#16084=CIRCLE ( 'NONE', #39058, 0.01500000000000006016 ) ;
#16087=CIRCLE ( 'NONE', #39064, 0.01499999999999996128 ) ;
#16089=CARTESIAN_POINT ( 'NONE',  ( -0.01548846960707422199, 0.4730347584886799295, 0.2341461249029806180 ) ) ;
#16094=CARTESIAN_POINT ( 'NONE',  ( -0.1399999999999997358, 0.2149999999999997469, -5.463695987328526437E-16 ) ) ;
#16117=( BOUNDED_SURFACE ( )  B_SPLINE_SURFACE ( 3, 2, ( 
 ( #16089, #3526, #31497 ),
 ( #13176, #6397, #18765 ),
 ( #28213, #31315, #21855 ),
 ( #3124, #31705, #19380 ),
 ( #9492, #6584, #12573 ),
 ( #25348, #28630, #22070 ),
 ( #15868, #15664, #28827 ),
 ( #80, #3736, #25133 ),
 ( #34594, #289, #19166 ),
 ( #685, #28417, #18965 ),
 ( #9699, #31914, #25746 ),
 ( #502, #38272, #12788 ),
 ( #37887, #10104, #22266 ),
 ( #16476, #12998, #25545 ),
 ( #34989, #38073, #9892 ),
 ( #22677, #35209, #7011 ),
 ( #19578, #32111, #3918 ),
 ( #29017, #884, #24932 ) ),
 .UNSPECIFIED., .F., .F., .F. ) 
 B_SPLINE_SURFACE_WITH_KNOTS ( ( 4, 2, 2, 2, 2, 2, 2, 2, 4 ),
 ( 3, 3 ),
 ( -0.001532620576208785709, -0.0007637936630078138219, 5.033250193158065461E-06, 0.0007738601633941299528, 0.001542687076595101840, 0.002311513989796073511, 0.003080340902997045615, 0.003849167816198017719, 0.004617994729398989390 ),
 ( 0.000000000000000000, 1.000000000000000000 ),
 .UNSPECIFIED. ) 
 GEOMETRIC_REPRESENTATION_ITEM ( )  RATIONAL_B_SPLINE_SURFACE ( (
 ( 1.000000000000000000, 0.7283825911960394306, 1.000000000000000000),
 ( 1.000000000000000000, 0.7404385082111522021, 1.000000000000000000),
 ( 1.000000000000000000, 0.7521504257741571386, 1.000000000000000000),
 ( 1.000000000000000000, 0.7744497410758119926, 1.000000000000000000),
 ( 1.000000000000000000, 0.7845654757376191446, 1.000000000000000000),
 ( 1.000000000000000000, 0.8022083990889726790, 1.000000000000000000),
 ( 1.000000000000000000, 0.8094167424698524016, 1.000000000000000000),
 ( 1.000000000000000000, 0.8194491993617223358, 1.000000000000000000),
 ( 1.000000000000000000, 0.8220634900779297816, 1.000000000000000000),
 ( 1.000000000000000000, 0.8220705070824532168, 1.000000000000000000),
 ( 1.000000000000000000, 0.8194468812479978048, 1.000000000000000000),
 ( 1.000000000000000000, 0.8094220769840463348, 1.000000000000000000),
 ( 1.000000000000000000, 0.8022659121985385999, 1.000000000000000000),
 ( 1.000000000000000000, 0.7845681159035809982, 1.000000000000000000),
 ( 1.000000000000000000, 0.7744426415185043933, 1.000000000000000000),
 ( 1.000000000000000000, 0.7522890290929258317, 1.000000000000000000),
 ( 1.000000000000000000, 0.7403540167215301171, 1.000000000000000000),
 ( 1.000000000000000000, 0.7283825911960428723, 1.000000000000000000) ) ) 
 REPRESENTATION_ITEM ( '' )  SURFACE ( )  );
#16138=CARTESIAN_POINT ( 'NONE',  ( -0.03868264068766711500, 0.4624969084406940767, -0.1149348357506045082 ) ) ;
#16140=CARTESIAN_POINT ( 'NONE',  ( -0.03647137243075569690, 0.08366781003817685969, 0.5049290013154925649 ) ) ;
#16145=VERTEX_POINT ( 'NONE', #31511 ) ;
#16154=CARTESIAN_POINT ( 'NONE',  ( 0.02242905165738221310, 0.4611019942560743989, 0.2233384654055277641 ) ) ;
#16156=CIRCLE ( 'NONE', #38489, 0.01500000000000005322 ) ;
#16160=CIRCLE ( 'NONE', #18801, 0.7750185148639454624 ) ;
#16165=VERTEX_POINT ( 'NONE', #38696 ) ;
#16177=CARTESIAN_POINT ( 'NONE',  ( -0.02953079040095652960, 0.2329676531120518090, 0.4763574306556300764 ) ) ;
#16179=CARTESIAN_POINT ( 'NONE',  ( -0.02953079040095700838, 0.000000000000000000, 0.000000000000000000 ) ) ;
#16183=CARTESIAN_POINT ( 'NONE',  ( 0.04760578872586068017, 0.4435171289962488994, -0.1893230556938475806 ) ) ;
#16187=EDGE_CURVE ( 'NONE', #26513, #14366, #8060, .T. ) ;
#16188=CARTESIAN_POINT ( 'NONE',  ( 0.01548846960712797240, 0.07651041855115807422, 0.5222379212567064277 ) ) ;
#16197=ORIENTED_EDGE ( 'NONE', *, *, #38648, .T. ) ;
#16226=CARTESIAN_POINT ( 'NONE',  ( 0.1499999999999994671, 0.5346638663566677385, -0.07572681171513587217 ) ) ;
#16235=EDGE_CURVE ( 'NONE', #36014, #39055, #33133, .T. ) ;
#16238=ADVANCED_FACE ( 'NONE', ( #27178 ), #17900, .T. ) ;
#16260=CARTESIAN_POINT ( 'NONE',  ( 0.000000000000000000, 0.000000000000000000, 0.000000000000000000 ) ) ;
#16279=ADVANCED_FACE ( 'NONE', ( #8436 ), #33522, .F. ) ;
#16280=CARTESIAN_POINT ( 'NONE',  ( 0.03674078017395952106, -0.3145504785376008750, 0.3636064179578495925 ) ) ;
#16281=EDGE_CURVE ( 'NONE', #34829, #30207, #25141, .T. ) ;
#16289=FACE_OUTER_BOUND ( 'NONE', #36808, .T. ) ;
#16301=ORIENTED_EDGE ( 'NONE', *, *, #10741, .F. ) ;
#16302=EDGE_LOOP ( 'NONE', ( #19226, #38238, #34561, #5757 ) ) ;
#16306=CARTESIAN_POINT ( 'NONE',  ( 0.000000000000000000, 0.000000000000000000, 0.000000000000000000 ) ) ;
#16317=FACE_OUTER_BOUND ( 'NONE', #10228, .T. ) ;
#16323=ADVANCED_FACE ( 'NONE', ( #30857 ), #30668, .T. ) ;
#16326=EDGE_CURVE ( 'NONE', #36862, #5225, #19585, .T. ) ;
#16332=CARTESIAN_POINT ( 'NONE',  ( -0.02881302694829873320, -0.06014213504334085109, 0.4945521340962454881 ) ) ;
#16333=ORIENTED_EDGE ( 'NONE', *, *, #5238, .F. ) ;
#16342=DIRECTION ( 'NONE',  ( 1.000000000000000000, 2.341930812374887555E-31, -1.664003471950578127E-31 ) ) ;
#16343=( BOUNDED_SURFACE ( )  B_SPLINE_SURFACE ( 3, 2, ( 
 ( #40636, #7080, #25006 ),
 ( #19460, #19046, #34469 ),
 ( #31793, #6674, #38354 ),
 ( #3610, #3997, #6284 ),
 ( #31397, #15741, #156 ),
 ( #37539, #34865, #31578 ),
 ( #12877, #38156, #16362 ),
 ( #9979, #22761, #31994 ),
 ( #15953, #12651, #25213 ),
 ( #28108, #9362, #19651 ),
 ( #32184, #37759, #9580 ),
 ( #22157, #35079, #6882 ),
 ( #22548, #25435, #37966 ),
 ( #3806, #22348, #28899 ),
 ( #760, #35285, #32597 ),
 ( #967, #7270, #16969 ),
 ( #4409, #29320, #16558 ),
 ( #1557, #23372, #14282 ),
 ( #38753, #13666, #38565 ),
 ( #4207, #8099, #26232 ),
 ( #20267, #35894, #26847 ),
 ( #32381, #16771, #13478 ) ),
 .UNSPECIFIED., .F., .F., .T. ) 
 B_SPLINE_SURFACE_WITH_KNOTS ( ( 4, 2, 2, 2, 2, 2, 2, 2, 2, 2, 4 ),
 ( 3, 3 ),
 ( 0.002013519961495850892, 0.002780892266055758240, 0.003548264570615666021, 0.004315636875175573803, 0.004699323027455527477, 0.005083009179735481151, 0.005466695332015434824, 0.005850381484295388498, 0.006617753788855296714, 0.007385126093415204929, 0.008152498397975112276 ),
 ( 0.000000000000000000, 1.000000000000000000 ),
 .UNSPECIFIED. ) 
 GEOMETRIC_REPRESENTATION_ITEM ( )  RATIONAL_B_SPLINE_SURFACE ( (
 ( 1.000000000000000000, 0.7283825911960390975, 1.000000000000000000),
 ( 1.000000000000000000, 0.7404375345927360907, 1.000000000000000000),
 ( 1.000000000000000000, 0.7521483142435548830, 1.000000000000000000),
 ( 1.000000000000000000, 0.7744460733776878936, 1.000000000000000000),
 ( 1.000000000000000000, 0.7845612039380914782, 1.000000000000000000),
 ( 1.000000000000000000, 0.8022035258263230384, 1.000000000000000000),
 ( 1.000000000000000000, 0.8093965293320422028, 1.000000000000000000),
 ( 1.000000000000000000, 0.8169028692726111318, 1.000000000000000000),
 ( 1.000000000000000000, 0.8188329634863092954, 1.000000000000000000),
 ( 1.000000000000000000, 0.8214004505364272957, 1.000000000000000000),
 ( 1.000000000000000000, 0.8220602406261449113, 1.000000000000000000),
 ( 1.000000000000000000, 0.8220736605435178257, 1.000000000000000000),
 ( 1.000000000000000000, 0.8214126668415498989, 1.000000000000000000),
 ( 1.000000000000000000, 0.8188520474558501627, 1.000000000000000000),
 ( 1.000000000000000000, 0.8169545908334044926, 1.000000000000000000),
 ( 1.000000000000000000, 0.8094771004220393529, 1.000000000000000000),
 ( 1.000000000000000000, 0.8022723753807737834, 1.000000000000000000),
 ( 1.000000000000000000, 0.7845733350637268400, 1.000000000000000000),
 ( 1.000000000000000000, 0.7744472902493437783, 1.000000000000000000),
 ( 1.000000000000000000, 0.7522916829163295294, 1.000000000000000000),
 ( 1.000000000000000000, 0.7403553004665951454, 1.000000000000000000),
 ( 1.000000000000000000, 0.7283825911960403188, 1.000000000000000000) ) ) 
 REPRESENTATION_ITEM ( '' )  SURFACE ( )  );
#16347=CARTESIAN_POINT ( 'NONE',  ( 0.03647137243074413671, 0.4543612417835987682, 0.2356044583002223913 ) ) ;
#16349=EDGE_LOOP ( 'NONE', ( #5640, #19219, #15446, #28278 ) ) ;
#16359=ORIENTED_EDGE ( 'NONE', *, *, #16675, .T. ) ;
#16362=CARTESIAN_POINT ( 'NONE',  ( -0.05279185365593493107, 0.3066183444142228653, -0.3541401447632883115 ) ) ;
#16368=CARTESIAN_POINT ( 'NONE',  ( 0.04157143636675642712, 0.4416880288200873417, -0.1614235308635272315 ) ) ;
#16379=ORIENTED_EDGE ( 'NONE', *, *, #3712, .T. ) ;
#16384=CARTESIAN_POINT ( 'NONE',  ( 0.01548846960707524721, 0.2306506793133126232, 0.4716198300880778960 ) ) ;
#16401=VERTEX_POINT ( 'NONE', #22237 ) ;
#16403=CYLINDRICAL_SURFACE ( 'NONE', #27902, 0.08139150547213643005 ) ;
#16424=CARTESIAN_POINT ( 'NONE',  ( 0.04293701532779483493, -0.2295363440003016231, 0.4381116105132966121 ) ) ;
#16454=CARTESIAN_POINT ( 'NONE',  ( 0.01548846960721255751, -0.3688619771570325612, 0.3775276577325259453 ) ) ;
#16456=CARTESIAN_POINT ( 'NONE',  ( -0.01548846960707348300, -0.4730347584886833157, 0.2341461249029785086 ) ) ;
#16464=DIRECTION ( 'NONE',  ( -1.416619696839557898E-11, 0.000000000000000000, -1.000000000000000000 ) ) ;
#16476=CARTESIAN_POINT ( 'NONE',  ( -0.03170953572519233377, 0.4816881781209654823, 0.09938198567066955369 ) ) ;
#16497=ORIENTED_EDGE ( 'NONE', *, *, #35051, .T. ) ;
#16506=CARTESIAN_POINT ( 'NONE',  ( -0.03654368633476864220, 0.08356155710620738475, 0.5047517311408972196 ) ) ;
#16525=ADVANCED_FACE ( 'NONE', ( #33085 ), #17253, .T. ) ;
#16537=ORIENTED_EDGE ( 'NONE', *, *, #29388, .F. ) ;
#16553=FACE_OUTER_BOUND ( 'NONE', #21416, .T. ) ;
#16558=CARTESIAN_POINT ( 'NONE',  ( -0.05078493045284266511, 0.2374933143169576932, -0.4099093267371657912 ) ) ;
#16561=ADVANCED_FACE ( 'NONE', ( #32873 ), #17462, .T. ) ;
#16571=CARTESIAN_POINT ( 'NONE',  ( 0.04285427992853851203, 0.4878399728613546649, -0.08281491827193158961 ) ) ;
#16585=AXIS2_PLACEMENT_3D ( 'NONE', #29, #12517, #3467 ) ;
#16592=EDGE_CURVE ( 'NONE', #5913, #2376, #15949, .T. ) ;
#16603=VERTEX_POINT ( 'NONE', #39061 ) ;
#16625=CARTESIAN_POINT ( 'NONE',  ( 0.03674078017396109619, 0.2486088097086621151, 0.4115158447297205258 ) ) ;
#16627=DIRECTION ( 'NONE',  ( 1.000000000000000000, 2.341930812374887555E-31, -1.664003471950578127E-31 ) ) ;
#16632=DIRECTION ( 'NONE',  ( 0.000000000000000000, 3.330669073875470114E-16, 1.000000000000000000 ) ) ;
#16635=APPLICATION_CONTEXT ( 'configuration controlled 3d designs of mechanical parts and assemblies' ) ;
#16637=VERTEX_POINT ( 'NONE', #14166 ) ;
#16640=CARTESIAN_POINT ( 'NONE',  ( -0.03868264068766702479, -0.03360988006411878837, 0.4753775160315156789 ) ) ;
#16658=EDGE_LOOP ( 'NONE', ( #27402, #6508, #9324 ) ) ;
#16662=CARTESIAN_POINT ( 'NONE',  ( -0.02231181081520831194, 0.07006449514257646893, -0.5077922075898729792 ) ) ;
#16671=CARTESIAN_POINT ( 'NONE',  ( 0.01548846960707309615, -0.3772621329473452301, 0.3651003739302747242 ) ) ;
#16672=AXIS2_PLACEMENT_3D ( 'NONE', #25809, #22519, #35446 ) ;
#16673=CARTESIAN_POINT ( 'NONE',  ( 0.03301162916268218783, -0.3732432789822014985, 0.3635092914618219262 ) ) ;
#16675=EDGE_CURVE ( 'NONE', #28193, #3229, #12012, .T. ) ;
#16687=CIRCLE ( 'NONE', #291, 0.01499999999999998904 ) ;
#16693=CARTESIAN_POINT ( 'NONE',  ( -0.01548846960707524721, 0.000000000000000000, 0.000000000000000000 ) ) ;
#16697=ADVANCED_BREP_SHAPE_REPRESENTATION ( '', ( #18435, #27819 ), #12683 ) ;
#16699=( BOUNDED_SURFACE ( )  B_SPLINE_SURFACE ( 3, 2, ( 
 ( #29986, #1820, #40452 ),
 ( #15750, #21346, #18035 ),
 ( #15142, #34069, #15356 ),
 ( #30984, #27703, #27914 ),
 ( #2807, #30785, #12277 ),
 ( #24835, #21549, #37357 ),
 ( #9169, #21733, #168 ),
 ( #34267, #6075, #11854 ),
 ( #33883, #24420, #28299 ),
 ( #18645, #27505, #25016 ),
 ( #31205, #37767, #40235 ),
 ( #12072, #6290, #3022 ),
 ( #2605, #12658, #36951 ),
 ( #22165, #34679, #30590 ),
 ( #25223, #21952, #15567 ),
 ( #24635, #8770, #2414 ),
 ( #5870, #9586, #14952 ),
 ( #28114, #12461, #37165 ),
 ( #5685, #8979, #34479 ),
 ( #40645, #40030, #18430 ),
 ( #37548, #9370, #18863 ),
 ( #31403, #3205, #18241 ) ),
 .UNSPECIFIED., .F., .F., .T. ) 
 B_SPLINE_SURFACE_WITH_KNOTS ( ( 4, 2, 2, 2, 2, 2, 2, 2, 2, 2, 4 ),
 ( 3, 3 ),
 ( 0.002013519961495849157, 0.002780892266055757373, 0.003548264570615666021, 0.004315636875175574670, 0.004699323027455529211, 0.005083009179735482885, 0.005466695332015436559, 0.005850381484295391100, 0.006617753788855299316, 0.007385126093415207531, 0.008152498397975115746 ),
 ( 0.000000000000000000, 1.000000000000000000 ),
 .UNSPECIFIED. ) 
 GEOMETRIC_REPRESENTATION_ITEM ( )  RATIONAL_B_SPLINE_SURFACE ( (
 ( 1.000000000000000000, 0.7283825911960390975, 1.000000000000000000),
 ( 1.000000000000000000, 0.7404375345927893814, 1.000000000000000000),
 ( 1.000000000000000000, 0.7521483142434828295, 1.000000000000000000),
 ( 1.000000000000000000, 0.7744460733777598360, 1.000000000000000000),
 ( 1.000000000000000000, 0.7845612039380338576, 1.000000000000000000),
 ( 1.000000000000000000, 0.8022035258263804369, 1.000000000000000000),
 ( 1.000000000000000000, 0.8093965293320565246, 1.000000000000000000),
 ( 1.000000000000000000, 0.8169028692726039154, 1.000000000000000000),
 ( 1.000000000000000000, 0.8188329634863094064, 1.000000000000000000),
 ( 1.000000000000000000, 0.8214004505364274067, 1.000000000000000000),
 ( 1.000000000000000000, 0.8220602406260869577, 1.000000000000000000),
 ( 1.000000000000000000, 0.8220736605435746691, 1.000000000000000000),
 ( 1.000000000000000000, 0.8214126668415572263, 1.000000000000000000),
 ( 1.000000000000000000, 0.8188520474558432793, 1.000000000000000000),
 ( 1.000000000000000000, 0.8169545908333754047, 1.000000000000000000),
 ( 1.000000000000000000, 0.8094771004220963073, 1.000000000000000000),
 ( 1.000000000000000000, 0.8022723753809752889, 1.000000000000000000),
 ( 1.000000000000000000, 0.7845733350635248904, 1.000000000000000000),
 ( 1.000000000000000000, 0.7744472902494010658, 1.000000000000000000),
 ( 1.000000000000000000, 0.7522916829162722419, 1.000000000000000000),
 ( 1.000000000000000000, 0.7403553004666372228, 1.000000000000000000),
 ( 1.000000000000000000, 0.7283825911960403188, 1.000000000000000000) ) ) 
 REPRESENTATION_ITEM ( '' )  SURFACE ( )  );
#16712=AXIS2_PLACEMENT_3D ( 'NONE', #18886, #38387, #7107 ) ;
#16720=TOROIDAL_SURFACE ( 'NONE', #4222, 0.5250000000000000222, 0.01499999999999999944 ) ;
#16722=CARTESIAN_POINT ( 'NONE',  ( -0.01548846960707477016, 0.2306506793134060762, 0.4716198300880319882 ) ) ;
#16724=AXIS2_PLACEMENT_3D ( 'NONE', #22112, #34634, #13221 ) ;
#16734=EDGE_CURVE ( 'NONE', #33009, #16401, #5346, .T. ) ;
#16755=EDGE_CURVE ( 'NONE', #1932, #5913, #35744, .T. ) ;
#16756=SPHERICAL_SURFACE ( 'NONE', #3568, 0.01499999999999999944 ) ;
#16758=ORIENTED_EDGE ( 'NONE', *, *, #20803, .T. ) ;
#16771=CARTESIAN_POINT ( 'NONE',  ( -0.02872242845530537450, 0.2464193076120113624, -0.4721747535844844079 ) ) ;
#16774=CARTESIAN_POINT ( 'NONE',  ( -0.04762200653274385048, -0.4700406811250516514, -0.1075684398553596738 ) ) ;
#16784=CARTESIAN_POINT ( 'NONE',  ( 0.03647060353176048014, 0.5060729159580583669, -0.07645842516611377204 ) ) ;
#16788=CARTESIAN_POINT ( 'NONE',  ( 0.03159140494780099395, 0.05458666898339488427, 0.4890560705835249600 ) ) ;
#16810=ORIENTED_EDGE ( 'NONE', *, *, #32050, .T. ) ;
#16818=DIRECTION ( 'NONE',  ( 1.000000000000000000, 2.341930812374887555E-31, -1.664003471950578127E-31 ) ) ;
#16819=ORIENTED_EDGE ( 'NONE', *, *, #15994, .F. ) ;
#16825=CARTESIAN_POINT ( 'NONE',  ( 0.02872242845530265445, -0.4768947642620242067, 0.2371557650701879294 ) ) ;
#16829=DIRECTION ( 'NONE',  ( 1.000000000000000000, 0.000000000000000000, 0.000000000000000000 ) ) ;
#16840=CARTESIAN_POINT ( 'NONE',  ( 0.03643058821097294731, 0.3645913838654474270, 0.3593578898915228415 ) ) ;
#16844=CIRCLE ( 'NONE', #18147, 0.01499999999999995955 ) ;
#16850=CARTESIAN_POINT ( 'NONE',  ( -0.05186792262757310146, -0.2910804482542292959, 0.3700673534428200462 ) ) ;
#16856=CARTESIAN_POINT ( 'NONE',  ( 0.01548846960707528191, 0.2306506793134049660, -0.4716198300880325434 ) ) ;
#16864=DIRECTION ( 'NONE',  ( 1.000000000000000000, 2.341930812374887555E-31, -1.664003471950578127E-31 ) ) ;
#16868=DIRECTION ( 'NONE',  ( -1.000000000000000000, -2.341930812374887555E-31, 1.664003471950578127E-31 ) ) ;
#16873=CIRCLE ( 'NONE', #18842, 0.2149999999999999967 ) ;
#16876=CARTESIAN_POINT ( 'NONE',  ( 0.02953079040095687308, 0.5250338024619264354, 0.07436286310882474215 ) ) ;
#16881=CARTESIAN_POINT ( 'NONE',  ( 0.04293701532779526514, 0.4875995331660214482, 0.08291810260646446940 ) ) ;
#16902=B_SPLINE_CURVE_WITH_KNOTS ( 'NONE', 3,
 ( #29004, #35579, #36183, #39079, #35991, #26937, #36390, #2258, #7797, #4504 ),
 .UNSPECIFIED., .F., .F.,
 ( 4, 2, 2, 2, 4 ),
 ( 8.771195575407730871E-17, 0.0007834172717712188216, 0.001566834543542350040, 0.002350251815313481474, 0.003133669087084613343 ),
 .UNSPECIFIED. ) ;
#16919=CARTESIAN_POINT ( 'NONE',  ( -0.02953079040095652960, 0.09152108205202803826, 0.5223162075576412988 ) ) ;
#16924=DIRECTION ( 'NONE',  ( 1.000000000000000000, 0.000000000000000000, 0.000000000000000000 ) ) ;
#16935=CARTESIAN_POINT ( 'NONE',  ( -2.372745691485074626E-32, 5.828670879282072084E-17, 0.1749999999999999889 ) ) ;
#16943=CARTESIAN_POINT ( 'NONE',  ( 0.1499999999999996336, 0.2450655194479851862, 0.4674710490749264258 ) ) ;
#16946=ORIENTED_EDGE ( 'NONE', *, *, #21550, .F. ) ;
#16947=CARTESIAN_POINT ( 'NONE',  ( 0.1499999999999990508, -0.4638115001431039053, -0.2459753896937787732 ) ) ;
#16961=DIRECTION ( 'NONE',  ( 0.3468893892380796595, 0.7770416411309266635, -0.5252371270032120121 ) ) ;
#16969=CARTESIAN_POINT ( 'NONE',  ( -0.05281452789367979683, 0.2421206024358339981, -0.4009379267244608247 ) ) ;
#16970=CARTESIAN_POINT ( 'NONE',  ( 0.1499999999999996059, -0.2372406987223689145, -0.4850946823762606330 ) ) ;
#16972=AXIS2_PLACEMENT_3D ( 'NONE', #32373, #7264, #752 ) ;
#16982=CARTESIAN_POINT ( 'NONE',  ( 0.01548846960721255751, -0.07651041855108323131, 0.5222379212565277928 ) ) ;
#16983=CARTESIAN_POINT ( 'NONE',  ( -0.02953079040095601959, -0.2329676531120513372, -0.4763574306556331295 ) ) ;
#17003=EDGE_CURVE ( 'NONE', #24257, #24870, #13598, .T. ) ;
#17023=DIRECTION ( 'NONE',  ( 0.000000000000000000, 3.330669073875470114E-16, 1.000000000000000000 ) ) ;
#17032=CARTESIAN_POINT ( 'NONE',  ( 0.04308611741967655756, 0.2425947520953613545, 0.4306844107907248920 ) ) ;
#17036=VERTEX_POINT ( 'NONE', #32504 ) ;
#17041=CARTESIAN_POINT ( 'NONE',  ( -0.05544444631433697451, -0.2544607094502361333, 0.3847718460475692548 ) ) ;
#17045=ORIENTED_EDGE ( 'NONE', *, *, #15801, .F. ) ;
#17053=CARTESIAN_POINT ( 'NONE',  ( -0.01548846960707463312, 0.4638115001430995199, 0.2459753896937826034 ) ) ;
#17056=CARTESIAN_POINT ( 'NONE',  ( -0.03662792686184479507, -0.4685177067346103508, 0.1089945633920634538 ) ) ;
#17066=CARTESIAN_POINT ( 'NONE',  ( -0.1399999999999997358, -9.793929126999064681E-17, -0.2150000000000000244 ) ) ;
#17080=DIRECTION ( 'NONE',  ( 1.000000000000000000, 2.280301054154495132E-31, -1.664003471950577689E-31 ) ) ;
#17096=VERTEX_POINT ( 'NONE', #10705 ) ;
#17098=CARTESIAN_POINT ( 'NONE',  ( 0.04211812644076717155, 0.4433543613217461599, 0.1530385388104468225 ) ) ;
#17100=DIRECTION ( 'NONE',  ( -1.000000000000000000, -2.280301054154495132E-31, 1.664003471950577689E-31 ) ) ;
#17113=VECTOR ( 'NONE', #15771, 39.37007874015748143 ) ;
#17130=DIRECTION ( 'NONE',  ( -3.543711097672506306E-32, 0.6954292836768432018, 0.7185945389471819489 ) ) ;
#17136=FACE_OUTER_BOUND ( 'NONE', #33793, .T. ) ;
#17149=CARTESIAN_POINT ( 'NONE',  ( -0.04140212552917778288, 0.4420250499596291571, -0.1614397576335124540 ) ) ;
#17162=CARTESIAN_POINT ( 'NONE',  ( -0.05137569054208215857, -0.4416101343670569834, -0.1670214652524110166 ) ) ;
#17164=CARTESIAN_POINT ( 'NONE',  ( -0.01548846960707477016, 0.5198120922912062847, -0.07362328916748482610 ) ) ;
#17172=AXIS2_PLACEMENT_3D ( 'NONE', #30447, #30226, #11529 ) ;
#17176=EDGE_CURVE ( 'NONE', #21164, #13737, #10619, .T. ) ;
#17179=FACE_OUTER_BOUND ( 'NONE', #11094, .T. ) ;
#17183=CARTESIAN_POINT ( 'NONE',  ( -0.05283094505690071052, 0.03968992937477607008, -0.4666439588235273828 ) ) ;
#17189=CARTESIAN_POINT ( 'NONE',  ( -0.02235124290213137341, 0.3550643254722171127, 0.3695962758878529320 ) ) ;
#17190=CARTESIAN_POINT ( 'NONE',  ( 0.01548846960707342575, 0.07651041855119247725, 0.5222379212568240003 ) ) ;
#17203=AXIS2_PLACEMENT_3D ( 'NONE', #4915, #37001, #26753 ) ;
#17215=CARTESIAN_POINT ( 'NONE',  ( 0.1399999999999994582, 0.000000000000000000, 0.000000000000000000 ) ) ;
#17216=CARTESIAN_POINT ( 'NONE',  ( 0.05561375719525241818, -0.4316271021131540264, 0.1617018132803446362 ) ) ;
#17220=CARTESIAN_POINT ( 'NONE',  ( -0.01548846960707524721, 0.000000000000000000, 0.000000000000000000 ) ) ;
#17222=DIRECTION ( 'NONE',  ( 1.000000000000000000, -2.549619951388196240E-12, 4.473262954207672140E-13 ) ) ;
#17228=CARTESIAN_POINT ( 'NONE',  ( -0.03309060444528683781, 0.5154120966056447983, -0.07470591001490199667 ) ) ;
#17235=ADVANCED_FACE ( 'NONE', ( #27417 ), #17534, .T. ) ;
#17238=CARTESIAN_POINT ( 'NONE',  ( -0.04760454375021173912, -0.3171166672795114883, 0.3633054878239699303 ) ) ;
#17246=CARTESIAN_POINT ( 'NONE',  ( 0.01548846960707370504, 0.2450655194479869625, -0.4674710490749294234 ) ) ;
#17251=CARTESIAN_POINT ( 'NONE',  ( 0.03309057659885114577, 0.5154121718708729594, -0.07470590733143775419 ) ) ;
#17252=ORIENTED_EDGE ( 'NONE', *, *, #31579, .T. ) ;
#17253=CYLINDRICAL_SURFACE ( 'NONE', #10689, 0.01499999999999999424 ) ;
#17290=DIRECTION ( 'NONE',  ( 0.000000000000000000, 3.330669073875470114E-16, 1.000000000000000000 ) ) ;
#17303=DIRECTION ( 'NONE',  ( -1.000000000000000000, -2.280301054154495132E-31, 1.664003471950577689E-31 ) ) ;
#17319=CIRCLE ( 'NONE', #16672, 0.01499999999999995781 ) ;
#17324=DIRECTION ( 'NONE',  ( -9.860761315262614725E-32, -0.9849933812516262766, 0.1725921171157263345 ) ) ;
#17342=B_SPLINE_CURVE_WITH_KNOTS ( 'NONE', 3,
 ( #38177, #29127, #988, #37780, #31605, #32011, #3420, #28733, #9795, #19870 ),
 .UNSPECIFIED., .F., .F.,
 ( 4, 2, 2, 2, 4 ),
 ( 0.000000000000000000, 0.0007746574062662862307, 0.001549314812532572461, 0.002323972218798858909, 0.003098629625065144923 ),
 .UNSPECIFIED. ) ;
#17354=CARTESIAN_POINT ( 'NONE',  ( 0.05634304521267768928, -2.731847993664263218E-15, -0.4588823192046729837 ) ) ;
#17358=CARTESIAN_POINT ( 'NONE',  ( -0.04760454375021105911, 0.4700983808485347248, -0.1075238135162311093 ) ) ;
#17374=CARTESIAN_POINT ( 'NONE',  ( -0.02953079040095612021, -0.5250338024619279897, -0.07436286310882828099 ) ) ;
#17381=CIRCLE ( 'NONE', #39047, 0.01500000000000003934 ) ;
#17388=CARTESIAN_POINT ( 'NONE',  ( -0.04229883635637923800, -0.2719170545448721388, -0.3816769773555965806 ) ) ;
#17395=CARTESIAN_POINT ( 'NONE',  ( 0.04293317454820616552, 0.2295413494973359003, 0.4381202835071925650 ) ) ;
#17396=CARTESIAN_POINT ( 'NONE',  ( 0.02881408050861127002, 0.06014027758172069138, 0.4945500181289073649 ) ) ;
#17398=SPHERICAL_SURFACE ( 'NONE', #10150, 0.01499999999999999944 ) ;
#17403=CARTESIAN_POINT ( 'NONE',  ( -0.04293701532779585495, -0.2295363440003029276, -0.4381116105132951688 ) ) ;
#17404=EDGE_LOOP ( 'NONE', ( #30847, #4934, #8199, #32366 ) ) ;
#17405=AXIS2_PLACEMENT_3D ( 'NONE', #24358, #17582, #21279 ) ;
#17423=CARTESIAN_POINT ( 'NONE',  ( 0.04308558661660559508, -0.4494156853470195334, 0.2058346122080974006 ) ) ;
#17435=CARTESIAN_POINT ( 'NONE',  ( 0.03672447062657503702, 0.3146083306767443188, 0.3636032511890208707 ) ) ;
#17446=CARTESIAN_POINT ( 'NONE',  ( -0.05269191099235827347, -0.2718205810683996804, 0.3817379850160088073 ) ) ;
#17455=CARTESIAN_POINT ( 'NONE',  ( -0.04582889109739289590, 0.2312034125369032966, -0.4285435303321075695 ) ) ;
#17458=ORIENTED_EDGE ( 'NONE', *, *, #35406, .F. ) ;
#17462=SPHERICAL_SURFACE ( 'NONE', #33669, 0.01499999999999999944 ) ;
#17469=AXIS2_PLACEMENT_3D ( 'NONE', #34452, #24200, #24389 ) ;
#17472=EDGE_CURVE ( 'NONE', #26954, #36862, #4508, .T. ) ;
#17479=EDGE_CURVE ( 'NONE', #26954, #19390, #2759, .T. ) ;
#17480=ADVANCED_FACE ( 'NONE', ( #38673 ), #4105, .T. ) ;
#17482=CARTESIAN_POINT ( 'NONE',  ( -0.02587796518899032269, 2.459870571432321995E-16, 0.5399999999999999245 ) ) ;
#17489=CARTESIAN_POINT ( 'NONE',  ( 0.04229956186878531393, -0.4483852441756314144, 0.1364680347311799102 ) ) ;
#17491=EDGE_CURVE ( 'NONE', #11991, #2287, #17868, .T. ) ;
#17498=VERTEX_POINT ( 'NONE', #32891 ) ;
#17502=EDGE_CURVE ( 'NONE', #37027, #33332, #40288, .T. ) ;
#17506=EDGE_LOOP ( 'NONE', ( #21979, #17510, #8500, #32988 ) ) ;
#17510=ORIENTED_EDGE ( 'NONE', *, *, #39902, .T. ) ;
#17517=ORIENTED_EDGE ( 'NONE', *, *, #17547, .T. ) ;
#17526=ADVANCED_FACE ( 'NONE', ( #32701 ), #35391, .F. ) ;
#17528=FACE_OUTER_BOUND ( 'NONE', #24056, .T. ) ;
#17534=CYLINDRICAL_SURFACE ( 'NONE', #33605, 0.5400000000000004796 ) ;
#17537=SPHERICAL_SURFACE ( 'NONE', #36998, 0.01499999999999999944 ) ;
#17547=EDGE_CURVE ( 'NONE', #31970, #30050, #34723, .T. ) ;
#17566=DIRECTION ( 'NONE',  ( -1.000000000000000000, -2.280301054154495132E-31, 1.664003471950577689E-31 ) ) ;
#17578=EDGE_CURVE ( 'NONE', #30050, #28751, #27718, .T. ) ;
#17582=DIRECTION ( 'NONE',  ( -2.526820087036053001E-31, -0.1402348365095093807, 0.9901182710308659152 ) ) ;
#17583=CARTESIAN_POINT ( 'NONE',  ( 0.05283102792148602206, -0.4315398646667508165, 0.1819478359276331114 ) ) ;
#17584=CARTESIAN_POINT ( 'NONE',  ( -0.02242905165738937404, -0.5043144057283245330, -0.09034433801567860745 ) ) ;
#17594=EDGE_CURVE ( 'NONE', #22691, #38078, #27076, .T. ) ;
#17596=CARTESIAN_POINT ( 'NONE',  ( -0.05279185365593280777, -0.2420570131477388365, -0.4010466975930389033 ) ) ;
#17602=CARTESIAN_POINT ( 'NONE',  ( 0.05561176441985762192, 0.2871508736821606345, 0.3605511861568527765 ) ) ;
#17603=CARTESIAN_POINT ( 'NONE',  ( 0.04157143636675603160, 0.01703379379375214581, 0.4699528923077435083 ) ) ;
#17619=ADVANCED_FACE ( 'NONE', ( #40078 ), #30215, .T. ) ;
#17625=CARTESIAN_POINT ( 'NONE',  ( 0.05269111014005897070, -0.4484844745756915718, 0.1361491033660628125 ) ) ;
#17629=CARTESIAN_POINT ( 'NONE',  ( 0.04582897286455959313, -0.06484386734940368602, 0.4825967645925794414 ) ) ;
#17631=DIRECTION ( 'NONE',  ( -1.000000000000000000, -2.280301054154495132E-31, 1.664003471950577689E-31 ) ) ;
#17636=CARTESIAN_POINT ( 'NONE',  ( 0.03664605387828118871, 0.3149102792626792269, -0.3635688186731551585 ) ) ;
#17649=CARTESIAN_POINT ( 'NONE',  ( -0.05082303569918694003, 0.4330427793496118838, 0.1918498709088739262 ) ) ;
#17660=ORIENTED_EDGE ( 'NONE', *, *, #11671, .T. ) ;
#17677=CARTESIAN_POINT ( 'NONE',  ( -0.01548846960707490547, 0.5346638663566677385, -0.07572681171513587217 ) ) ;
#17678=CARTESIAN_POINT ( 'NONE',  ( 0.04230188431063434257, -0.008729788072062542176, -0.4686063437799722342 ) ) ;
#17686=EDGE_CURVE ( 'NONE', #16637, #37027, #37211, .T. ) ;
#17693=CARTESIAN_POINT ( 'NONE',  ( 0.1499999999999990508, -0.4730347584886803736, -0.2341461249029834490 ) ) ;
#17702=VERTEX_POINT ( 'NONE', #6341 ) ;
#17727=CARTESIAN_POINT ( 'NONE',  ( 0.02953079040094795660, 0.09152108205202806601, -0.5223162075576639474 ) ) ;
#17733=ADVANCED_FACE ( 'NONE', ( #3464 ), #441, .T. ) ;
#17738=CARTESIAN_POINT ( 'NONE',  ( 0.02231181081520650783, 0.3551561381230151637, 0.3696296485972545010 ) ) ;
#17745=DIRECTION ( 'NONE',  ( -0.9378410757839561462, -0.1072489841977624786, 0.3300784330442383396 ) ) ;
#17748=TOROIDAL_SURFACE ( 'NONE', #31546, 0.5250000000000000222, 0.01499999999999999944 ) ;
#17758=DIRECTION ( 'NONE',  ( 0.9378410757839513723, -0.2807814858886641396, 0.2039996905746546685 ) ) ;
#17763=CARTESIAN_POINT ( 'NONE',  ( 0.03309057659885086822, -0.4608882367397868496, -0.2425133248663977337 ) ) ;
#17765=LINE ( 'NONE', #27252, #32518 ) ;
#17773=CIRCLE ( 'NONE', #28938, 0.01500000000000002894 ) ;
#17776=DIRECTION ( 'NONE',  ( -1.000000000000000000, -2.280301054154495132E-31, 1.664003471950577689E-31 ) ) ;
#17777=DIRECTION ( 'NONE',  ( -0.000000000000000000, 0.3090169943749569437, 0.9510565162951504226 ) ) ;
#17778=CARTESIAN_POINT ( 'NONE',  ( -0.03301200226531783577, -0.3732424419978427887, -0.3635087277994391575 ) ) ;
#17781=CARTESIAN_POINT ( 'NONE',  ( -0.02953079040095652960, 0.5250338024619264354, 0.07436286310882474215 ) ) ;
#17787=CARTESIAN_POINT ( 'NONE',  ( -0.04229956186878665314, 0.2825373843407192331, 0.3739591931584692608 ) ) ;
#17789=CARTESIAN_POINT ( 'NONE',  ( 0.04946288932099927871, -0.4635771722446667686, -0.1136559182874704588 ) ) ;
#17796=VERTEX_POINT ( 'NONE', #27045 ) ;
#17804=CARTESIAN_POINT ( 'NONE',  ( -0.01548846960721238578, 0.2450655194478933985, -0.4674710490746305513 ) ) ;
#17815=AXIS2_PLACEMENT_3D ( 'NONE', #34996, #28832, #7016 ) ;
#17838=AXIS2_PLACEMENT_3D ( 'NONE', #17901, #39926, #11743 ) ;
#17842=CARTESIAN_POINT ( 'NONE',  ( -0.03309057659885162456, 0.2303206601891044092, -0.4671007096900172684 ) ) ;
#17843=AXIS2_PLACEMENT_3D ( 'NONE', #15063, #12186, #34177 ) ;
#17854=CARTESIAN_POINT ( 'NONE',  ( -0.02869942827333544708, -0.3396431753871640424, 0.3648167270360663794 ) ) ;
#17868=CIRCLE ( 'NONE', #30363, 0.01500000000000002200 ) ;
#17869=CARTESIAN_POINT ( 'NONE',  ( 0.03650581953630534227, 0.2290855126858382385, -0.4575806651622376653 ) ) ;
#17876=CARTESIAN_POINT ( 'NONE',  ( 0.06980746140711582837, -4.527947890665460015E-17, -0.2150000000000000244 ) ) ;
#17887=DIRECTION ( 'NONE',  ( 1.000000000000000000, 2.341930812374887555E-31, -1.664003471950578127E-31 ) ) ;
#17891=CARTESIAN_POINT ( 'NONE',  ( 0.01548846960721238578, 0.5203207976464816475, -0.08861466064783077301 ) ) ;
#17893=EDGE_LOOP ( 'NONE', ( #8075, #7771, #28734 ) ) ;
#17894=AXIS2_PLACEMENT_3D ( 'NONE', #16083, #12569, #18761 ) ;
#17900=TOROIDAL_SURFACE ( 'NONE', #14614, 0.5250000000000000222, 0.01499999999999999944 ) ;
#17901=CARTESIAN_POINT ( 'NONE',  ( 0.01548846960707524721, 0.000000000000000000, 0.000000000000000000 ) ) ;
#17924=CARTESIAN_POINT ( 'NONE',  ( 0.01548846960707524721, 0.000000000000000000, 0.000000000000000000 ) ) ;
#17927=DIRECTION ( 'NONE',  ( 1.000000000000000000, -1.609192080949047896E-13, 1.762723797404871399E-11 ) ) ;
#17929=CIRCLE ( 'NONE', #4760, 0.01500000000000004628 ) ;
#17931=AXIS2_PLACEMENT_3D ( 'NONE', #6198, #36200, #20379 ) ;
#17933=CARTESIAN_POINT ( 'NONE',  ( 0.05201840200954339216, -0.01807554437688853669, -0.4701299851801460372 ) ) ;
#17934=B_SPLINE_CURVE_WITH_KNOTS ( 'NONE', 3,
 ( #16177, #13073, #34671, #6478, #28499, #577, #28291, #25624, #10194, #28715, #3199, #3398, #19253, #12455, #18854, #374, #25835, #9775 ),
 .UNSPECIFIED., .F., .F.,
 ( 4, 2, 2, 2, 2, 2, 2, 2, 4 ),
 ( 0.000000000000000000, 0.0007746617437634299155, 0.001549323487526859397, 0.002323985231290289204, 0.003098646975053718795, 0.003873308718817148385, 0.004647970462580578409, 0.005422632206344008866, 0.006197293950107437589 ),
 .UNSPECIFIED. ) ;
#17953=VECTOR ( 'NONE', #26630, 39.37007874015748143 ) ;
#17985=DIRECTION ( 'NONE',  ( -0.3468893892380646160, -0.9373665302208734618, -0.03180785525185502588 ) ) ;
#17992=CARTESIAN_POINT ( 'NONE',  ( -0.03170752374382680705, 0.05433200130547150702, -0.4888275802721897545 ) ) ;
#17995=ORIENTED_EDGE ( 'NONE', *, *, #500, .T. ) ;
#17996=CARTESIAN_POINT ( 'NONE',  ( 0.01548846960707528191, -0.4770632572900429524, 0.2530032579707506835 ) ) ;
#17998=CARTESIAN_POINT ( 'NONE',  ( 0.05201840200954539056, 0.01807554437689167307, 0.4701299851801462593 ) ) ;
#17999=CARTESIAN_POINT ( 'NONE',  ( 0.05201782277452800252, -0.4415348900197206272, -0.1624722611720488818 ) ) ;
#18002=CARTESIAN_POINT ( 'NONE',  ( 0.04574984450155244325, 0.4792536329485966862, 0.08732079948164367389 ) ) ;
#18004=CARTESIAN_POINT ( 'NONE',  ( -0.05634301242525835418, -0.2780425975185365495, -0.3652000572937718070 ) ) ;
#18035=CARTESIAN_POINT ( 'NONE',  ( -0.03303708955568322031, 0.2303604322856135367, 0.4672397951413029826 ) ) ;
#18046=EDGE_CURVE ( 'NONE', #30357, #25200, #9932, .T. ) ;
#18054=DIRECTION ( 'NONE',  ( -0.3468893892380659483, 0.7770416411310542282, -0.5252371270030326000 ) ) ;
#18065=CARTESIAN_POINT ( 'NONE',  ( -0.01548846960707517956, -0.09061086148575756005, -0.5171215251571035232 ) ) ;
#18067=CARTESIAN_POINT ( 'NONE',  ( 0.1499999999999993561, 0.000000000000000000, 0.000000000000000000 ) ) ;
#18070=DIRECTION ( 'NONE',  ( 0.000000000000000000, 0.9510565162951502005, -0.3090169943749580539 ) ) ;
#18083=ADVANCED_FACE ( 'NONE', ( #25345 ), #3520, .T. ) ;
#18084=CARTESIAN_POINT ( 'NONE',  ( -0.1499999999999996336, -7.971802777789936683E-17, -0.1750000000000000167 ) ) ;
#18095=CARTESIAN_POINT ( 'NONE',  ( 0.03868264068766501251, -0.4417248602032650684, 0.1788646266443654487 ) ) ;
#18097=DIRECTION ( 'NONE',  ( 0.000000000000000000, 0.9901182710308955581, -0.1402348365092997984 ) ) ;
#18099=DIRECTION ( 'NONE',  ( 0.000000000000000000, 3.330669073875470114E-16, 1.000000000000000000 ) ) ;
#18108=ORIENTED_EDGE ( 'NONE', *, *, #28166, .F. ) ;
#18111=AXIS2_PLACEMENT_3D ( 'NONE', #10833, #20492, #23409 ) ;
#18112=CIRCLE ( 'NONE', #6906, 0.5400000000000018119 ) ;
#18114=CARTESIAN_POINT ( 'NONE',  ( 0.02953079040095728247, 0.000000000000000000, 0.000000000000000000 ) ) ;
#18123=ORIENTED_EDGE ( 'NONE', *, *, #31579, .F. ) ;
#18125=CIRCLE ( 'NONE', #4315, 0.01500000000000004281 ) ;
#18127=CARTESIAN_POINT ( 'NONE',  ( -0.04945776359514589965, -0.4635931069071527189, 0.1136454792236764738 ) ) ;
#18147=AXIS2_PLACEMENT_3D ( 'NONE', #20685, #29940, #11624 ) ;
#18148=CARTESIAN_POINT ( 'NONE',  ( 0.04308611741967211667, 0.05688666786373643147, -0.4910246251072729051 ) ) ;
#18160=DIRECTION ( 'NONE',  ( 1.000000000000000000, 2.341930812374887555E-31, -1.664003471950578127E-31 ) ) ;
#18163=CARTESIAN_POINT ( 'NONE',  ( -0.02953079040095628327, 0.4684706630666132243, -0.2484463060367378962 ) ) ;
#18178=CARTESIAN_POINT ( 'NONE',  ( 0.02953079040095704308, -0.3810518745593846068, 0.3687679460475796756 ) ) ;
#18189=AXIS2_PLACEMENT_3D ( 'NONE', #23775, #36291, #37118 ) ;
#18191=CARTESIAN_POINT ( 'NONE',  ( -0.01548846960707524721, 0.000000000000000000, 0.000000000000000000 ) ) ;
#18196=CARTESIAN_POINT ( 'NONE',  ( -0.04085667396267390200, -0.2941474082995332862, 0.3688418229621477362 ) ) ;
#18199=CARTESIAN_POINT ( 'NONE',  ( -0.04085667396267567836, 0.02117046819985016898, -0.4712948116111316255 ) ) ;
#18203=ORIENTED_EDGE ( 'NONE', *, *, #21550, .T. ) ;
#18206=CARTESIAN_POINT ( 'NONE',  ( 0.05076679145662072595, 0.04886774829954446814, 0.4712599967968605363 ) ) ;
#18207=CARTESIAN_POINT ( 'NONE',  ( 0.05078310099560560953, -0.4330765661303609404, -0.1920364777915913590 ) ) ;
#18211=CARTESIAN_POINT ( 'NONE',  ( 0.03474824846560953945, 0.5087747035359670988, 0.08925086559848140200 ) ) ;
#18214=CARTESIAN_POINT ( 'NONE',  ( 0.02238826743733619493, -0.3549908576167588592, -0.3695531484129501720 ) ) ;
#18216=ORIENTED_EDGE ( 'NONE', *, *, #20268, .T. ) ;
#18234=CARTESIAN_POINT ( 'NONE',  ( -0.03158843595483497996, 0.4819971762524428716, 0.09920191295802914533 ) ) ;
#18241=CARTESIAN_POINT ( 'NONE',  ( -0.02953079040095645327, 0.3810518745593871048, 0.3687679460475778437 ) ) ;
#18255=ORIENTED_EDGE ( 'NONE', *, *, #24649, .F. ) ;
#18261=CARTESIAN_POINT ( 'NONE',  ( 0.02881195911414642305, 0.3393447726770189576, -0.3647551865608069654 ) ) ;
#18264=CARTESIAN_POINT ( 'NONE',  ( -0.01548846960707538425, -0.4638115001430989648, 0.2459753896937853235 ) ) ;
#18270=VECTOR ( 'NONE', #34666, 39.37007874015748143 ) ;
#18272=ORIENTED_EDGE ( 'NONE', *, *, #32808, .T. ) ;
#18278=CARTESIAN_POINT ( 'NONE',  ( -0.01548846960707531660, -0.2306506793134055211, -0.4716198300880352634 ) ) ;
#18299=CARTESIAN_POINT ( 'NONE',  ( 0.03662792686184294239, -0.4431041838557951418, 0.1872093443778323762 ) ) ;
#18314=ORIENTED_EDGE ( 'NONE', *, *, #24981, .F. ) ;
#18315=ORIENTED_EDGE ( 'NONE', *, *, #21821, .T. ) ;
#18317=ORIENTED_EDGE ( 'NONE', *, *, #28166, .T. ) ;
#18322=DIRECTION ( 'NONE',  ( 1.000000000000000000, 2.341930812374887555E-31, -1.664003471950578127E-31 ) ) ;
#18327=CARTESIAN_POINT ( 'NONE',  ( -0.04574984450155034077, -0.4792536329486041247, 0.08732079948164171712 ) ) ;
#18347=CARTESIAN_POINT ( 'NONE',  ( 0.04946288932100178365, -0.03516002272507855186, -0.4760097007310896688 ) ) ;
#18352=EDGE_CURVE ( 'NONE', #9503, #26696, #34643, .T. ) ;
#18358=EDGE_LOOP ( 'NONE', ( #35561, #31722, #20822, #34792, #9145, #35058, #7284, #8396, #5243, #24193, #34336, #13760, #26767, #32572 ) ) ;
#18364=CARTESIAN_POINT ( 'NONE',  ( -0.04285561529641556539, 0.4433460678679621014, -0.2197428102801899097 ) ) ;
#18371=CARTESIAN_POINT ( 'NONE',  ( -0.04582713223189532892, -0.3361263728083078717, 0.3523178389613212391 ) ) ;
#18386=CARTESIAN_POINT ( 'NONE',  ( -0.03303708955568183253, -0.08827115631760176773, 0.5134073995267878221 ) ) ;
#18389=CARTESIAN_POINT ( 'NONE',  ( -0.02953079040095632490, -0.2329676531120498939, 0.4763574306556330185 ) ) ;
#18390=CIRCLE ( 'NONE', #8552, 0.01500000000000001506 ) ;
#18393=CARTESIAN_POINT ( 'NONE',  ( -0.04230258372739731376, -0.004226829447873794131, -0.4686050468223225129 ) ) ;
#18397=DIRECTION ( 'NONE',  ( 1.000000000000000000, 0.000000000000000000, 0.000000000000000000 ) ) ;
#18398=VECTOR ( 'NONE', #124, 39.37007874015748143 ) ;
#18401=CARTESIAN_POINT ( 'NONE',  ( 0.05279755784604278634, -0.4562001582273347844, -0.1062924750453443506 ) ) ;
#18412=CARTESIAN_POINT ( 'NONE',  ( -0.03650581953630595983, -0.5059763899182400104, 0.07647306779615177519 ) ) ;
#18420=CARTESIAN_POINT ( 'NONE',  ( -0.06980746140711582837, 0.1750000000000001832, 0.000000000000000000 ) ) ;
#18430=CARTESIAN_POINT ( 'NONE',  ( -0.03647137243075408014, 0.3644785006310322650, 0.3593174381849622012 ) ) ;
#18435=MANIFOLD_SOLID_BREP ( 'Combine1', #14175 ) ;
#18443=CARTESIAN_POINT ( 'NONE',  ( 0.1499999999999994948, 0.2450655194479797461, -0.4674710490749308112 ) ) ;
#18458=ORIENTED_EDGE ( 'NONE', *, *, #10239, .F. ) ;
#18462=EDGE_LOOP ( 'NONE', ( #5994, #29346, #33619 ) ) ;
#18468=AXIS2_PLACEMENT_3D ( 'NONE', #16094, #31713, #35215 ) ;
#18469=AXIS2_PLACEMENT_3D ( 'NONE', #33789, #2332, #30097 ) ;
#18483=DIRECTION ( 'NONE',  ( 1.000000000000000000, 0.000000000000000000, 0.000000000000000000 ) ) ;
#18508=CARTESIAN_POINT ( 'NONE',  ( -0.02872242845530475694, -0.07817994906156883195, -0.5268390348591152073 ) ) ;
#18509=FACE_OUTER_BOUND ( 'NONE', #294, .T. ) ;
#18512=CARTESIAN_POINT ( 'NONE',  ( 0.03662792686184426078, 0.4431041838557911450, -0.1872093443778329869 ) ) ;
#18521=ORIENTED_EDGE ( 'NONE', *, *, #8139, .T. ) ;
#18524=CARTESIAN_POINT ( 'NONE',  ( -0.02872242845530404223, -0.5252126300208065368, 0.08844866507292674374 ) ) ;
#18527=AXIS2_PLACEMENT_3D ( 'NONE', #11105, #4706, #5523 ) ;
#18529=CARTESIAN_POINT ( 'NONE',  ( -0.02953079040095687308, 0.3810518745593911571, 0.3687679460475725701 ) ) ;
#18534=DIRECTION ( 'NONE',  ( 0.000000000000000000, -0.1725921171157271672, 0.9849933812516259435 ) ) ;
#18539=CARTESIAN_POINT ( 'NONE',  ( 0.01548846960707340320, -0.2450655194479847421, 0.4674710490749314218 ) ) ;
#18549=CARTESIAN_POINT ( 'NONE',  ( 0.05561176441985739988, -0.2541700551350220549, 0.3845131534397776552 ) ) ;
#18560=ORIENTED_EDGE ( 'NONE', *, *, #10798, .T. ) ;
#18563=EDGE_CURVE ( 'NONE', #10925, #4078, #6954, .T. ) ;
#18588=DIRECTION ( 'NONE',  ( -1.000000000000000000, -2.280301054154495132E-31, 1.664003471950577689E-31 ) ) ;
#18601=CARTESIAN_POINT ( 'NONE',  ( -0.01899468245561315022, -0.07378005917298360861, 0.5147132347679528319 ) ) ;
#18602=ORIENTED_EDGE ( 'NONE', *, *, #9267, .F. ) ;
#18608=CARTESIAN_POINT ( 'NONE',  ( -0.04285534776242663768, 0.07199417564834904859, -0.4895512033229227900 ) ) ;
#18612=CARTESIAN_POINT ( 'NONE',  ( -0.06980746140711623082, -9.793929126999064681E-17, -0.2150000000000000244 ) ) ;
#18620=CARTESIAN_POINT ( 'NONE',  ( 0.03647060353175575476, -0.2291014149038315684, -0.4576769917029361867 ) ) ;
#18628=CARTESIAN_POINT ( 'NONE',  ( -0.05562144613422575351, -0.4316454521248627718, 0.1615915407302010720 ) ) ;
#18638=CARTESIAN_POINT ( 'NONE',  ( -0.02869942827333594668, 0.4519168387192263325, 0.2102852866807454479 ) ) ;
#18645=CARTESIAN_POINT ( 'NONE',  ( -0.04211471441534125892, 0.2686849334112402787, 0.3844466239331203461 ) ) ;
#18659=DIRECTION ( 'NONE',  ( -1.000000000000000000, -2.341930812374887555E-31, 1.664003471950578127E-31 ) ) ;
#18676=DIRECTION ( 'NONE',  ( 0.000000000000000000, -3.330669073875470114E-16, -1.000000000000000000 ) ) ;
#18697=CARTESIAN_POINT ( 'NONE',  ( 0.1399999999999994582, 0.000000000000000000, 0.000000000000000000 ) ) ;
#18705=CARTESIAN_POINT ( 'NONE',  ( -0.01548846960707524721, 0.3880410510314791783, 0.3755318131854940567 ) ) ;
#18714=EDGE_LOOP ( 'NONE', ( #6465, #40569, #13787, #22690 ) ) ;
#18717=ORIENTED_EDGE ( 'NONE', *, *, #11426, .T. ) ;
#18724=EDGE_LOOP ( 'NONE', ( #29688, #10511, #6316 ) ) ;
#18727=ORIENTED_EDGE ( 'NONE', *, *, #687, .F. ) ;
#18737=EDGE_LOOP ( 'NONE', ( #31349, #6815, #36024, #6360, #11599 ) ) ;
#18743=CARTESIAN_POINT ( 'NONE',  ( -0.05281452789367811762, -0.4315450824722529832, 0.1820506770215943593 ) ) ;
#18760=CARTESIAN_POINT ( 'NONE',  ( 0.03875523708677636181, -0.2524014508497919862, 0.4040490413287874394 ) ) ;
#18761=DIRECTION ( 'NONE',  ( 0.000000000000000000, 0.5877852522924655876, -0.8090169943749527803 ) ) ;
#18765=CARTESIAN_POINT ( 'NONE',  ( -0.03303737228521335528, 0.4610015631984548667, 0.2426019986921462146 ) ) ;
#18778=CIRCLE ( 'NONE', #31264, 0.01499999999999996302 ) ;
#18780=EDGE_LOOP ( 'NONE', ( #7209, #41, #39698, #35231 ) ) ;
#18783=EDGE_CURVE ( 'NONE', #17036, #33948, #19931, .T. ) ;
#18784=CARTESIAN_POINT ( 'NONE',  ( 0.05561176441985765662, 0.4316390549698252421, -0.1616802657107470620 ) ) ;
#18795=CARTESIAN_POINT ( 'NONE',  ( -0.05562144613422690537, -0.2542273817772361388, 0.3844451335760749600 ) ) ;
#18801=AXIS2_PLACEMENT_3D ( 'NONE', #38755, #27042, #1169 ) ;
#18812=AXIS2_PLACEMENT_3D ( 'NONE', #6892, #10201, #22769 ) ;
#18817=CARTESIAN_POINT ( 'NONE',  ( 0.06980746140711582837, 0.000000000000000000, 0.000000000000000000 ) ) ;
#18819=CARTESIAN_POINT ( 'NONE',  ( -0.05634115714581361400, -0.005221855766565763196, 0.4588864551388208701 ) ) ;
#18826=CARTESIAN_POINT ( 'NONE',  ( -0.02881329448201249560, -0.06013561456248174564, -0.4945523155237964708 ) ) ;
#18836=CARTESIAN_POINT ( 'NONE',  ( 0.01896968469601798685, 0.4667670904252309572, 0.2292592343991468606 ) ) ;
#18839=CARTESIAN_POINT ( 'NONE',  ( 0.04308611741967822983, -0.2425947520953637970, -0.4306844107907368269 ) ) ;
#18842=AXIS2_PLACEMENT_3D ( 'NONE', #18817, #37114, #27862 ) ;
#18847=CARTESIAN_POINT ( 'NONE',  ( -0.04582713223189537749, -0.4790191777205499157, 0.08746099429787616841 ) ) ;
#18854=CARTESIAN_POINT ( 'NONE',  ( -0.04293317454820686635, 0.3457449726441636506, 0.3536934093827128756 ) ) ;
#18855=CARTESIAN_POINT ( 'NONE',  ( -0.01548846960707524721, 0.000000000000000000, 0.000000000000000000 ) ) ;
#18856=DIRECTION ( 'NONE',  ( 2.526820087036053001E-31, 0.1402348365095093807, -0.9901182710308659152 ) ) ;
#18859=VECTOR ( 'NONE', #17776, 39.37007874015748143 ) ;
#18863=CARTESIAN_POINT ( 'NONE',  ( -0.03301200226531702392, 0.3732424419978498942, 0.3635087277994350496 ) ) ;
#18872=DIRECTION ( 'NONE',  ( 4.930380657631316120E-32, -0.4685245517976818208, -0.8834504764630450868 ) ) ;
#18879=EDGE_LOOP ( 'NONE', ( #16819, #5497, #18602, #37392 ) ) ;
#18883=CARTESIAN_POINT ( 'NONE',  ( 0.01896931156527556159, 0.3622781579086356563, -0.3730773604463906157 ) ) ;
#18886=CARTESIAN_POINT ( 'NONE',  ( -0.01548846960707490547, 0.09061086148575973886, 0.5171215251571029681 ) ) ;
#18887=ORIENTED_EDGE ( 'NONE', *, *, #7947, .T. ) ;
#18892=ORIENTED_EDGE ( 'NONE', *, *, #22153, .F. ) ;
#18898=ORIENTED_EDGE ( 'NONE', *, *, #29100, .F. ) ;
#18911=DIRECTION ( 'NONE',  ( -1.000000000000000000, -2.280301054154495132E-31, 1.664003471950577689E-31 ) ) ;
#18916=ADVANCED_FACE ( 'NONE', ( #9994 ), #5432, .T. ) ;
#18932=CARTESIAN_POINT ( 'NONE',  ( -0.05283710938261064471, -0.4560492058803821691, -0.1064717188025600669 ) ) ;
#18934=CARTESIAN_POINT ( 'NONE',  ( 0.01548846960707524721, 0.2372406987223678043, 0.4850946823762586901 ) ) ;
#18935=ORIENTED_EDGE ( 'NONE', *, *, #29588, .F. ) ;
#18942=DIRECTION ( 'NONE',  ( 0.000000000000000000, 0.8090169943749455639, -0.5877852522924756906 ) ) ;
#18949=CARTESIAN_POINT ( 'NONE',  ( -0.04308449196698675016, -0.4845747790795000287, 0.09763455429601199109 ) ) ;
#18951=DIRECTION ( 'NONE',  ( -0.000000000000000000, 0.8090169943749540016, 0.5877852522924639223 ) ) ;
#18954=AXIS2_PLACEMENT_3D ( 'NONE', #38347, #26225, #19838 ) ;
#18956=DIRECTION ( 'NONE',  ( 1.702140497302372314E-12, -0.5877852522924748024, -0.8090169943749461190 ) ) ;
#18962=EDGE_CURVE ( 'NONE', #26219, #28034, #18991, .T. ) ;
#18965=CARTESIAN_POINT ( 'NONE',  ( -0.05634402396114354672, 0.4396062797411981471, 0.1319984305213857956 ) ) ;
#18984=ORIENTED_EDGE ( 'NONE', *, *, #4969, .F. ) ;
#18991=B_SPLINE_CURVE_WITH_KNOTS ( 'NONE', 3,
 ( #35094, #22776, #29118, #13494, #38765, #10209, #28910, #7286, #32196, #29335, #23169, #22961, #7502, #6898, #32398, #29522, #19863, #7091 ),
 .UNSPECIFIED., .F., .F.,
 ( 4, 2, 2, 2, 2, 2, 2, 2, 4 ),
 ( 0.0003425652276237299478, 0.001007165397454245050, 0.001671765567284760152, 0.002336365737115275037, 0.003000965906945790573, 0.003665566076776305242, 0.004330166246606820778, 0.004994766416437335446, 0.005659366586267850982 ),
 .UNSPECIFIED. ) ;
#19003=AXIS2_PLACEMENT_3D ( 'NONE', #8305, #26839, #27030 ) ;
#19006=EDGE_CURVE ( 'NONE', #13940, #17702, #40027, .T. ) ;
#19011=ADVANCED_FACE ( 'NONE', ( #39387 ), #36515, .T. ) ;
#19012=CARTESIAN_POINT ( 'NONE',  ( -0.05544444631433745330, 0.02030017825816688229, 0.4608552147122319531 ) ) ;
#19029=CARTESIAN_POINT ( 'NONE',  ( 0.05078310099560445767, -0.2374900923169175615, -0.4099167927582010873 ) ) ;
#19046=CARTESIAN_POINT ( 'NONE',  ( -0.03174036153404918847, 0.3664551212196169860, -0.3753291932915809315 ) ) ;
#19060=CARTESIAN_POINT ( 'NONE',  ( 0.02869942827333533952, 0.2420058122830180403, -0.4357544236535293991 ) ) ;
#19063=EDGE_LOOP ( 'NONE', ( #27625, #4627, #36478, #20197 ) ) ;
#19065=DIRECTION ( 'NONE',  ( 5.264498737790503632E-15, -0.8834504764630464191, 0.4685245517976792673 ) ) ;
#19066=CARTESIAN_POINT ( 'NONE',  ( 0.1499999999999994948, -0.4730347584886754331, 0.2341461249029889169 ) ) ;
#19069=ORIENTED_EDGE ( 'NONE', *, *, #32113, .T. ) ;
#19073=EDGE_CURVE ( 'NONE', #20917, #17096, #30717, .T. ) ;
#19074=CARTESIAN_POINT ( 'NONE',  ( 0.05634206451479451677, 0.2613530514269510330, -0.3773282889206430180 ) ) ;
#19080=EDGE_CURVE ( 'NONE', #11876, #20992, #1548, .T. ) ;
#19092=ORIENTED_EDGE ( 'NONE', *, *, #5434, .T. ) ;
#19097=SPHERICAL_SURFACE ( 'NONE', #37076, 0.01499999999999999944 ) ;
#19098=DIRECTION ( 'NONE',  ( 0.000000000000000000, -2.986499936241660365E-14, 1.000000000000000000 ) ) ;
#19099=CIRCLE ( 'NONE', #29599, 0.01500000000000005669 ) ;
#19103=DIRECTION ( 'NONE',  ( 1.000000000000000000, 2.325617669281439721E-12, 1.136734431350428609E-12 ) ) ;
#19113=DIRECTION ( 'NONE',  ( -1.416619696839553052E-11, -0.9510565162951529761, 0.3090169943749491166 ) ) ;
#19146=SPHERICAL_SURFACE ( 'NONE', #13889, 0.01499999999999999944 ) ;
#19148=CARTESIAN_POINT ( 'NONE',  ( -0.03158843595483506322, -0.05459869295505906384, -0.4890616322892848977 ) ) ;
#19156=CIRCLE ( 'NONE', #30294, 0.01500000000000001159 ) ;
#19166=CARTESIAN_POINT ( 'NONE',  ( -0.05634206451479800704, 0.4332270636364471406, 0.1516455289248359872 ) ) ;
#19212=DIRECTION ( 'NONE',  ( -1.000000000000000000, -2.280301054154495132E-31, 1.664003471950577689E-31 ) ) ;
#19213=CARTESIAN_POINT ( 'NONE',  ( -0.03171102739523346675, 0.05432883045314864517, 0.4888204606144165854 ) ) ;
#19216=DIRECTION ( 'NONE',  ( -1.355854680848614260E-31, 3.330669073875470114E-16, 1.000000000000000000 ) ) ;
#19219=ORIENTED_EDGE ( 'NONE', *, *, #5886, .T. ) ;
#19223=ORIENTED_EDGE ( 'NONE', *, *, #27507, .F. ) ;
#19224=DIRECTION ( 'NONE',  ( -1.000000000000000000, -2.280301054154495132E-31, 1.664003471950577689E-31 ) ) ;
#19226=ORIENTED_EDGE ( 'NONE', *, *, #8005, .T. ) ;
#19231=CARTESIAN_POINT ( 'NONE',  ( 0.04946288932100069424, -0.3082365379450882070, -0.3644333945507132189 ) ) ;
#19237=EDGE_LOOP ( 'NONE', ( #27124, #18317, #37852, #18717, #37123, #40489, #25054, #16001, #34150, #25884, #30015, #32133, #30369, #2679 ) ) ;
#19238=ADVANCED_FACE ( 'NONE', ( #16289 ), #16117, .T. ) ;
#19251=EDGE_CURVE ( 'NONE', #6931, #4571, #35673, .T. ) ;
#19253=CARTESIAN_POINT ( 'NONE',  ( -0.05083665881509068230, 0.3162195626322023556, 0.3525671453250067700 ) ) ;
#19254=AXIS2_PLACEMENT_3D ( 'NONE', #34866, #13074, #12654 ) ;
#19255=CARTESIAN_POINT ( 'NONE',  ( -0.03672309138969640646, -0.4430277080971899983, -0.1868557463394342477 ) ) ;
#19268=CARTESIAN_POINT ( 'NONE',  ( 0.03868264068766660846, 0.03360988006412097412, 0.4753775160315155124 ) ) ;
#19273=CARTESIAN_POINT ( 'NONE',  ( 0.01548846960712797240, -0.07651041855115535417, -0.5222379212567069828 ) ) ;
#19277=VERTEX_POINT ( 'NONE', #10500 ) ;
#19286=ORIENTED_EDGE ( 'NONE', *, *, #24589, .F. ) ;
#19296=ADVANCED_FACE ( 'NONE', ( #10321 ), #26490, .T. ) ;
#19304=CIRCLE ( 'NONE', #11417, 0.01499999999999995434 ) ;
#19307=ADVANCED_FACE ( 'NONE', ( #13783 ), #13389, .T. ) ;
#19316=DIRECTION ( 'NONE',  ( -0.9378410757839559242, 0.1072489841977647268, -0.3300784330442382841 ) ) ;
#19322=CARTESIAN_POINT ( 'NONE',  ( 0.02953079040095728247, 0.000000000000000000, 0.000000000000000000 ) ) ;
#19335=DIRECTION ( 'NONE',  ( 1.000000000000000000, -1.213308482346468028E-12, -2.286601241528066538E-12 ) ) ;
#19336=EDGE_LOOP ( 'NONE', ( #18123, #8398, #14713 ) ) ;
#19337=CARTESIAN_POINT ( 'NONE',  ( -0.04230188431063477972, -0.008729788072060947965, 0.4686063437799720677 ) ) ;
#19343=EDGE_LOOP ( 'NONE', ( #25613, #16197, #9203, #33521 ) ) ;
#19354=ORIENTED_EDGE ( 'NONE', *, *, #20114, .F. ) ;
#19359=CARTESIAN_POINT ( 'NONE',  ( -0.01548846960712824648, 0.07651041855115098267, -0.5222379212567075379 ) ) ;
#19374=CARTESIAN_POINT ( 'NONE',  ( 0.04308611741967745268, -0.3346393142056199310, 0.3638101219460039282 ) ) ;
#19380=CARTESIAN_POINT ( 'NONE',  ( -0.04285640132273837999, 0.4433417433457839119, 0.2197472875419949068 ) ) ;
#19382=ORIENTED_EDGE ( 'NONE', *, *, #9377, .T. ) ;
#19385=FACE_OUTER_BOUND ( 'NONE', #3318, .T. ) ;
#19390=VERTEX_POINT ( 'NONE', #17677 ) ;
#19397=CYLINDRICAL_SURFACE ( 'NONE', #23930, 0.1749999999999999889 ) ;
#19409=DIRECTION ( 'NONE',  ( -1.000000000000000000, -2.280301054154495132E-31, 1.664003471950577689E-31 ) ) ;
#19426=CARTESIAN_POINT ( 'NONE',  ( -0.03159140494780127151, 0.4819881711443534389, -0.09921162977303643604 ) ) ;
#19436=ORIENTED_EDGE ( 'NONE', *, *, #39902, .F. ) ;
#19443=CARTESIAN_POINT ( 'NONE',  ( 0.05076679145662187087, -0.3165345149637547872, -0.3525336044145329084 ) ) ;
#19451=DIRECTION ( 'NONE',  ( 1.000000000000000000, 2.280301054154495132E-31, -1.664003471950577689E-31 ) ) ;
#19460=CARTESIAN_POINT ( 'NONE',  ( -0.01899468245561687987, 0.3622301702732946826, -0.3730449234618297694 ) ) ;
#19461=CARTESIAN_POINT ( 'NONE',  ( -0.02881302694829757094, -0.4517620879735247397, -0.2100235834770130539 ) ) ;
#19468=CARTESIAN_POINT ( 'NONE',  ( 0.04762035657659004911, 0.4700462218748536758, -0.1075639008183982559 ) ) ;
#19471=DIRECTION ( 'NONE',  ( -1.664003471950577032E-31, -3.330669073875470607E-16, -1.000000000000000000 ) ) ;
#19477=DIRECTION ( 'NONE',  ( -1.000000000000000000, -2.341930812374887555E-31, 1.664003471950578127E-31 ) ) ;
#19510=FACE_OUTER_BOUND ( 'NONE', #18737, .T. ) ;
#19515=DIRECTION ( 'NONE',  ( 0.000000000000000000, -0.8090169943749496717, -0.5877852522924700285 ) ) ;
#19520=DIRECTION ( 'NONE',  ( 1.000000000000000000, 0.000000000000000000, 0.000000000000000000 ) ) ;
#19539=CARTESIAN_POINT ( 'NONE',  ( 0.05562144613422616291, -0.2542273817772364719, -0.3844451335760745159 ) ) ;
#19549=ORIENTED_EDGE ( 'NONE', *, *, #38323, .F. ) ;
#19559=EDGE_LOOP ( 'NONE', ( #11609, #18216 ) ) ;
#19562=CARTESIAN_POINT ( 'NONE',  ( -0.04229956186878645191, -0.008769846780144991555, -0.4686106502047107658 ) ) ;
#19563=DIRECTION ( 'NONE',  ( -2.563099466555616810E-12, -0.9510565162951545304, -0.3090169943749443426 ) ) ;
#19566=CARTESIAN_POINT ( 'NONE',  ( 0.01548846960707528191, 0.3772621329472758411, 0.3651003739303370632 ) ) ;
#19578=CARTESIAN_POINT ( 'NONE',  ( -0.01896931156526107318, 0.5123785568735040874, 0.08888416637130031051 ) ) ;
#19585=B_SPLINE_CURVE_WITH_KNOTS ( 'NONE', 3,
 ( #17891, #9057, #2487, #11930, #12145, #2288, #24710, #21619, #8848, #34143, #24906, #5951, #18512, #31065, #37430, #21818, #34347, #15638 ),
 .UNSPECIFIED., .F., .F.,
 ( 4, 2, 2, 2, 2, 2, 2, 2, 4 ),
 ( 0.0003425652276237246894, 0.001007165397454238762, 0.001671765567284752996, 0.002336365737115266798, 0.003000965906945781032, 0.003665566076776295267, 0.004330166246606809502, 0.004994766416437324170, 0.005659366586267837972 ),
 .UNSPECIFIED. ) ;
#19588=ORIENTED_EDGE ( 'NONE', *, *, #8723, .T. ) ;
#19592=ORIENTED_EDGE ( 'NONE', *, *, #11050, .F. ) ;
#19596=EDGE_CURVE ( 'NONE', #39882, #16145, #12037, .T. ) ;
#19608=CARTESIAN_POINT ( 'NONE',  ( -0.05083674528492039546, 0.04859289555129508303, 0.4711018118971380120 ) ) ;
#19620=EDGE_CURVE ( 'NONE', #1885, #4225, #29807, .T. ) ;
#19651=CARTESIAN_POINT ( 'NONE',  ( -0.05615703521555169553, 0.2783003116137218180, -0.3655156233916866948 ) ) ;
#19657=CARTESIAN_POINT ( 'NONE',  ( 0.05279905671745396128, 0.4561941007107730428, -0.1063003320160303133 ) ) ;
#19674=CARTESIAN_POINT ( 'NONE',  ( 0.02953079040095687308, 0.09152108205202803826, 0.5223162075576412988 ) ) ;
#19734=FACE_OUTER_BOUND ( 'NONE', #25086, .T. ) ;
#19755=CARTESIAN_POINT ( 'NONE',  ( 0.04946426091936632213, -0.3082279967728515091, 0.3644356914998804764 ) ) ;
#19765=DIRECTION ( 'NONE',  ( -1.000000000000000000, -2.341930812374887555E-31, 1.664003471950578127E-31 ) ) ;
#19769=DIRECTION ( 'NONE',  ( -1.000000000000000000, -2.280301054154495132E-31, 1.664003471950577689E-31 ) ) ;
#19770=ORIENTED_EDGE ( 'NONE', *, *, #36298, .T. ) ;
#19771=ORIENTED_EDGE ( 'NONE', *, *, #25559, .T. ) ;
#19775=VERTEX_POINT ( 'NONE', #32856 ) ;
#19791=CYLINDRICAL_SURFACE ( 'NONE', #29149, 0.01500000000000004802 ) ;
#19797=CARTESIAN_POINT ( 'NONE',  ( -0.8248651029816859159, -5.463695987328526437E-16, 0.000000000000000000 ) ) ;
#19800=( NAMED_UNIT ( * ) SI_UNIT ( $, .STERADIAN. ) SOLID_ANGLE_UNIT ( ) );
#19814=( BOUNDED_SURFACE ( )  B_SPLINE_SURFACE ( 3, 2, ( 
 ( #11364, #30702, #21245 ),
 ( #21035, #39530, #30895 ),
 ( #27613, #11581, #5589 ),
 ( #2323, #24328, #40142 ),
 ( #27817, #20639, #23934 ),
 ( #27214, #1919, #24144 ),
 ( #2522, #18347, #14865 ),
 ( #21461, #17933, #24535 ),
 ( #30278, #14644, #2107 ),
 ( #12185, #8279, #20848 ),
 ( #27425, #33556, #14437 ),
 ( #40352, #5790, #24744 ),
 ( #36853, #30091, #30493 ),
 ( #33371, #18148, #5370 ),
 ( #8666, #11970, #33176 ),
 ( #4980, #5175, #37067 ),
 ( #27002, #8474, #39950 ),
 ( #2714, #11768, #17727 ) ),
 .UNSPECIFIED., .F., .F., .F. ) 
 B_SPLINE_SURFACE_WITH_KNOTS ( ( 4, 2, 2, 2, 2, 2, 2, 2, 4 ),
 ( 3, 3 ),
 ( -0.001532620576208852279, -0.0007637936630077648160, 5.033250193322538930E-06, 0.0007738601633944098938, 0.001542687076595497357, 0.002311513989796584820, 0.003080340902997672284, 0.003849167816198759747, 0.004617994729399847210 ),
 ( 0.000000000000000000, 1.000000000000000000 ),
 .UNSPECIFIED. ) 
 GEOMETRIC_REPRESENTATION_ITEM ( )  RATIONAL_B_SPLINE_SURFACE ( (
 ( 1.000000000000000000, 0.7283825911960450927, 1.000000000000000000),
 ( 1.000000000000000000, 0.7404385082114955940, 1.000000000000000000),
 ( 1.000000000000000000, 0.7521504257737200438, 1.000000000000000000),
 ( 1.000000000000000000, 0.7744497410762684053, 1.000000000000000000),
 ( 1.000000000000000000, 0.7845654757373705657, 1.000000000000000000),
 ( 1.000000000000000000, 0.8022083990892434624, 1.000000000000000000),
 ( 1.000000000000000000, 0.8094167424699041380, 1.000000000000000000),
 ( 1.000000000000000000, 0.8194491993616890291, 1.000000000000000000),
 ( 1.000000000000000000, 0.8220634900780797727, 1.000000000000000000),
 ( 1.000000000000000000, 0.8220705070823152161, 1.000000000000000000),
 ( 1.000000000000000000, 0.8194468812479983599, 1.000000000000000000),
 ( 1.000000000000000000, 0.8094220769840453356, 1.000000000000000000),
 ( 1.000000000000000000, 0.8022659121985590280, 1.000000000000000000),
 ( 1.000000000000000000, 0.7845681159035412522, 1.000000000000000000),
 ( 1.000000000000000000, 0.7744426415186608237, 1.000000000000000000),
 ( 1.000000000000000000, 0.7522890290927356505, 1.000000000000000000),
 ( 1.000000000000000000, 0.7403540167216396961, 1.000000000000000000),
 ( 1.000000000000000000, 0.7283825911960196686, 1.000000000000000000) ) ) 
 REPRESENTATION_ITEM ( '' )  SURFACE ( )  );
#19819=CIRCLE ( 'NONE', #15890, 0.5400000000000015898 ) ;
#19826=DIRECTION ( 'NONE',  ( -3.543711097672501380E-32, -0.8983234858819668656, -0.4393346272636287630 ) ) ;
#19827=EDGE_LOOP ( 'NONE', ( #30606, #21386, #32767, #19092 ) ) ;
#19828=CARTESIAN_POINT ( 'NONE',  ( 0.03309058451312588828, -0.08822157290689926212, -0.5132714794726492835 ) ) ;
#19829=DIRECTION ( 'NONE',  ( 0.000000000000000000, -0.3090169943749502823, -0.9510565162951527540 ) ) ;
#19838=DIRECTION ( 'NONE',  ( 0.000000000000000000, 0.9510565162951547524, 0.3090169943749436210 ) ) ;
#19852=CARTESIAN_POINT ( 'NONE',  ( -0.05138886601528081660, -0.4553812863296833879, -0.1245405308888577478 ) ) ;
#19859=CARTESIAN_POINT ( 'NONE',  ( 0.03478489236951045477, 0.5086709597375891345, -0.08927530733453492573 ) ) ;
#19863=CARTESIAN_POINT ( 'NONE',  ( 0.01895884884825177821, -0.2428741539084897094, 0.4598572020609204558 ) ) ;
#19868=CIRCLE ( 'NONE', #27771, 0.01500000000000006016 ) ;
#19870=CARTESIAN_POINT ( 'NONE',  ( -0.05634304521267748805, 1.092739197465705287E-15, 0.4588823192046724841 ) ) ;
#19873=CARTESIAN_POINT ( 'NONE',  ( -0.02869712619511965296, -0.3396447909410095223, -0.3648221446286677438 ) ) ;
#19881=CARTESIAN_POINT ( 'NONE',  ( 0.1499999999999993561, 0.09319974324248773978, -0.5318964258758787089 ) ) ;
#19898=CARTESIAN_POINT ( 'NONE',  ( 0.03301162916267580405, -0.5156255563253935303, 0.07469829950278324138 ) ) ;
#19905=CIRCLE ( 'NONE', #12006, 0.01500000000000007057 ) ;
#19908=DIRECTION ( 'NONE',  ( 2.532366176626896502E-12, 0.8090169943749470072, -0.5877852522924736922 ) ) ;
#19909=CARTESIAN_POINT ( 'NONE',  ( 0.02869712619511872662, -0.2420104654861707505, -0.4357576342647261902 ) ) ;
#19915=AXIS2_PLACEMENT_3D ( 'NONE', #25076, #22619, #19113 ) ;
#19922=CARTESIAN_POINT ( 'NONE',  ( -0.03672309138969926529, -0.3146134659443306503, 0.3636027875696402623 ) ) ;
#19926=ORIENTED_EDGE ( 'NONE', *, *, #3960, .T. ) ;
#19931=B_SPLINE_CURVE_WITH_KNOTS ( 'NONE', 3,
 ( #33267, #11066, #20939, #36957, #8775, #17636, #33891, #30183, #15361, #6489, #15573, #22359, #21739, #31210, #19060, #392, #30989, #34274 ),
 .UNSPECIFIED., .F., .F.,
 ( 4, 2, 2, 2, 2, 2, 2, 2, 4 ),
 ( 0.0003425652276237174795, 0.001007165397454229221, 0.001671765567284740853, 0.002336365737115257257, 0.003000965906945773660, 0.003665566076776290063, 0.004330166246606806033, 0.004994766416437322436, 0.005659366586267838839 ),
 .UNSPECIFIED. ) ;
#19935=CARTESIAN_POINT ( 'NONE',  ( 0.1499999999999994948, 0.4770632572900484480, 0.2530032579707400253 ) ) ;
#19939=AXIS2_PLACEMENT_3D ( 'NONE', #5408, #9112, #36500 ) ;
#19942=CARTESIAN_POINT ( 'NONE',  ( -0.03868649100028177801, -0.2522293598345298204, 0.4043344736883388024 ) ) ;
#19948=AXIS2_PLACEMENT_3D ( 'NONE', #36955, #11470, #21553 ) ;
#19949=LINE ( 'NONE', #269, #33791 ) ;
#20009=CARTESIAN_POINT ( 'NONE',  ( 0.1499999999999996336, -0.2306506793134066036, 0.4716198300880325434 ) ) ;
#20015=CYLINDRICAL_SURFACE ( 'NONE', #14686, 0.01500000000000004108 ) ;
#20016=AXIS2_PLACEMENT_3D ( 'NONE', #17924, #8463, #2707 ) ;
#20024=B_SPLINE_CURVE_WITH_KNOTS ( 'NONE', 3,
 ( #38300, #22707, #35238, #7039, #19608, #38711, #3944, #16506, #10531, #16919 ),
 .UNSPECIFIED., .F., .F.,
 ( 4, 2, 2, 2, 4 ),
 ( 0.003098629625065144923, 0.003873295706325716355, 0.004647961787586288654, 0.005422627868846860086, 0.006197293950107432385 ),
 .UNSPECIFIED. ) ;
#20027=CARTESIAN_POINT ( 'NONE',  ( -0.01895884884825282252, 0.5124024296374540821, -0.08888335629180008080 ) ) ;
#20030=CIRCLE ( 'NONE', #1009, 0.5400000000000001465 ) ;
#20035=ADVANCED_FACE ( 'NONE', ( #27454 ), #21071, .T. ) ;
#20048=CARTESIAN_POINT ( 'NONE',  ( -0.02881302694829541641, 0.4889319715862935900, -0.09562644460326163998 ) ) ;
#20069=CARTESIAN_POINT ( 'NONE',  ( -0.02872242845530506572, -0.5252126300208028731, -0.08844866507293215607 ) ) ;
#20077=CARTESIAN_POINT ( 'NONE',  ( 0.05201840200954787469, 0.4415345355162785257, -0.1624690192511295816 ) ) ;
#20082=FACE_OUTER_BOUND ( 'NONE', #28396, .T. ) ;
#20084=CARTESIAN_POINT ( 'NONE',  ( 0.1499999999999994948, 0.1249999999999999029, 0.000000000000000000 ) ) ;
#20086=CARTESIAN_POINT ( 'NONE',  ( -0.05082294681499043010, 0.04864283519431752273, -0.4711332289091950121 ) ) ;
#20090=CIRCLE ( 'NONE', #12182, 0.01499999999999995434 ) ;
#20094=CARTESIAN_POINT ( 'NONE',  ( -0.04229956186878668090, -0.2825373843407160690, -0.3739591931584715367 ) ) ;
#20112=ORIENTED_EDGE ( 'NONE', *, *, #38689, .F. ) ;
#20114=EDGE_CURVE ( 'NONE', #5909, #1137, #14428, .T. ) ;
#20119=CARTESIAN_POINT ( 'NONE',  ( 0.04760578872587564042, -0.4435171289962518970, 0.1893230556938431397 ) ) ;
#20128=FACE_OUTER_BOUND ( 'NONE', #26688, .T. ) ;
#20132=CARTESIAN_POINT ( 'NONE',  ( 0.02881195911414505262, 0.2420394953216123413, 0.4354516087588692352 ) ) ;
#20141=EDGE_CURVE ( 'NONE', #37512, #26023, #27202, .T. ) ;
#20143=CARTESIAN_POINT ( 'NONE',  ( -0.05634115714581377360, -0.2739512608647004521, 0.3681776108865941755 ) ) ;
#20147=ORIENTED_EDGE ( 'NONE', *, *, #14559, .T. ) ;
#20151=CARTESIAN_POINT ( 'NONE',  ( -0.04293317454820699819, 0.4876093284570324204, 0.08292018301452676321 ) ) ;
#20152=ORIENTED_EDGE ( 'NONE', *, *, #33815, .F. ) ;
#20158=ORIENTED_EDGE ( 'NONE', *, *, #34273, .F. ) ;
#20169=CARTESIAN_POINT ( 'NONE',  ( 0.02869712619511921928, 0.4519224903895674994, 0.2102851490355753250 ) ) ;
#20174=DIRECTION ( 'NONE',  ( 0.000000000000000000, 0.3090169943749439541, -0.9510565162951547524 ) ) ;
#20186=CARTESIAN_POINT ( 'NONE',  ( 0.04154009738085454734, -0.01731731106881185395, -0.4700109389422704731 ) ) ;
#20189=( BOUNDED_SURFACE ( )  B_SPLINE_SURFACE ( 3, 2, ( 
 ( #31581, #13272, #10389 ),
 ( #25437, #28293, #9582 ),
 ( #34673, #9777, #6480 ),
 ( #19461, #31995, #37969 ),
 ( #22349, #22764, #6678 ),
 ( #19255, #31796, #3613 ),
 ( #3807, #27039, #10581 ),
 ( #4592, #17162, #32383 ),
 ( #7702, #39570, #11403 ),
 ( #13670, #32598, #10800 ),
 ( #4411, #26658, #23971 ),
 ( #29714, #23760, #36502 ),
 ( #29932, #4800, #1774 ),
 ( #36087, #23157, #20676 ),
 ( #1558, #19852, #11013 ),
 ( #33212, #29323, #4208 ),
 ( #23569, #16774, #1168 ),
 ( #7486, #39187, #14284 ),
 ( #7889, #14078, #30126 ),
 ( #17584, #26233, #5017 ),
 ( #20461, #32993, #35688 ),
 ( #38754, #20069, #17374 ) ),
 .UNSPECIFIED., .F., .F., .T. ) 
 B_SPLINE_SURFACE_WITH_KNOTS ( ( 4, 2, 2, 2, 2, 2, 2, 2, 2, 2, 4 ),
 ( 3, 3 ),
 ( 0.002013519961495848724, 0.002780892266055755638, 0.003548264570615662986, 0.004315636875175570333, 0.004699323027455524007, 0.005083009179735476814, 0.005466695332015429620, 0.005850381484295383294, 0.006617753788855290642, 0.007385126093415197990, 0.008152498397975105338 ),
 ( 0.000000000000000000, 1.000000000000000000 ),
 .UNSPECIFIED. ) 
 GEOMETRIC_REPRESENTATION_ITEM ( )  RATIONAL_B_SPLINE_SURFACE ( (
 ( 1.000000000000000000, 0.7283825911960385424, 1.000000000000000000),
 ( 1.000000000000000000, 0.7404375345929280483, 1.000000000000000000),
 ( 1.000000000000000000, 0.7521483142432979774, 1.000000000000000000),
 ( 1.000000000000000000, 0.7744460733779491290, 1.000000000000000000),
 ( 1.000000000000000000, 0.7845612039384242120, 1.000000000000000000),
 ( 1.000000000000000000, 0.8022035258259876400, 1.000000000000000000),
 ( 1.000000000000000000, 0.8093965293318987619, 1.000000000000000000),
 ( 1.000000000000000000, 0.8169028692726829632, 1.000000000000000000),
 ( 1.000000000000000000, 0.8188329634863246165, 1.000000000000000000),
 ( 1.000000000000000000, 0.8214004505364141950, 1.000000000000000000),
 ( 1.000000000000000000, 0.8220602406260524297, 1.000000000000000000),
 ( 1.000000000000000000, 0.8220736605436118616, 1.000000000000000000),
 ( 1.000000000000000000, 0.8214126668415132615, 1.000000000000000000),
 ( 1.000000000000000000, 0.8188520474558848017, 1.000000000000000000),
 ( 1.000000000000000000, 0.8169545908333680773, 1.000000000000000000),
 ( 1.000000000000000000, 0.8094771004221105182, 1.000000000000000000),
 ( 1.000000000000000000, 0.8022723753809029024, 1.000000000000000000),
 ( 1.000000000000000000, 0.7845733350635966108, 1.000000000000000000),
 ( 1.000000000000000000, 0.7744472902495156408, 1.000000000000000000),
 ( 1.000000000000000000, 0.7522916829161578889, 1.000000000000000000),
 ( 1.000000000000000000, 0.7403553004667213777, 1.000000000000000000),
 ( 1.000000000000000000, 0.7283825911960410959, 1.000000000000000000) ) ) 
 REPRESENTATION_ITEM ( '' )  SURFACE ( )  );
#20197=ORIENTED_EDGE ( 'NONE', *, *, #7273, .F. ) ;
#20199=ORIENTED_EDGE ( 'NONE', *, *, #18352, .F. ) ;
#20201=CARTESIAN_POINT ( 'NONE',  ( 0.04285561529640833506, 0.4433460678679726485, 0.2197428102802088945 ) ) ;
#20207=EDGE_LOOP ( 'NONE', ( #36735, #20158, #19223 ) ) ;
#20239=DIRECTION ( 'NONE',  ( 1.000000000000000000, 0.000000000000000000, 0.000000000000000000 ) ) ;
#20243=EDGE_LOOP ( 'NONE', ( #705, #34178, #15923, #8895 ) ) ;
#20253=CARTESIAN_POINT ( 'NONE',  ( -0.05616044724337389965, 0.4336395721329084907, -0.1516614036261209608 ) ) ;
#20260=DIRECTION ( 'NONE',  ( 0.000000000000000000, 0.8834504764629500517, 0.4685245517978610108 ) ) ;
#20267=CARTESIAN_POINT ( 'NONE',  ( -0.01896968469603060869, 0.2428673116372761231, -0.4598334287537079179 ) ) ;
#20268=EDGE_CURVE ( 'NONE', #2590, #20994, #13385, .T. ) ;
#20281=CARTESIAN_POINT ( 'NONE',  ( -0.05269191099235946696, -0.2790572191958481385, -0.3764802596566364512 ) ) ;
#20285=CARTESIAN_POINT ( 'NONE',  ( -0.03650577977170588184, 0.08362514765351788948, -0.5048437183011776908 ) ) ;
#20291=CARTESIAN_POINT ( 'NONE',  ( 0.04582713223189485013, 0.3361263728083095370, 0.3523178389613185746 ) ) ;
#20294=DIRECTION ( 'NONE',  ( 0.9378410757839552581, -0.1072489841977715685, -0.3300784330442382841 ) ) ;
#20312=CARTESIAN_POINT ( 'NONE',  ( 0.05076679145662038595, -0.4330939261214921121, 0.1921033382362652697 ) ) ;
#20313=ADVANCED_FACE ( 'NONE', ( #18509 ), #3093, .T. ) ;
#20320=CARTESIAN_POINT ( 'NONE',  ( 0.05083674528491973627, -0.04859289555129253646, 0.4711018118971379010 ) ) ;
#20325=B_SPLINE_CURVE_WITH_KNOTS ( 'NONE', 3,
 ( #40532, #15838, #34755, #472, #21431, #4302, #10074, #28798, #32476, #38655, #35776, #32084, #17056, #10293, #4086, #23250, #13957, #29409 ),
 .UNSPECIFIED., .F., .F.,
 ( 4, 2, 2, 2, 2, 2, 2, 2, 4 ),
 ( -0.002633528389679827900, -0.001975271857855798781, -0.001317015326031769880, -0.0006587587942077409789, -5.022623837118607437E-07, 0.0006577542694403172574, 0.001316010801264345942, 0.001974267333088375494, 0.002632523864912404178 ),
 .UNSPECIFIED. ) ;
#20336=DIRECTION ( 'NONE',  ( -2.682900528199988315E-31, 0.9510565162951527540, -0.3090169943749503378 ) ) ;
#20337=CARTESIAN_POINT ( 'NONE',  ( -0.03642997641689297433, -0.3645929376994312965, 0.3593586258117719145 ) ) ;
#20340=VERTEX_POINT ( 'NONE', #18934 ) ;
#20351=CARTESIAN_POINT ( 'NONE',  ( 0.02953079040095687308, 0.5250338024619264354, -0.07436286310882528339 ) ) ;
#20352=ORIENTED_EDGE ( 'NONE', *, *, #12927, .T. ) ;
#20365=EDGE_CURVE ( 'NONE', #17036, #37027, #15355, .T. ) ;
#20370=DIRECTION ( 'NONE',  ( 1.000000000000000000, 2.341930812374887555E-31, -1.664003471950578127E-31 ) ) ;
#20377=CARTESIAN_POINT ( 'NONE',  ( 0.1499999999999994948, 0.3688619771572980710, 0.3775276577326925898 ) ) ;
#20379=DIRECTION ( 'NONE',  ( 0.000000000000000000, -0.9510565162951634122, -0.3090169943749168646 ) ) ;
#20381=DIRECTION ( 'NONE',  ( -0.3468893892380660038, -0.7770416411310684390, -0.5252371270030113948 ) ) ;
#20382=ORIENTED_EDGE ( 'NONE', *, *, #1175, .T. ) ;
#20386=VERTEX_POINT ( 'NONE', #7354 ) ;
#20390=VERTEX_POINT ( 'NONE', #28593 ) ;
#20395=CARTESIAN_POINT ( 'NONE',  ( -0.03868649100028175719, -0.4624880946332493026, -0.1149381524902386292 ) ) ;
#20409=CIRCLE ( 'NONE', #36132, 0.1749999999999999889 ) ;
#20418=CARTESIAN_POINT ( 'NONE',  ( -0.02953079040095693900, -0.4684706630666107263, -0.2484463060367401721 ) ) ;
#20428=AXIS2_PLACEMENT_3D ( 'NONE', #30952, #24384, #30755 ) ;
#20441=CARTESIAN_POINT ( 'NONE',  ( 0.02953079040095687308, -0.3810518745593889922, -0.3687679460475752902 ) ) ;
#20443=CARTESIAN_POINT ( 'NONE',  ( -0.04947837552028831049, 0.4418396724781329943, -0.1804413675088953339 ) ) ;
#20459=ADVANCED_FACE ( 'NONE', ( #9854 ), #35368, .T. ) ;
#20461=CARTESIAN_POINT ( 'NONE',  ( -0.01896968469603809576, -0.5123777055006339953, -0.08888419526111762670 ) ) ;
#20463=AXIS2_PLACEMENT_3D ( 'NONE', #15610, #9631, #6937 ) ;
#20473=CARTESIAN_POINT ( 'NONE',  ( -0.03654368633476851730, -0.08356155710620498389, -0.5047517311408978857 ) ) ;
#20474=CARTESIAN_POINT ( 'NONE',  ( -0.03174036153404024424, -0.2437184149031433322, -0.4645026301777863686 ) ) ;
#20478=CARTESIAN_POINT ( 'NONE',  ( -0.1399999999999997358, 8.414405049830459540E-17, 0.2526340763130724976 ) ) ;
#20484=CARTESIAN_POINT ( 'NONE',  ( -0.03158843595483518119, 0.3316344853930314196, 0.3635668653053512056 ) ) ;
#20485=FACE_OUTER_BOUND ( 'NONE', #27474, .T. ) ;
#20486=CARTESIAN_POINT ( 'NONE',  ( 0.02872242845530443775, -0.5252126300208032061, -0.08844866507293194791 ) ) ;
#20492=DIRECTION ( 'NONE',  ( 1.000000000000000000, 2.280301054154495132E-31, -1.664003471950577689E-31 ) ) ;
#20498=EDGE_LOOP ( 'NONE', ( #11039, #131, #28850, #40363 ) ) ;
#20506=ORIENTED_EDGE ( 'NONE', *, *, #31392, .F. ) ;
#20507=AXIS2_PLACEMENT_3D ( 'NONE', #36524, #5430, #1792 ) ;
#20512=CARTESIAN_POINT ( 'NONE',  ( 0.04285427992853797080, -0.4878399728613565522, 0.08281491827192886956 ) ) ;
#20513=ADVANCED_FACE ( 'NONE', ( #25705 ), #13139, .F. ) ;
#20518=CARTESIAN_POINT ( 'NONE',  ( 0.03654368633476876016, -0.08356155710620387367, 0.5047517311408953322 ) ) ;
#20521=CARTESIAN_POINT ( 'NONE',  ( 0.03662792686184355301, -0.3149733899719675545, -0.3635662525351508467 ) ) ;
#20524=CARTESIAN_POINT ( 'NONE',  ( 0.03170874437002998286, 0.3312776501328030809, 0.3635338427919215798 ) ) ;
#20528=CIRCLE ( 'NONE', #25795, 0.01500000000000006016 ) ;
#20535=CARTESIAN_POINT ( 'NONE',  ( -0.05252049209742361280, -0.2830365943384500205, 0.3740706778132465993 ) ) ;
#20541=CARTESIAN_POINT ( 'NONE',  ( 0.1499999999999993561, -2.632527843410151989E-17, -0.1250000000000000000 ) ) ;
#20544=DIRECTION ( 'NONE',  ( -1.000000000000000000, -2.280301054154495132E-31, 1.664003471950577689E-31 ) ) ;
#20547=CARTESIAN_POINT ( 'NONE',  ( 0.05634304521267755744, 1.092739197465705287E-15, 0.4588823192046724841 ) ) ;
#20566=AXIS2_PLACEMENT_3D ( 'NONE', #29233, #17080, #22883 ) ;
#20571=CARTESIAN_POINT ( 'NONE',  ( 0.01548846960707524721, -0.3772621329472692908, -0.3651003739303438911 ) ) ;
#20578=DIRECTION ( 'NONE',  ( -1.000000000000000000, -2.280301054154495132E-31, 1.664003471950577689E-31 ) ) ;
#20581=CARTESIAN_POINT ( 'NONE',  ( 0.02235124290213141851, -0.5044963136724011088, 0.09030809412321962049 ) ) ;
#20586=CARTESIAN_POINT ( 'NONE',  ( 0.1499999999999994671, 0.5198120922912046193, 0.07362328916749273644 ) ) ;
#20587=CARTESIAN_POINT ( 'NONE',  ( 0.02235124290213196321, 0.07000983313419809062, -0.5077112423787067952 ) ) ;
#20595=EDGE_CURVE ( 'NONE', #14366, #14410, #758, .T. ) ;
#20604=EDGE_LOOP ( 'NONE', ( #20199, #11269, #19354, #9790 ) ) ;
#20606=CARTESIAN_POINT ( 'NONE',  ( -0.03664605387828129973, -0.4684681574363449563, -0.1090337349855014654 ) ) ;
#20612=ORIENTED_EDGE ( 'NONE', *, *, #36182, .T. ) ;
#20625=CIRCLE ( 'NONE', #23275, 0.01500000000000005496 ) ;
#20639=CARTESIAN_POINT ( 'NONE',  ( 0.04308558661661680139, -0.05688326490871156715, -0.4910261092774084180 ) ) ;
#20643=CIRCLE ( 'NONE', #2905, 0.01499999999999995781 ) ;
#20650=VERTEX_POINT ( 'NONE', #20547 ) ;
#20660=FACE_OUTER_BOUND ( 'NONE', #12924, .T. ) ;
#20671=ORIENTED_EDGE ( 'NONE', *, *, #6784, .T. ) ;
#20676=CARTESIAN_POINT ( 'NONE',  ( -0.05544444631433743942, -0.4445724550912839579, -0.1231054764780145916 ) ) ;
#20685=CARTESIAN_POINT ( 'NONE',  ( 0.01548846960707511190, 0.5198120922912057296, 0.07362328916748590857 ) ) ;
#20688=DIRECTION ( 'NONE',  ( -1.000000000000000000, -2.280301054154495132E-31, 1.664003471950577689E-31 ) ) ;
#20693=CARTESIAN_POINT ( 'NONE',  ( -0.05187277790672436412, -0.2910352029727574785, -0.3700865090056942308 ) ) ;
#20699=ORIENTED_EDGE ( 'NONE', *, *, #8922, .T. ) ;
#20701=CARTESIAN_POINT ( 'NONE',  ( 0.04229974373173313318, 0.008638059335311996934, 0.4686103131113881770 ) ) ;
#20711=CARTESIAN_POINT ( 'NONE',  ( -0.01548846960707477016, 0.4638115001430995199, -0.2459753896937812156 ) ) ;
#20726=CARTESIAN_POINT ( 'NONE',  ( 0.05279905671745279555, -0.4561941007107766510, 0.1063003320160282317 ) ) ;
#20731=CARTESIAN_POINT ( 'NONE',  ( 0.05283719472145074342, -0.03966590960886508255, 0.4666299489511763210 ) ) ;
#20736=CARTESIAN_POINT ( 'NONE',  ( 0.01895494625228179644, -0.2428766181966280080, -0.4598657641708848720 ) ) ;
#20746=CARTESIAN_POINT ( 'NONE',  ( -0.04293317454820692880, 0.4432234940308288906, -0.2195257349118421575 ) ) ;
#20752=FACE_OUTER_BOUND ( 'NONE', #21380, .T. ) ;
#20754=LINE ( 'NONE', #26913, #21090 ) ;
#20758=DIRECTION ( 'NONE',  ( -5.879757087931980518E-34, -0.5877852522924756906, -0.8090169943749455639 ) ) ;
#20763=CARTESIAN_POINT ( 'NONE',  ( 0.05562144613422641271, 0.4441896308501004365, -0.1229845283801405259 ) ) ;
#20782=CIRCLE ( 'NONE', #1737, 0.01500000000000005322 ) ;
#20786=CARTESIAN_POINT ( 'NONE',  ( 0.05634307799789382842, 0.2614070397638486587, -0.3772863199289389069 ) ) ;
#20803=EDGE_CURVE ( 'NONE', #39055, #13520, #8831, .T. ) ;
#20808=ADVANCED_FACE ( 'NONE', ( #27724 ), #38363, .T. ) ;
#20816=CARTESIAN_POINT ( 'NONE',  ( -0.04229956186878638252, -0.4483852441756287499, -0.1364680347311819086 ) ) ;
#20822=ORIENTED_EDGE ( 'NONE', *, *, #4412, .T. ) ;
#20846=EDGE_CURVE ( 'NONE', #33794, #39166, #31160, .T. ) ;
#20848=CARTESIAN_POINT ( 'NONE',  ( 0.05634402396114692596, 0.01030784378588770096, -0.4588801752140551082 ) ) ;
#20853=B_SPLINE_CURVE_WITH_KNOTS ( 'NONE', 3,
 ( #35363, #3271, #31464, #29187, #22843, #31665, #15825, #838, #22634, #13345, #19539, #22027, #3877, #28376, #12742, #9848, #13559, #34548 ),
 .UNSPECIFIED., .F., .F.,
 ( 4, 2, 2, 2, 2, 2, 2, 2, 4 ),
 ( -0.003133633995111201158, -0.002350221109836720442, -0.001566808224562239726, -0.0007833953392877642148, 1.754598671129675713E-08, 0.0007834304312611872420, 0.001566843316535663187, 0.002350256201810138265, 0.003133669087084614210 ),
 .UNSPECIFIED. ) ;
#20857=ORIENTED_EDGE ( 'NONE', *, *, #40301, .T. ) ;
#20860=CARTESIAN_POINT ( 'NONE',  ( -0.01548846960707538425, 0.09061086148575919763, -0.5171215251571033011 ) ) ;
#20869=CARTESIAN_POINT ( 'NONE',  ( 0.01548846960707306146, 0.3772621329473473950, -0.3651003739302714490 ) ) ;
#20878=ORIENTED_EDGE ( 'NONE', *, *, #13555, .T. ) ;
#20880=CARTESIAN_POINT ( 'NONE',  ( 0.03650581953630565452, -0.5059763899182380120, -0.07647306779615689609 ) ) ;
#20885=EDGE_CURVE ( 'NONE', #25917, #12964, #13414, .T. ) ;
#20899=CARTESIAN_POINT ( 'NONE',  ( -0.03478556507500340372, -0.3590471004907262453, -0.3712136264428358423 ) ) ;
#20906=CARTESIAN_POINT ( 'NONE',  ( 0.02881195911414760266, -0.06013796869037528470, 0.4945549975361901440 ) ) ;
#20911=CARTESIAN_POINT ( 'NONE',  ( 0.05279185365593443841, 0.4562178057547968679, 0.1062796545749007671 ) ) ;
#20917=VERTEX_POINT ( 'NONE', #22977 ) ;
#20939=CARTESIAN_POINT ( 'NONE',  ( 0.02235124290213221648, 0.3550643254722137820, -0.3695962758878520993 ) ) ;
#20950=CARTESIAN_POINT ( 'NONE',  ( -0.04293317454820687329, 0.2295413494973353175, -0.4381202835071930091 ) ) ;
#20978=EDGE_CURVE ( 'NONE', #15491, #26696, #17381, .T. ) ;
#20984=CARTESIAN_POINT ( 'NONE',  ( 0.04154009738085341630, -0.4416556227939135715, 0.1617111092119885296 ) ) ;
#20986=PRODUCT_DEFINITION_SHAPE ( 'NONE', 'NONE',  #25768 ) ;
#20990=CARTESIAN_POINT ( 'NONE',  ( -0.01548846960707545191, -0.2306506793134033284, 0.4716198300880330985 ) ) ;
#20992=VERTEX_POINT ( 'NONE', #19674 ) ;
#20994=VERTEX_POINT ( 'NONE', #25461 ) ;
#21001=DIRECTION ( 'NONE',  ( -1.000000000000000000, -2.280301054154495132E-31, 1.664003471950577689E-31 ) ) ;
#21003=ORIENTED_EDGE ( 'NONE', *, *, #11027, .F. ) ;
#21009=EDGE_CURVE ( 'NONE', #32432, #35619, #14085, .T. ) ;
#21019=CARTESIAN_POINT ( 'NONE',  ( -0.01548846960707463312, 0.4638115001430995199, 0.2459753896937826034 ) ) ;
#21035=CARTESIAN_POINT ( 'NONE',  ( 0.01899496522502568466, -0.07377983897467746410, -0.5147126279162580476 ) ) ;
#21037=ORIENTED_EDGE ( 'NONE', *, *, #30818, .F. ) ;
#21054=DIRECTION ( 'NONE',  ( 0.000000000000000000, 0.8090169943749455639, -0.5877852522924756906 ) ) ;
#21057=EDGE_CURVE ( 'NONE', #11876, #20340, #9479, .T. ) ;
#21065=EDGE_CURVE ( 'NONE', #4571, #19277, #29742, .T. ) ;
#21067=CARTESIAN_POINT ( 'NONE',  ( 0.03654364704248769941, -0.4542255574219836722, -0.2354487068768244262 ) ) ;
#21071=SPHERICAL_SURFACE ( 'NONE', #19939, 0.01499999999999999944 ) ;
#21090=VECTOR ( 'NONE', #2020, 39.37007874015748143 ) ;
#21092=CARTESIAN_POINT ( 'NONE',  ( -0.04945776359514544862, 0.03517487494623269817, -0.4760216296475741071 ) ) ;
#21095=CARTESIAN_POINT ( 'NONE',  ( 0.03650581953630542553, 0.3643937567481987938, 0.3592734714612024760 ) ) ;
#21097=CARTESIAN_POINT ( 'NONE',  ( 0.03672447062657951955, -0.4682441148239235851, -0.1092390724017577447 ) ) ;
#21098=DIRECTION ( 'NONE',  ( -0.000000000000000000, 0.3090169943749569437, 0.9510565162951504226 ) ) ;
#21110=CARTESIAN_POINT ( 'NONE',  ( -0.05561176441985712926, -0.4442366066780419342, 0.1229089882096642827 ) ) ;
#21113=ORIENTED_EDGE ( 'NONE', *, *, #5421, .F. ) ;
#21133=CARTESIAN_POINT ( 'NONE',  ( 0.04285427992854282803, 0.2295125098185389900, 0.4383721679652319847 ) ) ;
#21143=ORIENTED_EDGE ( 'NONE', *, *, #2096, .F. ) ;
#21144=CARTESIAN_POINT ( 'NONE',  ( -0.01548846960707517956, -0.3772621329472698459, 0.3651003739303452234 ) ) ;
#21146=( BOUNDED_SURFACE ( )  B_SPLINE_SURFACE ( 3, 2, ( 
 ( #17190, #4825, #39398 ),
 ( #13693, #38777, #29737 ),
 ( #10607, #23183, #23402 ),
 ( #17396, #1581, #35709 ),
 ( #14306, #30557, #37132 ),
 ( #2177, #27063, #18206 ),
 ( #5041, #36919, #5433 ),
 ( #17603, #17998, #14496 ),
 ( #20701, #14921, #33428 ),
 ( #12038, #27476, #8733 ),
 ( #24598, #24806, #33233 ),
 ( #8945, #14716, #2574 ),
 ( #24195, #27279, #21310 ),
 ( #15110, #21521, #33849 ),
 ( #20906, #5651, #2776 ),
 ( #8337, #2379, #33621 ),
 ( #40001, #5234, #30148 ),
 ( #34038, #40418, #5839 ) ),
 .UNSPECIFIED., .F., .F., .F. ) 
 B_SPLINE_SURFACE_WITH_KNOTS ( ( 4, 2, 2, 2, 2, 2, 2, 2, 4 ),
 ( 3, 3 ),
 ( -0.001532620576208851846, -0.0007637936630077643823, 5.033250193322972611E-06, 0.0007738601633944103275, 0.001542687076595497791, 0.002311513989796585254, 0.003080340902997672284, 0.003849167816198759747, 0.004617994729399847210 ),
 ( 0.000000000000000000, 1.000000000000000000 ),
 .UNSPECIFIED. ) 
 GEOMETRIC_REPRESENTATION_ITEM ( )  RATIONAL_B_SPLINE_SURFACE ( (
 ( 1.000000000000000000, 0.7283825911960444266, 1.000000000000000000),
 ( 1.000000000000000000, 0.7404385082113551508, 1.000000000000000000),
 ( 1.000000000000000000, 0.7521504257739064503, 1.000000000000000000),
 ( 1.000000000000000000, 0.7744497410760828870, 1.000000000000000000),
 ( 1.000000000000000000, 0.7845654757375588595, 1.000000000000000000),
 ( 1.000000000000000000, 0.8022083990890596095, 1.000000000000000000),
 ( 1.000000000000000000, 0.8094167424698901492, 1.000000000000000000),
 ( 1.000000000000000000, 0.8194491993617027958, 1.000000000000000000),
 ( 1.000000000000000000, 0.8220634900780797727, 1.000000000000000000),
 ( 1.000000000000000000, 0.8220705070823152161, 1.000000000000000000),
 ( 1.000000000000000000, 0.8194468812481560116, 1.000000000000000000),
 ( 1.000000000000000000, 0.8094220769838861296, 1.000000000000000000),
 ( 1.000000000000000000, 0.8022659121983863884, 1.000000000000000000),
 ( 1.000000000000000000, 0.7845681159037143360, 1.000000000000000000),
 ( 1.000000000000000000, 0.7744426415184757495, 1.000000000000000000),
 ( 1.000000000000000000, 0.7522890290929225010, 1.000000000000000000),
 ( 1.000000000000000000, 0.7403540167214970324, 1.000000000000000000),
 ( 1.000000000000000000, 0.7283825911960213340, 1.000000000000000000) ) ) 
 REPRESENTATION_ITEM ( '' )  SURFACE ( )  );
#21150=CARTESIAN_POINT ( 'NONE',  ( -0.02953079040095700838, 0.2329676531120452587, -0.4763574306556336291 ) ) ;
#21151=AXIS2_PLACEMENT_3D ( 'NONE', #34491, #6304, #594 ) ;
#21162=CARTESIAN_POINT ( 'NONE',  ( -0.03662792686184376811, -0.3149733899719669439, 0.3635662525351520125 ) ) ;
#21164=VERTEX_POINT ( 'NONE', #1797 ) ;
#21168=DIRECTION ( 'NONE',  ( 0.000000000000000000, 0.9510565162951547524, 0.3090169943749439541 ) ) ;
#21169=SPHERICAL_SURFACE ( 'NONE', #34904, 0.01499999999999999944 ) ;
#21174=AXIS2_PLACEMENT_3D ( 'NONE', #38151, #29098, #37960 ) ;
#21177=DIRECTION ( 'NONE',  ( 1.000000000000000000, 0.000000000000000000, 0.000000000000000000 ) ) ;
#21194=CIRCLE ( 'NONE', #2809, 0.01500000000000001853 ) ;
#21215=CARTESIAN_POINT ( 'NONE',  ( 0.01548846960707528191, -0.09319974324248665731, 0.5318964258758798191 ) ) ;
#21232=CARTESIAN_POINT ( 'NONE',  ( 0.03170874437002593749, -0.2433708063334450444, 0.4274019033148761526 ) ) ;
#21240=AXIS2_PLACEMENT_3D ( 'NONE', #30139, #17777, #39797 ) ;
#21245=CARTESIAN_POINT ( 'NONE',  ( 0.02953079040095500304, -0.09152108205201843483, -0.5223162075576466279 ) ) ;
#21257=ORIENTED_EDGE ( 'NONE', *, *, #27391, .T. ) ;
#21279=DIRECTION ( 'NONE',  ( 0.000000000000000000, -0.9901182710308658041, -0.1402348365095101024 ) ) ;
#21300=CARTESIAN_POINT ( 'NONE',  ( -0.04308745346420909256, -0.2425953941929105406, 0.4306799763758633048 ) ) ;
#21303=CARTESIAN_POINT ( 'NONE',  ( -0.05078493045284435126, -0.04880252970039603705, -0.4712186791567240518 ) ) ;
#21310=CARTESIAN_POINT ( 'NONE',  ( 0.05078310099560734425, -0.04880952477023445257, 0.4712228254505129721 ) ) ;
#21312=CARTESIAN_POINT ( 'NONE',  ( 0.02242828275838676735, -0.4611032487610184916, -0.2233397882698420489 ) ) ;
#21318=CARTESIAN_POINT ( 'NONE',  ( 0.03174060074380018193, -0.3664546090234483966, -0.3753288017716262526 ) ) ;
#21323=ORIENTED_EDGE ( 'NONE', *, *, #11148, .F. ) ;
#21342=CARTESIAN_POINT ( 'NONE',  ( -0.01548846960688975496, 0.09061086148592420453, -0.5171215251575761451 ) ) ;
#21346=CARTESIAN_POINT ( 'NONE',  ( -0.03174036153404255489, 0.2437184149031580704, 0.4645026301777952504 ) ) ;
#21354=EDGE_LOOP ( 'NONE', ( #25509, #4633, #4073, #12349 ) ) ;
#21368=ADVANCED_FACE ( 'NONE', ( #34043 ), #15858, .T. ) ;
#21369=CARTESIAN_POINT ( 'NONE',  ( 0.03170874437003164126, 0.2433708063334497629, -0.4274019033148664937 ) ) ;
#21380=EDGE_LOOP ( 'NONE', ( #8619, #18272, #34967, #3288 ) ) ;
#21381=CARTESIAN_POINT ( 'NONE',  ( -0.02231181081520755560, 0.3551561381230132208, -0.3696296485972541124 ) ) ;
#21386=ORIENTED_EDGE ( 'NONE', *, *, #8646, .T. ) ;
#21404=EDGE_CURVE ( 'NONE', #21164, #35448, #25954, .T. ) ;
#21409=DIRECTION ( 'NONE',  ( -1.664003471950577032E-31, -3.330669073875470607E-16, -1.000000000000000000 ) ) ;
#21416=EDGE_LOOP ( 'NONE', ( #13703, #28095, #14128, #15669 ) ) ;
#21431=CARTESIAN_POINT ( 'NONE',  ( -0.03158843595483366157, -0.4482533282649006634, 0.2030547983902455944 ) ) ;
#21435=EDGE_CURVE ( 'NONE', #1535, #14410, #2938, .T. ) ;
#21442=CARTESIAN_POINT ( 'NONE',  ( -0.05187277790672265715, -0.4419080096627363563, 0.1624279055868609323 ) ) ;
#21453=AXIS2_PLACEMENT_3D ( 'NONE', #18278, #33921, #12313 ) ;
#21461=CARTESIAN_POINT ( 'NONE',  ( 0.04157143636675288134, -0.01703379379374815594, -0.4699528923077430087 ) ) ;
#21476=SPHERICAL_SURFACE ( 'NONE', #11271, 0.01499999999999999944 ) ;
#21514=CARTESIAN_POINT ( 'NONE',  ( -0.01548846960707517956, -0.3772621329472692908, -0.3651003739303438911 ) ) ;
#21516=CARTESIAN_POINT ( 'NONE',  ( -0.04211471441534185567, 0.008601378579329254509, -0.4689528935642813257 ) ) ;
#21521=CARTESIAN_POINT ( 'NONE',  ( 0.04308611741967044440, -0.05688666786373557105, 0.4910246251072628021 ) ) ;
#21545=CARTESIAN_POINT ( 'NONE',  ( -0.03868264068766689295, 0.4417248602032612936, 0.1788646266443642829 ) ) ;
#21549=CARTESIAN_POINT ( 'NONE',  ( -0.04760454375021182932, 0.2475296122118653130, 0.4138634427292582352 ) ) ;
#21550=EDGE_CURVE ( 'NONE', #13008, #36014, #40425, .T. ) ;
#21553=DIRECTION ( 'NONE',  ( 0.000000000000000000, 3.330669073875470114E-16, 1.000000000000000000 ) ) ;
#21566=CARTESIAN_POINT ( 'NONE',  ( 0.01548846960706656492, 0.3688619771573081185, -0.3775276577327085215 ) ) ;
#21583=EDGE_LOOP ( 'NONE', ( #2333, #19436 ) ) ;
#21595=EDGE_CURVE ( 'NONE', #38334, #13520, #20030, .T. ) ;
#21609=ORIENTED_EDGE ( 'NONE', *, *, #25279, .F. ) ;
#21613=DIRECTION ( 'NONE',  ( -1.000000000000000000, -2.341930812374887555E-31, 1.664003471950578127E-31 ) ) ;
#21619=CARTESIAN_POINT ( 'NONE',  ( 0.04155248107635927529, 0.4523094957185405662, -0.1288470070525098432 ) ) ;
#21639=DIRECTION ( 'NONE',  ( -1.000000000000000000, -2.280301054154496446E-31, -1.355854680848613603E-31 ) ) ;
#21653=ORIENTED_EDGE ( 'NONE', *, *, #37822, .F. ) ;
#21674=ORIENTED_EDGE ( 'NONE', *, *, #33140, .F. ) ;
#21679=DIRECTION ( 'NONE',  ( 0.000000000000000000, 3.330669073875470114E-16, 1.000000000000000000 ) ) ;
#21689=CARTESIAN_POINT ( 'NONE',  ( -0.05281452789367711842, -0.3064952470001998663, -0.3541670097232285652 ) ) ;
#21696=CARTESIAN_POINT ( 'NONE',  ( -0.05489899477340628303, 0.02536133381296927503, -0.4620560448752992211 ) ) ;
#21703=CARTESIAN_POINT ( 'NONE',  ( 0.04157078424165231573, -0.4416882993450223505, -0.1614266821413831432 ) ) ;
#21706=CARTESIAN_POINT ( 'NONE',  ( 0.05268850283020568709, 0.4471020566665044327, 0.1404229504685621521 ) ) ;
#21708=CARTESIAN_POINT ( 'NONE',  ( 0.04575106512774653605, -0.3363942840372673437, -0.3523417416125881885 ) ) ;
#21709=ORIENTED_EDGE ( 'NONE', *, *, #24584, .F. ) ;
#21714=ADVANCED_FACE ( 'NONE', ( #19734 ), #10473, .T. ) ;
#21733=CARTESIAN_POINT ( 'NONE',  ( -0.04945776359514872378, 0.2513414220725579407, 0.4057848608195681606 ) ) ;
#21739=CARTESIAN_POINT ( 'NONE',  ( 0.03662792686184422608, 0.2484399233013424024, -0.4119056456069861705 ) ) ;
#21743=EDGE_LOOP ( 'NONE', ( #4738, #26769, #16050, #19382 ) ) ;
#21756=CARTESIAN_POINT ( 'NONE',  ( 0.04308611741967133257, 0.3346393142056199310, -0.3638101219459927149 ) ) ;
#21762=ORIENTED_EDGE ( 'NONE', *, *, #38689, .T. ) ;
#21768=ADVANCED_FACE ( 'NONE', ( #6321 ), #24867, .T. ) ;
#21774=ORIENTED_EDGE ( 'NONE', *, *, #11727, .T. ) ;
#21798=AXIS2_PLACEMENT_3D ( 'NONE', #24555, #17566, #30109 ) ;
#21809=DIRECTION ( 'NONE',  ( 1.000000000000000000, -1.049121689386597152E-11, 1.416614914756796105E-11 ) ) ;
#21810=ORIENTED_EDGE ( 'NONE', *, *, #32320, .F. ) ;
#21812=DIRECTION ( 'NONE',  ( 0.000000000000000000, 3.330669073875470114E-16, 1.000000000000000000 ) ) ;
#21814=DIRECTION ( 'NONE',  ( 0.3468893892380797705, -0.7770416411309306604, 0.5252371270032060169 ) ) ;
#21818=CARTESIAN_POINT ( 'NONE',  ( 0.02231181081520726070, 0.4612879682508960189, -0.2235517164227164566 ) ) ;
#21821=EDGE_CURVE ( 'NONE', #20386, #9762, #743, .T. ) ;
#21833=CARTESIAN_POINT ( 'NONE',  ( -0.03877220711930352143, -0.4416859332762705370, 0.1784371778270249786 ) ) ;
#21848=CARTESIAN_POINT ( 'NONE',  ( 0.04575106512774684830, -0.2311453587453369818, 0.4288095618640354045 ) ) ;
#21855=CARTESIAN_POINT ( 'NONE',  ( -0.03643058821097221872, 0.4544345964805175386, 0.2356993163710971728 ) ) ;
#21873=CARTESIAN_POINT ( 'NONE',  ( 0.04293701532779490432, 0.4432143466407591492, -0.2195216604697225182 ) ) ;
#21874=TOROIDAL_SURFACE ( 'NONE', #28432, 0.6154198107346402491, 0.7750185148639454624 ) ;
#21879=ADVANCED_FACE ( 'NONE', ( #36773 ), #26349, .F. ) ;
#21891=CIRCLE ( 'NONE', #26457, 0.01500000000000001853 ) ;
#21905=CARTESIAN_POINT ( 'NONE',  ( -0.03672309138969667014, -0.04080728438229332816, 0.4790859898006363249 ) ) ;
#21913=CARTESIAN_POINT ( 'NONE',  ( -0.05615703521555036326, 0.01030498872321548333, -0.4592891699083767598 ) ) ;
#21922=CARTESIAN_POINT ( 'NONE',  ( 0.01548846960707524721, -0.09061086148575756005, -0.5171215251571035232 ) ) ;
#21924=CARTESIAN_POINT ( 'NONE',  ( 0.03170953572518930147, -0.2433677181033266079, -0.4274019581173345017 ) ) ;
#21932=CIRCLE ( 'NONE', #15984, 0.1249999999999999584 ) ;
#21942=FACE_OUTER_BOUND ( 'NONE', #27293, .T. ) ;
#21943=DIRECTION ( 'NONE',  ( -1.416619696839555637E-11, 0.5877852522924655876, -0.8090169943749527803 ) ) ;
#21952=CARTESIAN_POINT ( 'NONE',  ( -0.05138886601528275949, 0.2952081121918923023, 0.3684218102521255589 ) ) ;
#21968=DIRECTION ( 'NONE',  ( 1.654489825136704222E-31, -0.9510565162951546414, -0.3090169943749438985 ) ) ;
#21971=AXIS2_PLACEMENT_3D ( 'NONE', #32865, #8184, #39447 ) ;
#21979=ORIENTED_EDGE ( 'NONE', *, *, #12355, .F. ) ;
#21988=ORIENTED_EDGE ( 'NONE', *, *, #32755, .F. ) ;
#21999=CARTESIAN_POINT ( 'NONE',  ( -0.01548846960712776770, 0.5203207976466729390, -0.08861466064782422269 ) ) ;
#22022=DIRECTION ( 'NONE',  ( -1.000000000000000000, -2.280301054154495132E-31, 1.664003471950577689E-31 ) ) ;
#22027=CARTESIAN_POINT ( 'NONE',  ( 0.05283710938261026308, -0.2421875768565588671, -0.4008269984734638691 ) ) ;
#22030=CARTESIAN_POINT ( 'NONE',  ( 0.03868649100028130616, 0.2522293598345318744, 0.4043344736883378032 ) ) ;
#22033=ORIENTED_EDGE ( 'NONE', *, *, #22971, .T. ) ;
#22047=CARTESIAN_POINT ( 'NONE',  ( 0.1499999999999996059, -0.3232818887608613356, -0.4449593469062207429 ) ) ;
#22049=CARTESIAN_POINT ( 'NONE',  ( -0.02881302694830086691, -0.4889319715862793791, 0.09562644460326608087 ) ) ;
#22053=CARTESIAN_POINT ( 'NONE',  ( 0.1499999999999996336, -0.09319974324249266640, -0.5318964258758781538 ) ) ;
#22056=EDGE_CURVE ( 'NONE', #26023, #39166, #27175, .T. ) ;
#22064=CARTESIAN_POINT ( 'NONE',  ( 0.05201782277453730063, -0.2909620873304541444, 0.3697179445082250382 ) ) ;
#22066=PRODUCT_DEFINITION_CONTEXT ( 'detailed design', #16635, 'design' ) ;
#22070=CARTESIAN_POINT ( 'NONE',  ( -0.05076679145662017084, 0.4330939261214903357, 0.1921033382362740127 ) ) ;
#22086=ORIENTED_EDGE ( 'NONE', *, *, #933, .F. ) ;
#22087=EDGE_LOOP ( 'NONE', ( #38905, #2444, #22086, #10029 ) ) ;
#22108=CARTESIAN_POINT ( 'NONE',  ( 0.04582889109739183425, -0.4790149006698671830, 0.08746027838083611505 ) ) ;
#22112=CARTESIAN_POINT ( 'NONE',  ( 0.08978098643734198914, 0.000000000000000000, 0.000000000000000000 ) ) ;
#22123=CARTESIAN_POINT ( 'NONE',  ( -0.04575334816097881979, 0.06504672743687374414, 0.4827724779829230539 ) ) ;
#22132=ORIENTED_EDGE ( 'NONE', *, *, #16235, .T. ) ;
#22146=ORIENTED_EDGE ( 'NONE', *, *, #22762, .T. ) ;
#22153=EDGE_CURVE ( 'NONE', #26023, #23035, #7256, .T. ) ;
#22157=CARTESIAN_POINT ( 'NONE',  ( -0.04230258372739908318, 0.2720195588163330513, -0.3815939145425404355 ) ) ;
#22163=AXIS2_PLACEMENT_3D ( 'NONE', #18191, #14091, #39199 ) ;
#22165=CARTESIAN_POINT ( 'NONE',  ( -0.04140212552917726246, 0.2901315858634238576, 0.3705031754532664423 ) ) ;
#22172=CARTESIAN_POINT ( 'NONE',  ( 0.01548846960707524721, 0.5198120922912040642, 0.07362328916749247276 ) ) ;
#22183=CARTESIAN_POINT ( 'NONE',  ( 0.04285640132274361885, 0.2295067898340935886, -0.4383690285535431497 ) ) ;
#22224=ORIENTED_EDGE ( 'NONE', *, *, #36841, .F. ) ;
#22228=CARTESIAN_POINT ( 'NONE',  ( -0.03158843595483520200, 0.05459869295506113857, 0.4890616322892843981 ) ) ;
#22229=CARTESIAN_POINT ( 'NONE',  ( -0.04293317454820639451, -0.4876093284570337527, -0.08292018301452905304 ) ) ;
#22237=CARTESIAN_POINT ( 'NONE',  ( 0.1499999999999993561, 5.828670879282072084E-17, 0.1749999999999999889 ) ) ;
#22245=ORIENTED_EDGE ( 'NONE', *, *, #35019, .T. ) ;
#22249=CARTESIAN_POINT ( 'NONE',  ( -0.03301200226531703086, -0.4610556019031558095, 0.2426442821263273819 ) ) ;
#22257=CIRCLE ( 'NONE', #30742, 0.5302738246768088359 ) ;
#22259=DIRECTION ( 'NONE',  ( 0.000000000000000000, 0.3090169943749439541, -0.9510565162951547524 ) ) ;
#22266=CARTESIAN_POINT ( 'NONE',  ( -0.05078310099561082064, 0.4632425114130818700, 0.09919524461159424933 ) ) ;
#22268=EDGE_CURVE ( 'NONE', #34829, #13520, #40133, .T. ) ;
#22287=ORIENTED_EDGE ( 'NONE', *, *, #22762, .F. ) ;
#22300=DIRECTION ( 'NONE',  ( 0.000000000000000000, 3.330669073875470114E-16, 1.000000000000000000 ) ) ;
#22303=CARTESIAN_POINT ( 'NONE',  ( -0.01548846960721252282, -0.4730347584884301293, 0.2341461249027971259 ) ) ;
#22309=CARTESIAN_POINT ( 'NONE',  ( -0.03874953289575296805, -0.03331175461110518626, 0.4752512399555741673 ) ) ;
#22310=ADVANCED_FACE ( 'NONE', ( #8908 ), #5613, .T. ) ;
#22317=ORIENTED_EDGE ( 'NONE', *, *, #31770, .T. ) ;
#22329=CARTESIAN_POINT ( 'NONE',  ( 0.01896931156527473933, -0.2428675472501181931, -0.4598342473848889278 ) ) ;
#22337=ADVANCED_FACE ( 'NONE', ( #12208 ), #9236, .T. ) ;
#22348=CARTESIAN_POINT ( 'NONE',  ( -0.05187277790672548822, 0.2620383623028448850, -0.3911539469301719696 ) ) ;
#22349=CARTESIAN_POINT ( 'NONE',  ( -0.03170752374382804911, -0.4481131438208651452, -0.2027288335082092219 ) ) ;
#22355=VECTOR ( 'NONE', #22603, 39.37007874015748143 ) ;
#22356=CARTESIAN_POINT ( 'NONE',  ( 0.04230170315644477680, 0.4483301424763361243, -0.1366247710447582586 ) ) ;
#22359=CARTESIAN_POINT ( 'NONE',  ( 0.03868264068766665009, 0.2522289290439784226, -0.4043438810462526845 ) ) ;
#22363=CARTESIAN_POINT ( 'NONE',  ( -0.02953079040095700838, 0.000000000000000000, 0.000000000000000000 ) ) ;
#22373=DIRECTION ( 'NONE',  ( 0.000000000000000000, -0.9510565162951545304, -0.3090169943749445092 ) ) ;
#22408=DIRECTION ( 'NONE',  ( -0.9378410757839557021, -0.1072489841977669889, -0.3300784330442382286 ) ) ;
#22414=AXIS2_PLACEMENT_3D ( 'NONE', #15536, #34651, #13052 ) ;
#22421=AXIS2_PLACEMENT_3D ( 'NONE', #11270, #1834, #27116 ) ;
#22422=FACE_OUTER_BOUND ( 'NONE', #37429, .T. ) ;
#22443=CARTESIAN_POINT ( 'NONE',  ( -0.01895884884825295436, 0.07380796352548431305, -0.5147901372834192690 ) ) ;
#22448=FACE_OUTER_BOUND ( 'NONE', #834, .T. ) ;
#22453=DIRECTION ( 'NONE',  ( 0.9378410757839510392, -0.2807814858886686360, -0.2039996905746500333 ) ) ;
#22476=DIRECTION ( 'NONE',  ( -1.000000000000000000, -2.280301054154495132E-31, 1.664003471950577689E-31 ) ) ;
#22491=VERTEX_POINT ( 'NONE', #25159 ) ;
#22497=CARTESIAN_POINT ( 'NONE',  ( -0.02953079040095700838, 0.000000000000000000, 0.000000000000000000 ) ) ;
#22510=CIRCLE ( 'NONE', #9323, 0.5302738246768106123 ) ;
#22512=CARTESIAN_POINT ( 'NONE',  ( -0.02953079040095627286, 0.09152108205202029445, 0.5223162075576441854 ) ) ;
#22519=DIRECTION ( 'NONE',  ( 0.3468893892380646715, 0.3199132558031939078, 0.8816593788960921385 ) ) ;
#22527=AXIS2_PLACEMENT_3D ( 'NONE', #19797, #7655, #3400 ) ;
#22529=CARTESIAN_POINT ( 'NONE',  ( 0.04946426091937270592, -0.2513512500265240313, -0.4057590668656845256 ) ) ;
#22530=EDGE_LOOP ( 'NONE', ( #34001, #33843 ) ) ;
#22532=EDGE_LOOP ( 'NONE', ( #12504, #20857, #39355, #39907 ) ) ;
#22542=CARTESIAN_POINT ( 'NONE',  ( -0.02953079040095652960, 0.5250338024619264354, -0.07436286310882528339 ) ) ;
#22548=CARTESIAN_POINT ( 'NONE',  ( -0.04211812644076726175, 0.2687274166943798837, -0.3844079338164257398 ) ) ;
#22560=CARTESIAN_POINT ( 'NONE',  ( 0.01548846960707360443, 0.4730347584886807066, -0.2341461249029813674 ) ) ;
#22563=CARTESIAN_POINT ( 'NONE',  ( 0.04155248107635910182, -0.01723053523177138849, 0.4699878081388675910 ) ) ;
#22568=EDGE_LOOP ( 'NONE', ( #12155, #20699 ) ) ;
#22580=CARTESIAN_POINT ( 'NONE',  ( 0.01548846960706677829, 0.5198120922912281561, -0.07362328916749191765 ) ) ;
#22583=CARTESIAN_POINT ( 'NONE',  ( -0.1399999999999997358, 0.000000000000000000, 0.000000000000000000 ) ) ;
#22596=AXIS2_PLACEMENT_3D ( 'NONE', #37235, #21613, #21812 ) ;
#22603=DIRECTION ( 'NONE',  ( -1.000000000000000000, -2.341930812374887555E-31, 1.664003471950578127E-31 ) ) ;
#22607=DIRECTION ( 'NONE',  ( 1.000000000000000000, 2.280301054154495132E-31, -1.664003471950577689E-31 ) ) ;
#22612=CARTESIAN_POINT ( 'NONE',  ( 0.06980746140711582837, 7.160938508832261116E-17, 0.2149999999999999967 ) ) ;
#22619=DIRECTION ( 'NONE',  ( 1.000000000000000000, -1.671477276948176127E-11, -5.600159359328265480E-12 ) ) ;
#22625=ADVANCED_FACE ( 'NONE', ( #6727 ), #9922, .T. ) ;
#22634=CARTESIAN_POINT ( 'NONE',  ( 0.05634307799789382148, -0.2780413953411557948, -0.3652007531760622094 ) ) ;
#22640=ORIENTED_EDGE ( 'NONE', *, *, #4146, .F. ) ;
#22644=ORIENTED_EDGE ( 'NONE', *, *, #4864, .F. ) ;
#22645=AXIS2_PLACEMENT_3D ( 'NONE', #26752, #20174, #35792 ) ;
#22656=CARTESIAN_POINT ( 'NONE',  ( -0.01895494625228214686, -0.07381100255646640129, -0.5147985126481153806 ) ) ;
#22668=DIRECTION ( 'NONE',  ( 1.000000000000000000, 1.049121689386595374E-11, -1.416614914756797075E-11 ) ) ;
#22670=CARTESIAN_POINT ( 'NONE',  ( 0.03875673594170116892, -0.3062691647558810071, 0.3649083695375496816 ) ) ;
#22672=AXIS2_PLACEMENT_3D ( 'NONE', #11797, #24568, #14467 ) ;
#22677=CARTESIAN_POINT ( 'NONE',  ( -0.02242828275839765448, 0.5043161982042816405, 0.09034400517547079568 ) ) ;
#22679=EDGE_LOOP ( 'NONE', ( #1566, #19588, #16301, #10896 ) ) ;
#22680=CARTESIAN_POINT ( 'NONE',  ( 0.1499999999999996336, 1.092739197465705287E-15, 0.5500000000000003775 ) ) ;
#22690=ORIENTED_EDGE ( 'NONE', *, *, #7273, .T. ) ;
#22691=VERTEX_POINT ( 'NONE', #13907 ) ;
#22692=DIRECTION ( 'NONE',  ( 0.000000000000000000, 0.5877852522924426060, -0.8090169943749696557 ) ) ;
#22707=CARTESIAN_POINT ( 'NONE',  ( -0.05634304521267748805, 0.01028134608269738216, 0.4588823192046725952 ) ) ;
#22715=CIRCLE ( 'NONE', #10216, 0.3698489655878002824 ) ;
#22724=CARTESIAN_POINT ( 'NONE',  ( -0.05268850283020124620, -0.004611971649426341129, 0.4686124025367036650 ) ) ;
#22742=CARTESIAN_POINT ( 'NONE',  ( 0.04047043078436068225, -0.2415826219374506978, -0.4392104278742940404 ) ) ;
#22743=ORIENTED_EDGE ( 'NONE', *, *, #13928, .F. ) ;
#22756=B_SPLINE_CURVE_WITH_KNOTS ( 'NONE', 3,
 ( #9296, #38452, #22852, #21873, #34402, #35371, #6217, #18784, #35976, #7580, #20763, #29802, #39263, #26315, #5093, #13750, #17251, #20351 ),
 .UNSPECIFIED., .F., .F.,
 ( 4, 2, 2, 2, 2, 2, 2, 2, 4 ),
 ( -0.003133633995111210699, -0.002350221109836731284, -0.001566808224562251869, -0.0007833953392877724548, 1.754598670695994844E-08, 0.0007834304312611863746, 0.001566843316535665789, 0.002350256201810145204, 0.003133669087084624619 ),
 .UNSPECIFIED. ) ;
#22761=CARTESIAN_POINT ( 'NONE',  ( -0.05137569054208679376, 0.2953118892970998943, -0.3683837247633647283 ) ) ;
#22762=EDGE_CURVE ( 'NONE', #16145, #39882, #5317, .T. ) ;
#22764=CARTESIAN_POINT ( 'NONE',  ( -0.04308449196697855532, -0.4494173824501559444, -0.2058378951121007383 ) ) ;
#22769=DIRECTION ( 'NONE',  ( 0.9378410757839521494, 0.1072489841977705138, -0.3300784330442476655 ) ) ;
#22771=CARTESIAN_POINT ( 'NONE',  ( 0.03170953572518750430, 0.4816881781209779723, -0.09938198567066169886 ) ) ;
#22774=VERTEX_POINT ( 'NONE', #11656 ) ;
#22776=CARTESIAN_POINT ( 'NONE',  ( 0.01895494625228159868, -0.3623053290766977130, 0.3730957266516582438 ) ) ;
#22790=DIRECTION ( 'NONE',  ( 0.9378410757839510392, 0.3470650033817896385, 0.000000000000000000 ) ) ;
#22794=CARTESIAN_POINT ( 'NONE',  ( 0.01548846960707528191, -0.4638115001430989648, 0.2459753896937853235 ) ) ;
#22808=EDGE_LOOP ( 'NONE', ( #28876, #14975 ) ) ;
#22821=AXIS2_PLACEMENT_3D ( 'NONE', #34918, #9819, #6520 ) ;
#22843=CARTESIAN_POINT ( 'NONE',  ( 0.04582713223189486401, -0.3361263728083079827, -0.3523178389613200179 ) ) ;
#22845=CARTESIAN_POINT ( 'NONE',  ( -0.04229956186878661151, 0.008769846780145210130, 0.4686106502047103772 ) ) ;
#22852=CARTESIAN_POINT ( 'NONE',  ( 0.03650581953630514798, 0.4542932396444852028, -0.2355374485430464515 ) ) ;
#22866=DIRECTION ( 'NONE',  ( -1.000000000000000000, -2.341930812374887555E-31, 1.664003471950578127E-31 ) ) ;
#22872=DIRECTION ( 'NONE',  ( 0.3468893892380643384, -0.7770416411310734350, -0.5252371270030050665 ) ) ;
#22877=DIRECTION ( 'NONE',  ( 0.9378410757839554801, 0.1072489841977693065, 0.3300784330442383396 ) ) ;
#22879=CARTESIAN_POINT ( 'NONE',  ( 0.03171861681800964422, -0.3665016810530177804, 0.3753647833258587641 ) ) ;
#22883=DIRECTION ( 'NONE',  ( 5.879757087911781259E-34, 0.5877852522924815748, 0.8090169943749412340 ) ) ;
#22891=FACE_OUTER_BOUND ( 'NONE', #18879, .T. ) ;
#22892=EDGE_LOOP ( 'NONE', ( #30816, #15321, #9456, #38587 ) ) ;
#22898=DIRECTION ( 'NONE',  ( -1.355854680848614260E-31, 3.330669073875470114E-16, 1.000000000000000000 ) ) ;
#22917=( LENGTH_UNIT ( ) NAMED_UNIT ( * ) SI_UNIT ( $, .METRE. ) );
#22919=CARTESIAN_POINT ( 'NONE',  ( 0.03868264068766581742, -0.4624969084406961306, -0.1149348357506052437 ) ) ;
#22936=CARTESIAN_POINT ( 'NONE',  ( -0.02587796518899032269, 0.000000000000000000, 0.000000000000000000 ) ) ;
#22939=CARTESIAN_POINT ( 'NONE',  ( -0.02953079040095619306, 0.5250338024619283228, -0.07436286310882472828 ) ) ;
#22957=CARTESIAN_POINT ( 'NONE',  ( -0.01548846960688955027, -0.3772621329476795737, 0.3651003739306307172 ) ) ;
#22958=CARTESIAN_POINT ( 'NONE',  ( 0.04308558661662140882, 0.4494156853470169244, -0.2058346122081022578 ) ) ;
#22961=CARTESIAN_POINT ( 'NONE',  ( 0.03868264068766624070, -0.2522289290439759801, 0.4043438810462554045 ) ) ;
#22962=CARTESIAN_POINT ( 'NONE',  ( -0.02872242845530504490, -0.2464193076120103354, -0.4721747535844858512 ) ) ;
#22970=CARTESIAN_POINT ( 'NONE',  ( -0.04155248107635989285, -0.2901916982059679073, -0.3701002694350356559 ) ) ;
#22971=EDGE_CURVE ( 'NONE', #10166, #1535, #30943, .T. ) ;
#22973=DIRECTION ( 'NONE',  ( -2.280301054154496008E-31, 1.000000000000000000, -3.330669073875470114E-16 ) ) ;
#22977=CARTESIAN_POINT ( 'NONE',  ( -0.05634304521267782806, -2.731847993664263218E-15, -0.4588823192046729837 ) ) ;
#22982=CARTESIAN_POINT ( 'NONE',  ( 0.01548846960707524721, 0.5198120922912040642, 0.07362328916749247276 ) ) ;
#22994=CARTESIAN_POINT ( 'NONE',  ( 0.03643058821096724353, -0.4544345964805293625, 0.2356993163711000594 ) ) ;
#23000=ADVANCED_FACE ( 'NONE', ( #17136, #29687 ), #1530, .F. ) ;
#23005=DIRECTION ( 'NONE',  ( -1.000000000000000000, -2.280301054154495132E-31, 1.664003471950577689E-31 ) ) ;
#23011=CARTESIAN_POINT ( 'NONE',  ( 0.04047170147976884153, 0.3430616206016774417, 0.3654769923554775923 ) ) ;
#23032=ORIENTED_EDGE ( 'NONE', *, *, #1491, .F. ) ;
#23035=VERTEX_POINT ( 'NONE', #5796 ) ;
#23041=CARTESIAN_POINT ( 'NONE',  ( -0.03664605387828207689, -0.2484618661253097660, 0.4118464167359232597 ) ) ;
#23054=DIRECTION ( 'NONE',  ( 1.000000000000000000, 2.341930812374887555E-31, -1.664003471950578127E-31 ) ) ;
#23058=EDGE_CURVE ( 'NONE', #1932, #11795, #30302, .T. ) ;
#23092=ORIENTED_EDGE ( 'NONE', *, *, #3963, .F. ) ;
#23104=AXIS2_PLACEMENT_3D ( 'NONE', #10245, #28759, #26096 ) ;
#23112=( NAMED_UNIT ( * ) SI_UNIT ( $, .STERADIAN. ) SOLID_ANGLE_UNIT ( ) );
#23114=DIRECTION ( 'NONE',  ( 0.000000000000000000, -0.5877852522924689183, -0.8090169943749506709 ) ) ;
#23121=CIRCLE ( 'NONE', #5338, 0.5400000000000004796 ) ;
#23123=CARTESIAN_POINT ( 'NONE',  ( -0.01548846960707477016, 0.3772621329472714558, -0.3651003739303416706 ) ) ;
#23128=AXIS2_PLACEMENT_3D ( 'NONE', #31321, #3129, #15668 ) ;
#23130=VERTEX_POINT ( 'NONE', #35409 ) ;
#23138=CARTESIAN_POINT ( 'NONE',  ( 0.04293694706340183548, -0.07181688488226646572, -0.4893579783150012186 ) ) ;
#23140=CARTESIAN_POINT ( 'NONE',  ( -0.01548846960707434342, 0.5203207976467951745, -0.08861466064782075325 ) ) ;
#23141=ORIENTED_EDGE ( 'NONE', *, *, #25842, .F. ) ;
#23157=CARTESIAN_POINT ( 'NONE',  ( -0.05187277790672314981, -0.4529838172322686041, -0.1283400749691716025 ) ) ;
#23169=CARTESIAN_POINT ( 'NONE',  ( 0.04154009738085443632, -0.2622554993748571484, 0.3904256972020325733 ) ) ;
#23170=CARTESIAN_POINT ( 'NONE',  ( -0.05137569054208727948, -0.2590973494995065796, -0.3946951280584622967 ) ) ;
#23174=CARTESIAN_POINT ( 'NONE',  ( -0.05634304521267782806, -2.731847993664263218E-15, -0.4588823192046729837 ) ) ;
#23176=DIRECTION ( 'NONE',  ( 1.000000000000000000, 2.280301054154495132E-31, -1.664003471950577689E-31 ) ) ;
#23180=CARTESIAN_POINT ( 'NONE',  ( -0.04154009738085488734, -0.2622554993748581476, -0.3904256972020316296 ) ) ;
#23183=CARTESIAN_POINT ( 'NONE',  ( 0.03474878377840755206, 0.07233677907409778729, 0.5114521822558344422 ) ) ;
#23184=CARTESIAN_POINT ( 'NONE',  ( 0.04308558661660893963, -0.4845714764516787509, -0.09763621268895587846 ) ) ;
#23185=DIRECTION ( 'NONE',  ( 1.000000000000000000, 0.000000000000000000, 0.000000000000000000 ) ) ;
#23189=DIRECTION ( 'NONE',  ( -1.000000000000000000, -2.341930812374887555E-31, 1.664003471950578127E-31 ) ) ;
#23193=FACE_OUTER_BOUND ( 'NONE', #38737, .T. ) ;
#23206=CARTESIAN_POINT ( 'NONE',  ( 0.02953079040094766169, -0.5250338024619503052, 0.07436286310882213313 ) ) ;
#23212=CARTESIAN_POINT ( 'NONE',  ( 0.03309059653085733022, -0.08822156176787505910, 0.5132714489379874845 ) ) ;
#23219=AXIS2_PLACEMENT_3D ( 'NONE', #18067, #34850, #39659 ) ;
#23221=CARTESIAN_POINT ( 'NONE',  ( 0.04285640132273772773, 0.3459922227646676229, 0.3537374076363822839 ) ) ;
#23230=CARTESIAN_POINT ( 'NONE',  ( -0.04945776359515208220, -0.3082555652855825112, 0.3644343153303030713 ) ) ;
#23235=FACE_OUTER_BOUND ( 'NONE', #28541, .T. ) ;
#23250=CARTESIAN_POINT ( 'NONE',  ( -0.02231181081520691722, -0.5045902076536115111, 0.09028112709016047899 ) ) ;
#23258=CARTESIAN_POINT ( 'NONE',  ( 0.02869942827333513830, 0.4892109928530955498, 0.09550568247005990219 ) ) ;
#23265=CARTESIAN_POINT ( 'NONE',  ( 0.05634307799789359250, 0.4395998308137160637, 0.1320249839695993577 ) ) ;
#23275=AXIS2_PLACEMENT_3D ( 'NONE', #23123, #17130, #26015 ) ;
#23295=ADVANCED_FACE ( 'NONE', ( #22891 ), #1464, .T. ) ;
#23308=CIRCLE ( 'NONE', #12773, 0.01499999999999995087 ) ;
#23320=DIRECTION ( 'NONE',  ( -1.725633230170958726E-31, -0.8983234858819668656, 0.4393346272636288186 ) ) ;
#23321=CARTESIAN_POINT ( 'NONE',  ( 0.01548846960707528191, 0.2306506793134049660, -0.4716198300880325434 ) ) ;
#23322=CIRCLE ( 'NONE', #20016, 0.5399999999999999245 ) ;
#23339=CARTESIAN_POINT ( 'NONE',  ( -0.01548846960707504251, -0.3772621329472741758, 0.3651003739303441131 ) ) ;
#23356=CARTESIAN_POINT ( 'NONE',  ( -0.04211812644076891321, 0.4433543613217477697, -0.1530385388104362199 ) ) ;
#23368=AXIS2_PLACEMENT_3D ( 'NONE', #7426, #3760, #524 ) ;
#23372=CARTESIAN_POINT ( 'NONE',  ( -0.04308745346420421451, 0.2425953941929087643, -0.4306799763758774602 ) ) ;
#23379=B_SPLINE_CURVE_WITH_KNOTS ( 'NONE', 3,
 ( #2040, #7594, #29608, #20169, #26745, #10900, #7988, #1854, #14180, #14369, #38854, #11097, #8202, #39274, #23258, #7793, #23472, #23657 ),
 .UNSPECIFIED., .F., .F.,
 ( 4, 2, 2, 2, 2, 2, 2, 2, 4 ),
 ( -0.002633528389679591110, -0.001975271857855645692, -0.001317015326031700274, -0.0006587587942077548567, -5.022623838094389392E-07, 0.0006577542694401359788, 0.001316010801264081397, 0.001974267333088026814, 0.002632523864911972232 ),
 .UNSPECIFIED. ) ;
#23389=CARTESIAN_POINT ( 'NONE',  ( 0.03662792686184425384, 0.04111994379180462789, 0.4792679903722379953 ) ) ;
#23390=CARTESIAN_POINT ( 'NONE',  ( -0.05268850283020126007, -0.2717122958104509767, -0.3818262463465889600 ) ) ;
#23393=CARTESIAN_POINT ( 'NONE',  ( 0.01548846960707511190, -0.5198120922912051745, -0.07362328916749329155 ) ) ;
#23396=CIRCLE ( 'NONE', #17469, 0.01499999999999995955 ) ;
#23398=DIMENSIONAL_EXPONENTS ( 1.000000000000000000, 0.000000000000000000, 0.000000000000000000, 0.000000000000000000, 0.000000000000000000, 0.000000000000000000, 0.000000000000000000 ) ;
#23402=CARTESIAN_POINT ( 'NONE',  ( 0.03643058821097343303, 0.08373535757664200829, 0.5050280785339766876 ) ) ;
#23409=DIRECTION ( 'NONE',  ( -1.654489825136719548E-31, 0.9510565162951568619, 0.3090169943749375703 ) ) ;
#23412=EDGE_CURVE ( 'NONE', #3229, #13737, #31658, .T. ) ;
#23426=CARTESIAN_POINT ( 'NONE',  ( 0.03672447062657525213, -0.4430265621404764209, 0.1868507191434652936 ) ) ;
#23434=CARTESIAN_POINT ( 'NONE',  ( 0.04154009738085462367, -0.2902754972779521547, -0.3700679770908125166 ) ) ;
#23437=CARTESIAN_POINT ( 'NONE',  ( 0.01899496522501941537, 0.3622296354306406285, 0.3730445619378072730 ) ) ;
#23446=CARTESIAN_POINT ( 'NONE',  ( -0.02242905165738659501, -0.2417642932583371762, 0.4517135660370446559 ) ) ;
#23452=SPHERICAL_SURFACE ( 'NONE', #31588, 0.01499999999999999944 ) ;
#23453=FACE_OUTER_BOUND ( 'NONE', #36248, .T. ) ;
#23466=SPHERICAL_SURFACE ( 'NONE', #37879, 0.01499999999999999944 ) ;
#23472=CARTESIAN_POINT ( 'NONE',  ( 0.01895884884825219455, 0.5124024296374549703, 0.08888335629180021957 ) ) ;
#23521=AXIS2_PLACEMENT_3D ( 'NONE', #31558, #31772, #26175 ) ;
#23535=EDGE_CURVE ( 'NONE', #16052, #26041, #19819, .T. ) ;
#23539=ORIENTED_EDGE ( 'NONE', *, *, #26401, .F. ) ;
#23544=EDGE_LOOP ( 'NONE', ( #15604, #38120, #40429 ) ) ;
#23554=CARTESIAN_POINT ( 'NONE',  ( -0.03877220711930485370, 0.4416859332762665402, -0.1784371778270208153 ) ) ;
#23569=CARTESIAN_POINT ( 'NONE',  ( -0.03674260963082443682, -0.4681940304452939516, -0.1092801147583400689 ) ) ;
#23578=CARTESIAN_POINT ( 'NONE',  ( -0.05283719472145156915, -0.03966590960886421519, -0.4666299489511761545 ) ) ;
#23580=CARTESIAN_POINT ( 'NONE',  ( -0.02238765564325697829, -0.2417679119117833453, -0.4518160092940294859 ) ) ;
#23581=VERTEX_POINT ( 'NONE', #29342 ) ;
#23585=CARTESIAN_POINT ( 'NONE',  ( -0.02953079040095652960, 0.3810518745593862167, -0.3687679460475775106 ) ) ;
#23597=CARTESIAN_POINT ( 'NONE',  ( -0.03650581953630641779, -0.2290855126858369062, -0.4575806651622373877 ) ) ;
#23610=CYLINDRICAL_SURFACE ( 'NONE', #25422, 0.5400000000000019229 ) ;
#23614=CARTESIAN_POINT ( 'NONE',  ( 0.03174060074381315766, -0.4701996045334360663, 0.2325360656122961167 ) ) ;
#23621=SPHERICAL_SURFACE ( 'NONE', #23861, 0.01499999999999999944 ) ;
#23622=EDGE_CURVE ( 'NONE', #1137, #29592, #32966, .T. ) ;
#23633=CARTESIAN_POINT ( 'NONE',  ( -0.05489899477340625528, -0.2921074789649947823, 0.3589041746640633246 ) ) ;
#23634=ORIENTED_EDGE ( 'NONE', *, *, #17491, .T. ) ;
#23639=FACE_OUTER_BOUND ( 'NONE', #49, .T. ) ;
#23640=CARTESIAN_POINT ( 'NONE',  ( 0.01899496522502858512, 0.2428513482851171745, -0.4597779644694632295 ) ) ;
#23648=DIRECTION ( 'NONE',  ( 0.9378410757839518164, -0.1072489841977738861, -0.3300784330442475545 ) ) ;
#23654=ORIENTED_EDGE ( 'NONE', *, *, #27391, .F. ) ;
#23655=CARTESIAN_POINT ( 'NONE',  ( 0.000000000000000000, 0.000000000000000000, 0.000000000000000000 ) ) ;
#23657=CARTESIAN_POINT ( 'NONE',  ( 0.01548846960712797240, 0.5203207976466739382, 0.08861466064782476393 ) ) ;
#23679=B_SPLINE_CURVE_WITH_KNOTS ( 'NONE', 3,
 ( #1322, #7452, #25590, #7052, #35036, #3777, #32348, #31751, #3570, #38932, #35253, #16138, #28870, #19426, #28676, #543, #20027, #25801 ),
 .UNSPECIFIED., .F., .F.,
 ( 4, 2, 2, 2, 2, 2, 2, 2, 4 ),
 ( -0.002633528389679722949, -0.001975271857855722454, -0.001317015326031721958, -0.0006587587942077214632, -5.022623837209680420E-07, 0.0006577542694402795272, 0.001316010801264280022, 0.001974267333088280084, 0.002632523864912281013 ),
 .UNSPECIFIED. ) ;
#23684=ORIENTED_EDGE ( 'NONE', *, *, #1446, .F. ) ;
#23689=CARTESIAN_POINT ( 'NONE',  ( 0.01548846960707524721, 0.000000000000000000, 0.000000000000000000 ) ) ;
#23724=DIRECTION ( 'NONE',  ( -0.3468893892380672250, 0.3199132558031694828, -0.8816593788961000211 ) ) ;
#23731=ORIENTED_EDGE ( 'NONE', *, *, #36298, .F. ) ;
#23739=AXIS2_PLACEMENT_3D ( 'NONE', #30901, #28221, #30708 ) ;
#23752=EDGE_CURVE ( 'NONE', #19390, #1288, #14553, .T. ) ;
#23754=CARTESIAN_POINT ( 'NONE',  ( 0.02953079040095673430, -0.5250338024619269905, -0.07436286310882420092 ) ) ;
#23760=CARTESIAN_POINT ( 'NONE',  ( -0.05269191099235819714, -0.4470515771378631431, -0.1405532101198447847 ) ) ;
#23761=AXIS2_PLACEMENT_3D ( 'NONE', #23949, #33387, #5191 ) ;
#23772=CARTESIAN_POINT ( 'NONE',  ( 0.02953079040094805374, 0.5250338024619489730, -0.07436286310882397887 ) ) ;
#23773=CARTESIAN_POINT ( 'NONE',  ( 0.1499999999999994671, 0.5203207976467936202, 0.08861466064782093366 ) ) ;
#23775=CARTESIAN_POINT ( 'NONE',  ( 0.01548846960707511190, -0.5198120922912051745, -0.07362328916749329155 ) ) ;
#23780=AXIS2_PLACEMENT_3D ( 'NONE', #40435, #12054, #14937 ) ;
#23783=CARTESIAN_POINT ( 'NONE',  ( 0.04293701532779510555, 0.3457382709204490090, 0.3536859687696371490 ) ) ;
#23805=ORIENTED_EDGE ( 'NONE', *, *, #40593, .T. ) ;
#23814=CARTESIAN_POINT ( 'NONE',  ( 0.02953079040095346608, -0.4684706630666200522, 0.2484463060367382847 ) ) ;
#23825=CARTESIAN_POINT ( 'NONE',  ( 0.05561310505367080687, 0.2541457526436888825, 0.3845267872006546961 ) ) ;
#23835=CARTESIAN_POINT ( 'NONE',  ( -0.05187277790672315675, -0.2620383623028431641, 0.3911539469301649752 ) ) ;
#23843=CARTESIAN_POINT ( 'NONE',  ( -0.05083665881509057127, 0.4630607685881610869, 0.09936361682460814748 ) ) ;
#23853=CARTESIAN_POINT ( 'NONE',  ( 0.01548846960712783535, -0.5203207976466778240, -0.08861466064782558272 ) ) ;
#23854=AXIS2_PLACEMENT_3D ( 'NONE', #25335, #31089, #31490 ) ;
#23855=ADVANCED_FACE ( 'NONE', ( #35213 ), #25354, .F. ) ;
#23861=AXIS2_PLACEMENT_3D ( 'NONE', #1821, #14337, #26900 ) ;
#23885=AXIS2_PLACEMENT_3D ( 'NONE', #34735, #7144, #34941 ) ;
#23918=CIRCLE ( 'NONE', #14024, 0.7750185148639454624 ) ;
#23920=DIRECTION ( 'NONE',  ( -4.410796239770424606E-15, -0.4393346272636315941, 0.8983234858819654223 ) ) ;
#23930=AXIS2_PLACEMENT_3D ( 'NONE', #16306, #9340, #22898 ) ;
#23932=EDGE_CURVE ( 'NONE', #16401, #33009, #20409, .T. ) ;
#23934=CARTESIAN_POINT ( 'NONE',  ( 0.04575106512774701484, -0.06504741310981120017, -0.4827780559048409637 ) ) ;
#23946=AXIS2_PLACEMENT_3D ( 'NONE', #21514, #27663, #24590 ) ;
#23949=CARTESIAN_POINT ( 'NONE',  ( 0.1499999999999994671, -0.5230810839623352138, -0.1699593469062213591 ) ) ;
#23954=CARTESIAN_POINT ( 'NONE',  ( -0.04047161733260127431, 0.4536038223829612082, -0.2133268955647374676 ) ) ;
#23958=CIRCLE ( 'NONE', #7503, 0.01499999999999995608 ) ;
#23967=CARTESIAN_POINT ( 'NONE',  ( 0.04293701532779490432, -0.4875995331660219478, -0.08291810260646698127 ) ) ;
#23971=CARTESIAN_POINT ( 'NONE',  ( -0.05634115714581421769, -0.4348133112253127486, -0.1467699930803220698 ) ) ;
#23978=AXIS2_PLACEMENT_3D ( 'NONE', #21922, #38137, #37739 ) ;
#23979=CARTESIAN_POINT ( 'NONE',  ( 0.1499999999999994671, 0.3688619771572926309, -0.3775276577326977523 ) ) ;
#23988=CARTESIAN_POINT ( 'NONE',  ( -0.04308745346420565087, -0.3346348984074261068, -0.3638093623074884486 ) ) ;
#23991=EDGE_CURVE ( 'NONE', #36862, #38078, #29590, .T. ) ;
#23996=CARTESIAN_POINT ( 'NONE',  ( 0.03654364704248850432, 0.2290829176602898198, 0.4574690890339227489 ) ) ;
#24003=CARTESIAN_POINT ( 'NONE',  ( -0.02953079040095693900, -0.3810518745593889922, -0.3687679460475752902 ) ) ;
#24006=ORIENTED_EDGE ( 'NONE', *, *, #3625, .T. ) ;
#24009=AXIS2_PLACEMENT_3D ( 'NONE', #5641, #27660, #3171 ) ;
#24046=EDGE_CURVE ( 'NONE', #23035, #15212, #13167, .T. ) ;
#24052=DIRECTION ( 'NONE',  ( 1.707404996040162391E-15, 0.4393346272636243222, -0.8983234858819689750 ) ) ;
#24053=CARTESIAN_POINT ( 'NONE',  ( -0.04293701532779600066, 0.3457382709204480653, -0.3536859687696375376 ) ) ;
#24056=EDGE_LOOP ( 'NONE', ( #11190, #18935, #26962 ) ) ;
#24059=DIRECTION ( 'NONE',  ( 0.000000000000000000, -0.9510565162951529761, 0.3090169943749491166 ) ) ;
#24065=CARTESIAN_POINT ( 'NONE',  ( -0.04154009738085463754, -0.2902754972779529319, 0.3700679770908128496 ) ) ;
#24072=DIRECTION ( 'NONE',  ( 1.000000000000000000, 2.280301054154495132E-31, -1.664003471950577689E-31 ) ) ;
#24076=DIRECTION ( 'NONE',  ( 1.702140497302373526E-12, -0.5877852522924708056, 0.8090169943749491166 ) ) ;
#24109=EDGE_CURVE ( 'NONE', #10925, #38396, #18390, .T. ) ;
#24119=EDGE_CURVE ( 'NONE', #30207, #3229, #20853, .T. ) ;
#24123=ADVANCED_FACE ( 'NONE', ( #38231 ), #17748, .T. ) ;
#24126=DIRECTION ( 'NONE',  ( 0.000000000000000000, -0.5877852522924906786, 0.8090169943749346837 ) ) ;
#24144=CARTESIAN_POINT ( 'NONE',  ( 0.05076679145661983777, -0.04886774829954456528, -0.4712599967968629233 ) ) ;
#24175=CARTESIAN_POINT ( 'NONE',  ( 0.05082303569918527469, -0.4330427793496154365, 0.1918498709088723442 ) ) ;
#24182=CARTESIAN_POINT ( 'NONE',  ( 0.06980746140711582837, 0.000000000000000000, 0.000000000000000000 ) ) ;
#24185=CIRCLE ( 'NONE', #23521, 0.01500000000000005496 ) ;
#24191=CARTESIAN_POINT ( 'NONE',  ( -0.04575334816097852142, -0.06504672743687492376, -0.4827724779829238311 ) ) ;
#24193=ORIENTED_EDGE ( 'NONE', *, *, #36156, .T. ) ;
#24194=CARTESIAN_POINT ( 'NONE',  ( -0.04154009738085499837, 0.2622554993748598129, 0.3904256972020302419 ) ) ;
#24195=CARTESIAN_POINT ( 'NONE',  ( 0.03674078017396018025, -0.04075419261117101122, 0.4790519037776401201 ) ) ;
#24196=CARTESIAN_POINT ( 'NONE',  ( 0.02872242845529722130, -0.4768947642620330329, -0.2371557650702024733 ) ) ;
#24199=CARTESIAN_POINT ( 'NONE',  ( 0.03303708955568378236, 0.5155567402493611562, 0.07470075307486020999 ) ) ;
#24200=DIRECTION ( 'NONE',  ( -0.3468893892380666699, 0.2594111197898833487, 0.9013177145509789767 ) ) ;
#24205=ORIENTED_EDGE ( 'NONE', *, *, #21435, .F. ) ;
#24208=CARTESIAN_POINT ( 'NONE',  ( -0.03309060444528710843, -0.5154120966056451314, 0.07470591001490139993 ) ) ;
#24210=SPHERICAL_SURFACE ( 'NONE', #23780, 0.01499999999999999944 ) ;
#24221=CARTESIAN_POINT ( 'NONE',  ( 0.1499999999999996336, -0.07651041855119578017, -0.5222379212568201146 ) ) ;
#24235=ORIENTED_EDGE ( 'NONE', *, *, #18962, .T. ) ;
#24238=CARTESIAN_POINT ( 'NONE',  ( -0.01548846960707524721, 0.000000000000000000, 0.000000000000000000 ) ) ;
#24246=ORIENTED_EDGE ( 'NONE', *, *, #19073, .T. ) ;
#24257=VERTEX_POINT ( 'NONE', #34949 ) ;
#24258=CARTESIAN_POINT ( 'NONE',  ( 0.06980746140711582837, -3.685538980774209949E-17, -0.1750000000000000167 ) ) ;
#24270=CARTESIAN_POINT ( 'NONE',  ( 0.03309057659885145108, 0.4608882367397874602, 0.2425133248663937369 ) ) ;
#24301=VERTEX_POINT ( 'NONE', #20541 ) ;
#24304=CARTESIAN_POINT ( 'NONE',  ( -0.05543910610524961646, -0.4446004295725691224, 0.1230574251923865076 ) ) ;
#24314=DIRECTION ( 'NONE',  ( 9.244463733058726621E-33, 0.4685245517976878160, 0.8834504764630419782 ) ) ;
#24319=CARTESIAN_POINT ( 'NONE',  ( 0.03174060074381968716, -0.2437182008228601648, 0.4645020220639594077 ) ) ;
#24324=CIRCLE ( 'NONE', #3951, 0.01499999999999995434 ) ;
#24328=CARTESIAN_POINT ( 'NONE',  ( 0.04047170147976490023, -0.06272069502581187339, -0.4973236590858508555 ) ) ;
#24338=EDGE_LOOP ( 'NONE', ( #2945, #6848, #6556, #937 ) ) ;
#24340=FACE_OUTER_BOUND ( 'NONE', #35289, .T. ) ;
#24344=CARTESIAN_POINT ( 'NONE',  ( -0.04762200653274207413, 0.4434980416368405898, -0.1892582844414349152 ) ) ;
#24347=DIRECTION ( 'NONE',  ( 1.000000000000000000, 1.799754070459507683E-12, -1.860523581402830585E-12 ) ) ;
#24356=DIRECTION ( 'NONE',  ( 0.000000000000000000, 0.9510565162951502005, -0.3090169943749580539 ) ) ;
#24358=CARTESIAN_POINT ( 'NONE',  ( -0.01548846960707545191, -0.5198120922912051745, -0.07362328916749329155 ) ) ;
#24366=ADVANCED_FACE ( 'NONE', ( #27523 ), #37454, .T. ) ;
#24378=CARTESIAN_POINT ( 'NONE',  ( -0.04285561529641568335, -0.07198636226547319716, -0.4895514295879473399 ) ) ;
#24380=ORIENTED_EDGE ( 'NONE', *, *, #5360, .T. ) ;
#24384=DIRECTION ( 'NONE',  ( -1.000000000000000000, -2.280301054154495132E-31, 1.664003471950577689E-31 ) ) ;
#24389=DIRECTION ( 'NONE',  ( -0.9378410757839554801, -0.1072489841977692648, -0.3300784330442382286 ) ) ;
#24390=CARTESIAN_POINT ( 'NONE',  ( -0.03309057659885163843, -0.3730661755626923370, -0.3633900220890627919 ) ) ;
#24402=EDGE_CURVE ( 'NONE', #23035, #9503, #9392, .T. ) ;
#24408=CIRCLE ( 'NONE', #5308, 0.01500000000000001159 ) ;
#24413=FACE_OUTER_BOUND ( 'NONE', #2185, .T. ) ;
#24418=DIRECTION ( 'NONE',  ( 1.000000000000000000, -1.023084414572551917E-11, -1.435532102222566415E-11 ) ) ;
#24420=CARTESIAN_POINT ( 'NONE',  ( -0.05186792262757213001, 0.2620061627190607423, 0.3911910583554848997 ) ) ;
#24428=DIRECTION ( 'NONE',  ( -1.000000000000000000, -2.341930812374887555E-31, 1.664003471950578127E-31 ) ) ;
#24439=CARTESIAN_POINT ( 'NONE',  ( 0.02881408050861173492, 0.2420347005671112106, -0.4354489374660193701 ) ) ;
#24448=ORIENTED_EDGE ( 'NONE', *, *, #19620, .T. ) ;
#24449=CARTESIAN_POINT ( 'NONE',  ( -0.03868264068766708724, 0.3066108573455319508, -0.3648330973802349497 ) ) ;
#24459=DIRECTION ( 'NONE',  ( -1.355854680848614260E-31, 3.330669073875470114E-16, 1.000000000000000000 ) ) ;
#24460=DIRECTION ( 'NONE',  ( 0.000000000000000000, -0.3090169943749502823, -0.9510565162951527540 ) ) ;
#24468=CARTESIAN_POINT ( 'NONE',  ( 0.02953079040095717839, 0.4684706630666118365, 0.2484463060367366194 ) ) ;
#24489=CARTESIAN_POINT ( 'NONE',  ( 0.1499999999999993561, 0.07651041855119031232, -0.5222379212568211138 ) ) ;
#24496=EDGE_LOOP ( 'NONE', ( #15684, #9623, #3336, #8628 ) ) ;
#24509=CARTESIAN_POINT ( 'NONE',  ( -0.05268850283020078823, -0.4471020566665147578, 0.1404229504685532148 ) ) ;
#24531=TOROIDAL_SURFACE ( 'NONE', #33702, 0.5250000000000000222, 0.01499999999999999944 ) ;
#24535=CARTESIAN_POINT ( 'NONE',  ( 0.05561375719525327166, -0.02040745343123889777, -0.4604703763991774834 ) ) ;
#24538=AXIS2_PLACEMENT_3D ( 'NONE', #8508, #34015, #31145 ) ;
#24540=VERTEX_POINT ( 'NONE', #11032 ) ;
#24555=CARTESIAN_POINT ( 'NONE',  ( -0.1499999999999996336, 0.000000000000000000, 0.000000000000000000 ) ) ;
#24562=DIRECTION ( 'NONE',  ( -2.682900528199994008E-31, 0.9510565162951504226, -0.3090169943749569437 ) ) ;
#24564=ADVANCED_FACE ( 'NONE', ( #20485 ), #10827, .T. ) ;
#24568=DIRECTION ( 'NONE',  ( 1.000000000000000000, 2.280301054154495132E-31, -1.664003471950577689E-31 ) ) ;
#24572=CIRCLE ( 'NONE', #40319, 0.01499999999999996302 ) ;
#24579=AXIS2_PLACEMENT_3D ( 'NONE', #27334, #33077, #20758 ) ;
#24582=CARTESIAN_POINT ( 'NONE',  ( -0.02872242845530496164, -0.3729171224323663547, -0.3802687114177501493 ) ) ;
#24583=AXIS2_PLACEMENT_3D ( 'NONE', #35488, #10407, #12898 ) ;
#24584=EDGE_CURVE ( 'NONE', #17702, #12964, #1793, .T. ) ;
#24588=FACE_OUTER_BOUND ( 'NONE', #22087, .T. ) ;
#24589=EDGE_CURVE ( 'NONE', #26219, #37479, #17773, .T. ) ;
#24590=DIRECTION ( 'NONE',  ( 1.000000000000000000, 0.000000000000000000, 0.000000000000000000 ) ) ;
#24592=CARTESIAN_POINT ( 'NONE',  ( -0.05187277790672318450, -0.01792103310036803968, -0.4704724753798314452 ) ) ;
#24598=CARTESIAN_POINT ( 'NONE',  ( 0.04157078424165364799, -0.01703670724029039338, 0.4699541233906588955 ) ) ;
#24599=CARTESIAN_POINT ( 'NONE',  ( 0.03478489236951080865, -0.4639981600178390564, -0.2267640475915320142 ) ) ;
#24602=CARTESIAN_POINT ( 'NONE',  ( 0.04229883635638006373, 0.4470233673486206927, 0.1406638142521503265 ) ) ;
#24604=CARTESIAN_POINT ( 'NONE',  ( -0.05634307799789443211, -0.2614070397638467713, -0.3772863199289407388 ) ) ;
#24605=ORIENTED_EDGE ( 'NONE', *, *, #4471, .T. ) ;
#24610=ADVANCED_FACE ( 'NONE', ( #29348 ), #21146, .T. ) ;
#24619=EDGE_CURVE ( 'NONE', #10835, #15637, #33540, .T. ) ;
#24624=DIRECTION ( 'NONE',  ( -1.355854680848614260E-31, 3.330669073875470114E-16, 1.000000000000000000 ) ) ;
#24635=CARTESIAN_POINT ( 'NONE',  ( -0.03877220711930155078, 0.3061923002804438076, 0.3649281646214391772 ) ) ;
#24641=CARTESIAN_POINT ( 'NONE',  ( 0.02953079040095704308, -0.09152108205201929525, 0.5223162075576431862 ) ) ;
#24648=CARTESIAN_POINT ( 'NONE',  ( 0.1499999999999989120, -0.3688619771572964612, -0.3775276577326955874 ) ) ;
#24649=EDGE_CURVE ( 'NONE', #15212, #15646, #97, .T. ) ;
#24650=AXIS2_PLACEMENT_3D ( 'NONE', #20084, #592, #3818 ) ;
#24658=DIRECTION ( 'NONE',  ( -0.3468893892380665589, 0.7396492646828625173, -0.5767033179097742490 ) ) ;
#24673=ORIENTED_EDGE ( 'NONE', *, *, #34287, .T. ) ;
#24682=AXIS2_PLACEMENT_3D ( 'NONE', #10638, #39426, #17023 ) ;
#24694=CARTESIAN_POINT ( 'NONE',  ( 0.01548846960721252282, 0.2450655194478999765, 0.4674710490746267211 ) ) ;
#24697=EDGE_LOOP ( 'NONE', ( #28337, #14558, #3646, #26860 ) ) ;
#24710=CARTESIAN_POINT ( 'NONE',  ( 0.03868649100028155596, 0.4624880946332495801, -0.1149381524902354373 ) ) ;
#24716=DIRECTION ( 'NONE',  ( 1.000000000000000000, -1.693379103678898785E-12, 2.967165974375456995E-13 ) ) ;
#24723=CARTESIAN_POINT ( 'NONE',  ( 0.01548846960707497486, -0.5198120922912106145, -0.07362328916748536733 ) ) ;
#24735=FACE_OUTER_BOUND ( 'NONE', #349, .T. ) ;
#24744=CARTESIAN_POINT ( 'NONE',  ( 0.05279905671744771628, 0.03987410640504355369, -0.4667149812770573503 ) ) ;
#24755=ORIENTED_EDGE ( 'NONE', *, *, #23622, .F. ) ;
#24759=DIRECTION ( 'NONE',  ( 0.000000000000000000, 0.000000000000000000, 1.000000000000000000 ) ) ;
#24762=ORIENTED_EDGE ( 'NONE', *, *, #27831, .T. ) ;
#24770=CARTESIAN_POINT ( 'NONE',  ( -0.05634307799789442517, -0.2780413953411582928, 0.3652007531760607661 ) ) ;
#24777=CARTESIAN_POINT ( 'NONE',  ( 0.02953079040095673430, -0.2329676531120485339, -0.4763574306556319637 ) ) ;
#24778=EDGE_CURVE ( 'NONE', #6931, #33948, #36191, .T. ) ;
#24798=PLANE ( 'NONE',  #79 ) ;
#24801=CARTESIAN_POINT ( 'NONE',  ( -0.04574984450155245713, 0.06505050184193394980, -0.4827809015761244105 ) ) ;
#24803=EDGE_LOOP ( 'NONE', ( #4491, #4140, #10721 ) ) ;
#24806=CARTESIAN_POINT ( 'NONE',  ( 0.05201782277453272096, -0.01807851807932046515, 0.4701313241416045230 ) ) ;
#24809=CARTESIAN_POINT ( 'NONE',  ( 0.04285534776242382049, 0.4878382857517603588, 0.08280911155782964828 ) ) ;
#24811=CARTESIAN_POINT ( 'NONE',  ( 0.02953079040095420854, -0.3810518745593896028, -0.3687679460475819515 ) ) ;
#24817=CARTESIAN_POINT ( 'NONE',  ( -0.05283710938260965245, -0.4315340639268090972, 0.1819215676045965735 ) ) ;
#24832=DIRECTION ( 'NONE',  ( -1.000000000000000000, -2.341930812374887555E-31, 1.664003471950578127E-31 ) ) ;
#24833=ADVANCED_FACE ( 'NONE', ( #15722 ), #28294, .T. ) ;
#24835=CARTESIAN_POINT ( 'NONE',  ( -0.03672309138970067388, 0.2485858928251931943, 0.4115746274616670641 ) ) ;
#24838=CARTESIAN_POINT ( 'NONE',  ( 0.01548846960706657880, 0.2450655194479920418, 0.4674710490749448555 ) ) ;
#24844=DIRECTION ( 'NONE',  ( 0.000000000000000000, 0.5877852522924756906, 0.8090169943749454529 ) ) ;
#24855=CARTESIAN_POINT ( 'NONE',  ( 0.04047043078435860058, 0.3430608037303070068, -0.3654822131371353033 ) ) ;
#24857=DIRECTION ( 'NONE',  ( 1.000000000000000000, 2.280301054154495132E-31, -1.664003471950577689E-31 ) ) ;
#24867=CYLINDRICAL_SURFACE ( 'NONE', #25295, 0.01500000000000005669 ) ;
#24870=VERTEX_POINT ( 'NONE', #741 ) ;
#24890=DIRECTION ( 'NONE',  ( 0.000000000000000000, 0.9510565162951414298, -0.3090169943749848658 ) ) ;
#24892=CARTESIAN_POINT ( 'NONE',  ( -0.02953079040095693900, -0.3810518745593846068, 0.3687679460475796756 ) ) ;
#24895=ADVANCED_FACE ( 'NONE', ( #32771 ), #8575, .T. ) ;
#24896=ORIENTED_EDGE ( 'NONE', *, *, #1491, .T. ) ;
#24899=ORIENTED_EDGE ( 'NONE', *, *, #35019, .F. ) ;
#24906=CARTESIAN_POINT ( 'NONE',  ( 0.04154009738085467918, 0.4416556227939101298, -0.1617111092119887517 ) ) ;
#24917=CARTESIAN_POINT ( 'NONE',  ( -0.03170752374382796585, -0.4816921673044493590, 0.09938322573836505525 ) ) ;
#24932=CARTESIAN_POINT ( 'NONE',  ( -0.02953079040095689042, 0.5250338024619264354, 0.07436286310882508910 ) ) ;
#24934=CARTESIAN_POINT ( 'NONE',  ( 0.04293317454820651941, -0.3457449726441599314, 0.3536934093827153180 ) ) ;
#24945=ORIENTED_EDGE ( 'NONE', *, *, #35574, .F. ) ;
#24969=CARTESIAN_POINT ( 'NONE',  ( -0.05489899477340599854, -0.02536133381296585068, 0.4620560448753001093 ) ) ;
#24975=ORIENTED_EDGE ( 'NONE', *, *, #30010, .T. ) ;
#24976=CARTESIAN_POINT ( 'NONE',  ( -0.03174036153405046523, 0.07585545617081057568, -0.5190446117378511026 ) ) ;
#24981=EDGE_CURVE ( 'NONE', #13737, #1061, #10930, .T. ) ;
#24988=CARTESIAN_POINT ( 'NONE',  ( 0.03674260963082216086, 0.4430101671189279333, 0.1867880763203807470 ) ) ;
#24990=CARTESIAN_POINT ( 'NONE',  ( 0.05279905671744909018, -0.2420693533014104115, -0.4010177630757500444 ) ) ;
#25006=CARTESIAN_POINT ( 'NONE',  ( -0.02953079040095603694, 0.3810518745593876599, -0.3687679460475788429 ) ) ;
#25008=CARTESIAN_POINT ( 'NONE',  ( 0.1499999999999993561, -0.3772621329472632401, 0.3651003739303507190 ) ) ;
#25011=AXIS2_PLACEMENT_3D ( 'NONE', #4434, #993, #26868 ) ;
#25016=CARTESIAN_POINT ( 'NONE',  ( -0.05615703521554987060, 0.2616264896058755340, 0.3776298641847850579 ) ) ;
#25040=B_SPLINE_CURVE_WITH_KNOTS ( 'NONE', 3,
 ( #14102, #11821, #21095, #23783, #20291, #4614, #11427, #17602, #30343, #29955, #36302, #29733, #14714, #39210, #17395, #23996, #11031, #26867 ),
 .UNSPECIFIED., .F., .F.,
 ( 4, 2, 2, 2, 2, 2, 2, 2, 4 ),
 ( -0.003133633995111204627, -0.002350221109836722611, -0.001566808224562240811, -0.0007833953392877642148, 1.754598671259779974E-08, 0.0007834304312611898441, 0.001566843316535666657, 0.002350256201810143469, 0.003133669087084620282 ),
 .UNSPECIFIED. ) ;
#25044=ADVANCED_FACE ( 'NONE', ( #24340 ), #39545, .T. ) ;
#25050=DIRECTION ( 'NONE',  ( 1.000000000000000000, 2.280301054154495132E-31, -1.664003471950577689E-31 ) ) ;
#25054=ORIENTED_EDGE ( 'NONE', *, *, #20595, .T. ) ;
#25076=CARTESIAN_POINT ( 'NONE',  ( -0.01548846960688968731, -0.2306506793135497668, -0.4716198300885139361 ) ) ;
#25086=EDGE_LOOP ( 'NONE', ( #4339, #4834, #16810, #26428 ) ) ;
#25090=CARTESIAN_POINT ( 'NONE',  ( -0.01548846960688914087, 0.2306506793135502942, 0.4716198300885117156 ) ) ;
#25091=CARTESIAN_POINT ( 'NONE',  ( 0.01895494625228208441, 0.2428766181966295346, 0.4598657641708832067 ) ) ;
#25092=EDGE_CURVE ( 'NONE', #16637, #33948, #6603, .T. ) ;
#25133=CARTESIAN_POINT ( 'NONE',  ( -0.05561375719525295941, 0.4316271021131496410, 0.1617018132803555996 ) ) ;
#25141=CIRCLE ( 'NONE', #6064, 0.5302738246768090580 ) ;
#25159=CARTESIAN_POINT ( 'NONE',  ( 0.01548846960707528191, 0.3880410510314791783, 0.3755318131854940567 ) ) ;
#25168=CARTESIAN_POINT ( 'NONE',  ( 0.05634307799789257248, -0.4332460723641358147, 0.1515798417490696048 ) ) ;
#25170=ADVANCED_FACE ( 'NONE', ( #5603 ), #2536, .F. ) ;
#25180=CARTESIAN_POINT ( 'NONE',  ( -0.05078493045284415697, 0.04880252970040156041, 0.4712186791567239408 ) ) ;
#25193=AXIS2_PLACEMENT_3D ( 'NONE', #16034, #22022, #455 ) ;
#25197=CARTESIAN_POINT ( 'NONE',  ( 0.04308745346419525640, 0.4494111352305708018, 0.2058334250444144586 ) ) ;
#25199=CARTESIAN_POINT ( 'NONE',  ( 0.04157143636675652426, -0.2900120080285103485, -0.3701876636500650575 ) ) ;
#25200=VERTEX_POINT ( 'NONE', #2127 ) ;
#25204=CARTESIAN_POINT ( 'NONE',  ( 0.05082294681498979866, 0.04864283519431678721, 0.4711332289091949566 ) ) ;
#25207=DIRECTION ( 'NONE',  ( -1.000000000000000000, -2.280301054154495132E-31, 1.664003471950577689E-31 ) ) ;
#25213=CARTESIAN_POINT ( 'NONE',  ( -0.05543910610524985239, 0.2873579635174380864, -0.3608851239303206282 ) ) ;
#25217=DIRECTION ( 'NONE',  ( -0.3515883117872521946, 3.118021572908016454E-16, 0.9361547195921140485 ) ) ;
#25222=AXIS2_PLACEMENT_3D ( 'NONE', #35557, #37848, #464 ) ;
#25223=CARTESIAN_POINT ( 'NONE',  ( -0.04087116408467122985, 0.2940498268759185185, 0.3688792544161150211 ) ) ;
#25235=DIRECTION ( 'NONE',  ( 1.000000000000000000, -1.799754070459521415E-12, 1.860523581402820487E-12 ) ) ;
#25246=CARTESIAN_POINT ( 'NONE',  ( 0.02242828275838930699, 0.3548975010106716343, -0.3695194593235469060 ) ) ;
#25268=ORIENTED_EDGE ( 'NONE', *, *, #3396, .F. ) ;
#25272=CARTESIAN_POINT ( 'NONE',  ( 0.1499999999999990508, -0.4770632572900511681, -0.2530032579707427454 ) ) ;
#25279=EDGE_CURVE ( 'NONE', #27922, #10402, #9512, .T. ) ;
#25281=CARTESIAN_POINT ( 'NONE',  ( 0.05083665881509029372, 0.3162195626322004127, -0.3525671453250072140 ) ) ;
#25285=AXIS2_PLACEMENT_3D ( 'NONE', #14833, #24716, #2074 ) ;
#25287=EDGE_CURVE ( 'NONE', #33332, #33486, #22756, .T. ) ;
#25295=AXIS2_PLACEMENT_3D ( 'NONE', #28146, #12311, #18070 ) ;
#25303=ORIENTED_EDGE ( 'NONE', *, *, #34382, .F. ) ;
#25304=ADVANCED_FACE ( 'NONE', ( #11085 ), #11496, .T. ) ;
#25308=CARTESIAN_POINT ( 'NONE',  ( 0.03662792686184443425, 0.3149733899719660002, 0.3635662525351497365 ) ) ;
#25312=ORIENTED_EDGE ( 'NONE', *, *, #9781, .F. ) ;
#25327=CARTESIAN_POINT ( 'NONE',  ( -0.02872242845530427816, -0.4768947642620218197, 0.2371557650701859032 ) ) ;
#25335=CARTESIAN_POINT ( 'NONE',  ( 0.01548846960703768524, 0.09061086148575155097, -0.5171215251571049665 ) ) ;
#25343=CARTESIAN_POINT ( 'NONE',  ( 0.03170953572519073088, -0.3312786565686222096, 0.3635309226454363496 ) ) ;
#25345=FACE_OUTER_BOUND ( 'NONE', #35120, .T. ) ;
#25348=CARTESIAN_POINT ( 'NONE',  ( -0.03672447062657657052, 0.4430265621404759213, 0.1868507191434773673 ) ) ;
#25350=AXIS2_PLACEMENT_3D ( 'NONE', #5575, #11955, #9828 ) ;
#25352=EDGE_CURVE ( 'NONE', #30159, #20340, #30283, .T. ) ;
#25354=CYLINDRICAL_SURFACE ( 'NONE', #40186, 0.08139150547213672149 ) ;
#25379=DIRECTION ( 'NONE',  ( 1.000000000000000000, 2.280301054154495132E-31, -1.664003471950577689E-31 ) ) ;
#25386=DIRECTION ( 'NONE',  ( 0.000000000000000000, -0.8834504764629538265, -0.4685245517978538499 ) ) ;
#25392=CARTESIAN_POINT ( 'NONE',  ( 0.04154009738085429754, -0.4523583096281913463, -0.1287716261385816463 ) ) ;
#25400=CARTESIAN_POINT ( 'NONE',  ( -0.03478556507500938505, 0.07228131100493534467, 0.5113607228826224649 ) ) ;
#25403=FACE_BOUND ( 'NONE', #19559, .T. ) ;
#25406=CIRCLE ( 'NONE', #493, 0.01500000000000005496 ) ;
#25411=DIRECTION ( 'NONE',  ( 0.000000000000000000, -0.9901182710308679136, 0.1402348365094949756 ) ) ;
#25415=CARTESIAN_POINT ( 'NONE',  ( 0.03877220711929791480, 0.4416859332762684276, 0.1784371778270431863 ) ) ;
#25417=CARTESIAN_POINT ( 'NONE',  ( 0.04157078424165335656, -0.2624491172974833808, -0.3902147976630872539 ) ) ;
#25419=CARTESIAN_POINT ( 'NONE',  ( -0.03664605387828200056, 0.2484618661253114036, -0.4118464167359224271 ) ) ;
#25422=AXIS2_PLACEMENT_3D ( 'NONE', #14325, #36124, #7932 ) ;
#25424=ORIENTED_EDGE ( 'NONE', *, *, #4146, .T. ) ;
#25435=CARTESIAN_POINT ( 'NONE',  ( -0.05252359774140038379, 0.2683439431814198528, -0.3847367734645201209 ) ) ;
#25437=CARTESIAN_POINT ( 'NONE',  ( -0.01899468245561210245, -0.4667220838189795051, -0.2292241428221102884 ) ) ;
#25439=LINE ( 'NONE', #28718, #9565 ) ;
#25444=CARTESIAN_POINT ( 'NONE',  ( 0.03174060074382212965, 0.4701996045334482233, -0.2325360656123031111 ) ) ;
#25454=FACE_OUTER_BOUND ( 'NONE', #4286, .T. ) ;
#25458=DIRECTION ( 'NONE',  ( 0.000000000000000000, 0.8834504764630464191, -0.4685245517976792673 ) ) ;
#25461=CARTESIAN_POINT ( 'NONE',  ( 0.06980746140711582837, 5.828670879282072084E-17, 0.1749999999999999889 ) ) ;
#25473=EDGE_LOOP ( 'NONE', ( #12706, #6378 ) ) ;
#25482=CARTESIAN_POINT ( 'NONE',  ( 0.02953079040095700838, 0.3810518745593862167, -0.3687679460475775106 ) ) ;
#25489=SPHERICAL_SURFACE ( 'NONE', #39567, 0.01499999999999999944 ) ;
#25502=ORIENTED_EDGE ( 'NONE', *, *, #36182, .F. ) ;
#25504=ORIENTED_EDGE ( 'NONE', *, *, #4202, .T. ) ;
#25505=CARTESIAN_POINT ( 'NONE',  ( -0.03868649100028202781, 0.03360400204099593668, 0.4753701585314237255 ) ) ;
#25506=CARTESIAN_POINT ( 'NONE',  ( 0.02869942827333547136, 0.3396431753871657078, 0.3648167270360635484 ) ) ;
#25508=DIRECTION ( 'NONE',  ( -1.000000000000000000, -2.341930812374887555E-31, 1.664003471950578127E-31 ) ) ;
#25509=ORIENTED_EDGE ( 'NONE', *, *, #6197, .T. ) ;
#25510=ADVANCED_FACE ( 'NONE', ( #34298 ), #5499, .T. ) ;
#25516=DIRECTION ( 'NONE',  ( -1.355854680848614260E-31, 3.330669073875470114E-16, 1.000000000000000000 ) ) ;
#25534=DIRECTION ( 'NONE',  ( -1.355854680848614260E-31, 3.330669073875470114E-16, 1.000000000000000000 ) ) ;
#25540=CARTESIAN_POINT ( 'NONE',  ( 0.02881195911414956984, -0.3393447726770147943, 0.3647551865608084642 ) ) ;
#25545=CARTESIAN_POINT ( 'NONE',  ( -0.04575185649131228993, 0.4792489163483339421, 0.08731931755212994639 ) ) ;
#25551=CYLINDRICAL_SURFACE ( 'NONE', #17815, 0.5399999999999999245 ) ;
#25559=EDGE_CURVE ( 'NONE', #15099, #29592, #37499, .T. ) ;
#25576=ORIENTED_EDGE ( 'NONE', *, *, #24046, .F. ) ;
#25579=CARTESIAN_POINT ( 'NONE',  ( 0.05561176441985648394, -0.4316390549698289059, 0.1616802657107465069 ) ) ;
#25590=CARTESIAN_POINT ( 'NONE',  ( -0.02235124290213108197, 0.4612278572487595873, -0.2234747101372520361 ) ) ;
#25591=CARTESIAN_POINT ( 'NONE',  ( -0.04308745346420495698, 0.05688354191225430956, 0.4910214150057473081 ) ) ;
#25593=( BOUNDED_SURFACE ( )  B_SPLINE_SURFACE ( 3, 2, ( 
 ( #4662, #7568, #37125 ),
 ( #33841, #26721, #39041 ),
 ( #13735, #40194, #20337 ),
 ( #33069, #10659, #26508 ),
 ( #29392, #11072, #39250 ),
 ( #19922, #17238, #4283 ),
 ( #26302, #23230, #38827 ),
 ( #18196, #1236, #23633 ),
 ( #36151, #16850, #7960 ),
 ( #4875, #20535, #2566 ),
 ( #35755, #7770, #20143 ),
 ( #29787, #17446, #29998 ),
 ( #39442, #32858, #15101 ),
 ( #32669, #23835, #17041 ),
 ( #1629, #1831, #4475 ),
 ( #29580, #14347, #11267 ),
 ( #36911, #1424, #8721 ),
 ( #13938, #21300, #5642 ),
 ( #30746, #35963, #10873 ),
 ( #23446, #27662, #12027 ),
 ( #15918, #31164, #6037 ),
 ( #15526, #31366, #18389 ) ),
 .UNSPECIFIED., .F., .F., .F. ) 
 B_SPLINE_SURFACE_WITH_KNOTS ( ( 4, 2, 2, 2, 2, 2, 2, 2, 2, 2, 4 ),
 ( 3, 3 ),
 ( 0.002013519961495848290, 0.002780892266055755638, 0.003548264570615663419, 0.004315636875175571201, 0.004699323027455524875, 0.005083009179735478549, 0.005466695332015433090, 0.005850381484295386764, 0.006617753788855294111, 0.007385126093415201459, 0.008152498397975108807 ),
 ( 0.000000000000000000, 1.000000000000000000 ),
 .UNSPECIFIED. ) 
 GEOMETRIC_REPRESENTATION_ITEM ( )  RATIONAL_B_SPLINE_SURFACE ( (
 ( 1.000000000000000000, 0.7283825911960400967, 1.000000000000000000),
 ( 1.000000000000000000, 0.7404375345926941243, 1.000000000000000000),
 ( 1.000000000000000000, 0.7521483142436122815, 1.000000000000000000),
 ( 1.000000000000000000, 0.7744460733776301620, 1.000000000000000000),
 ( 1.000000000000000000, 0.7845612039380656100, 1.000000000000000000),
 ( 1.000000000000000000, 0.8022035258263469082, 1.000000000000000000),
 ( 1.000000000000000000, 0.8093965293321139232, 1.000000000000000000),
 ( 1.000000000000000000, 0.8169028692725751606, 1.000000000000000000),
 ( 1.000000000000000000, 0.8188329634862675510, 1.000000000000000000),
 ( 1.000000000000000000, 0.8214004505364708164, 1.000000000000000000),
 ( 1.000000000000000000, 0.8220602406261015016, 1.000000000000000000),
 ( 1.000000000000000000, 0.8220736605435605693, 1.000000000000000000),
 ( 1.000000000000000000, 0.8214126668415207000, 1.000000000000000000),
 ( 1.000000000000000000, 0.8188520474558780293, 1.000000000000000000),
 ( 1.000000000000000000, 0.8169545908333755158, 1.000000000000000000),
 ( 1.000000000000000000, 0.8094771004220964183, 1.000000000000000000),
 ( 1.000000000000000000, 0.8022723753809752889, 1.000000000000000000),
 ( 1.000000000000000000, 0.7845733350635248904, 1.000000000000000000),
 ( 1.000000000000000000, 0.7744472902493149125, 1.000000000000000000),
 ( 1.000000000000000000, 0.7522916829163579511, 1.000000000000000000),
 ( 1.000000000000000000, 0.7403553004665739401, 1.000000000000000000),
 ( 1.000000000000000000, 0.7283825911960407629, 1.000000000000000000) ) ) 
 REPRESENTATION_ITEM ( '' )  SURFACE ( )  );
#25602=EDGE_LOOP ( 'NONE', ( #1383, #7267, #40199, #23805 ) ) ;
#25603=DIRECTION ( 'NONE',  ( 9.244463733058732095E-32, -0.1402348365094961968, -0.9901182710308678026 ) ) ;
#25607=CARTESIAN_POINT ( 'NONE',  ( 0.04947837552028769292, 0.4418396724781423202, 0.1804413675089291402 ) ) ;
#25613=ORIENTED_EDGE ( 'NONE', *, *, #4117, .T. ) ;
#25624=CARTESIAN_POINT ( 'NONE',  ( -0.05561176441985807989, 0.2541700551350232762, 0.3845131534397769890 ) ) ;
#25634=AXIS2_PLACEMENT_3D ( 'NONE', #8231, #36810, #27573 ) ;
#25635=CARTESIAN_POINT ( 'NONE',  ( 0.04946426091937942970, 0.4635716124040155650, -0.1136627969334498417 ) ) ;
#25638=CARTESIAN_POINT ( 'NONE',  ( 0.04230188431063452298, 0.008729788072061312257, 0.4686063437799718456 ) ) ;
#25651=CARTESIAN_POINT ( 'NONE',  ( 0.01548846960707511190, -0.5346638663566692928, 0.07572681171513533094 ) ) ;
#25675=DIRECTION ( 'NONE',  ( 0.000000000000000000, -0.9510565162951545304, -0.3090169943749443426 ) ) ;
#25684=DIRECTION ( 'NONE',  ( 0.3468893892380646715, 0.2594111197898561483, -0.9013177145509876365 ) ) ;
#25687=DIRECTION ( 'NONE',  ( 0.000000000000000000, 3.330669073875470114E-16, 1.000000000000000000 ) ) ;
#25688=CARTESIAN_POINT ( 'NONE',  ( -0.01548846960707463312, 0.2306506793134060762, 0.4716198300880322658 ) ) ;
#25702=DIRECTION ( 'NONE',  ( 1.000000000000000000, 0.000000000000000000, 0.000000000000000000 ) ) ;
#25705=FACE_OUTER_BOUND ( 'NONE', #6270, .T. ) ;
#25722=CARTESIAN_POINT ( 'NONE',  ( -0.04154009738085504000, 0.01731731106881310295, -0.4700109389422700845 ) ) ;
#25732=CARTESIAN_POINT ( 'NONE',  ( 0.03650581953630612636, 0.5059763899182371238, 0.07647306779615405115 ) ) ;
#25736=AXIS2_PLACEMENT_3D ( 'NONE', #16693, #19769, #38283 ) ;
#25737=CARTESIAN_POINT ( 'NONE',  ( 0.04762035657658286042, -0.3170509070583802935, 0.3633072608571672468 ) ) ;
#25738=ADVANCED_FACE ( 'NONE', ( #23193 ), #38786, .T. ) ;
#25746=CARTESIAN_POINT ( 'NONE',  ( -0.05561310505367114687, 0.4442420632723341201, 0.1228816621031162265 ) ) ;
#25756=AXIS2_PLACEMENT_3D ( 'NONE', #1260, #13579, #10080 ) ;
#25768=PRODUCT_DEFINITION ( 'UNKNOWN', '', #30575, #22066 ) ;
#25782=DIRECTION ( 'NONE',  ( 0.9378410757839514833, 0.2807814858886687470, 0.2039996905746478406 ) ) ;
#25786=CARTESIAN_POINT ( 'NONE',  ( 0.03654364704248813656, -0.5058694728073483970, 0.07650507870000912425 ) ) ;
#25795=AXIS2_PLACEMENT_3D ( 'NONE', #9071, #37870, #6782 ) ;
#25801=CARTESIAN_POINT ( 'NONE',  ( -0.01548846960712776770, 0.5203207976466729390, -0.08861466064782422269 ) ) ;
#25803=CARTESIAN_POINT ( 'NONE',  ( -0.05138886601528163539, 0.02227547295149007178, 0.4715784802958499777 ) ) ;
#25809=CARTESIAN_POINT ( 'NONE',  ( 0.01548846960707511190, -0.09061086148576411037, -0.5171215251571027460 ) ) ;
#25813=DIRECTION ( 'NONE',  ( 0.000000000000000000, -0.5877852522924708056, 0.8090169943749491166 ) ) ;
#25819=CARTESIAN_POINT ( 'NONE',  ( 0.04285427992854216883, -0.2295125098185414325, -0.4383721679652327619 ) ) ;
#25828=CYLINDRICAL_SURFACE ( 'NONE', #18954, 0.08139150547213669373 ) ;
#25835=CARTESIAN_POINT ( 'NONE',  ( -0.03309057659885149272, 0.3730661755626945020, 0.3633900220890601274 ) ) ;
#25842=EDGE_CURVE ( 'NONE', #38396, #13846, #9975, .T. ) ;
#25848=CARTESIAN_POINT ( 'NONE',  ( 0.03474878377841050109, 0.4640666366555413203, -0.2268437812334264392 ) ) ;
#25866=VECTOR ( 'NONE', #8100, 39.37007874015748143 ) ;
#25884=ORIENTED_EDGE ( 'NONE', *, *, #14670, .T. ) ;
#25900=AXIS2_PLACEMENT_3D ( 'NONE', #16076, #22259, #28620 ) ;
#25917=VERTEX_POINT ( 'NONE', #2785 ) ;
#25920=AXIS2_PLACEMENT_3D ( 'NONE', #16384, #28925, #13300 ) ;
#25923=CARTESIAN_POINT ( 'NONE',  ( 0.01548846960703768524, -0.2306506793134120714, -0.4716198300880298233 ) ) ;
#25951=CIRCLE ( 'NONE', #35790, 0.5400000000000012568 ) ;
#25954=CIRCLE ( 'NONE', #23978, 0.01500000000000004628 ) ;
#25955=DIRECTION ( 'NONE',  ( 0.000000000000000000, 0.1725921171159214285, -0.9849933812515919707 ) ) ;
#25959=CARTESIAN_POINT ( 'NONE',  ( 0.05561375719525293859, -0.2541477197272140054, 0.3845235600768915352 ) ) ;
#25965=DIRECTION ( 'NONE',  ( 1.000000000000000000, 2.341930812374887555E-31, -1.664003471950578127E-31 ) ) ;
#25980=ORIENTED_EDGE ( 'NONE', *, *, #26252, .T. ) ;
#25994=DIRECTION ( 'NONE',  ( 1.000000000000000000, 2.341930812374887555E-31, -1.664003471950578127E-31 ) ) ;
#26003=AXIS2_PLACEMENT_3D ( 'NONE', #30982, #37163, #40642 ) ;
#26004=CARTESIAN_POINT ( 'NONE',  ( 0.02869712619511970847, -0.4519224903895654455, -0.2102851490355770736 ) ) ;
#26014=AXIS2_PLACEMENT_3D ( 'NONE', #16671, #6788, #4509 ) ;
#26015=DIRECTION ( 'NONE',  ( 0.000000000000000000, 0.7185945389471846134, -0.6954292836768403152 ) ) ;
#26023=VERTEX_POINT ( 'NONE', #8536 ) ;
#26029=CARTESIAN_POINT ( 'NONE',  ( -0.05186792262757158878, 0.4530091620765398508, -0.1282979832840799583 ) ) ;
#26041=VERTEX_POINT ( 'NONE', #2496 ) ;
#26055=CARTESIAN_POINT ( 'NONE',  ( 0.05269111014006343241, 0.4484844745756971784, -0.1361491033660635341 ) ) ;
#26056=CIRCLE ( 'NONE', #21453, 0.01500000000000003240 ) ;
#26067=CARTESIAN_POINT ( 'NONE',  ( -0.01548846960721259221, -0.5203207976464859774, -0.08861466064783186936 ) ) ;
#26096=DIRECTION ( 'NONE',  ( 2.686534417925922091E-31, -0.5877852522924700285, 0.8090169943749496717 ) ) ;
#26104=CARTESIAN_POINT ( 'NONE',  ( -0.01548846960707517956, -0.4638115001431016848, -0.2459753896937850459 ) ) ;
#26105=CIRCLE ( 'NONE', #40526, 0.01499999999999994914 ) ;
#26116=CARTESIAN_POINT ( 'NONE',  ( 0.05634402396114371325, 0.2613837787620694186, 0.3773006586902090675 ) ) ;
#26129=CARTESIAN_POINT ( 'NONE',  ( 0.01548846960712814240, 0.3688619771571980954, 0.3775276577326248106 ) ) ;
#26131=DIRECTION ( 'NONE',  ( 0.000000000000000000, -0.5877852522924820189, -0.8090169943749409009 ) ) ;
#26144=ADVANCED_FACE ( 'NONE', ( #34969 ), #266, .F. ) ;
#26147=CARTESIAN_POINT ( 'NONE',  ( -0.04575334816097668261, -0.4390433668671559486, 0.2110480141057394232 ) ) ;
#26159=CARTESIAN_POINT ( 'NONE',  ( -0.01548846960707531660, -0.2306506793134033284, 0.4716198300880330985 ) ) ;
#26160=DIRECTION ( 'NONE',  ( -1.000000000000000000, -2.341930812374887555E-31, 1.664003471950578127E-31 ) ) ;
#26175=DIRECTION ( 'NONE',  ( 0.000000000000000000, -0.7185945389473212819, 0.6954292836766992059 ) ) ;
#26178=ADVANCED_FACE ( 'NONE', ( #59 ), #19146, .T. ) ;
#26190=DIRECTION ( 'NONE',  ( -0.3468893892380656707, -0.3199132558031744233, 0.8816593788960987998 ) ) ;
#26192=CARTESIAN_POINT ( 'NONE',  ( 0.01548846960707350555, 0.4638115001430552775, 0.2459753896938760287 ) ) ;
#26195=( NAMED_UNIT ( * ) PLANE_ANGLE_UNIT ( ) SI_UNIT ( $, .RADIAN. ) );
#26212=EDGE_LOOP ( 'NONE', ( #37096, #16497, #37153, #32932 ) ) ;
#26218=CARTESIAN_POINT ( 'NONE',  ( -0.03303708955568261663, 0.5155567402493677065, -0.07470075307484629057 ) ) ;
#26219=VERTEX_POINT ( 'NONE', #16454 ) ;
#26225=DIRECTION ( 'NONE',  ( -1.000000000000000000, -2.341930812374887555E-31, 1.664003471950578127E-31 ) ) ;
#26232=CARTESIAN_POINT ( 'NONE',  ( -0.03647137243075494750, 0.2291011402250028028, -0.4576748478490495486 ) ) ;
#26233=CARTESIAN_POINT ( 'NONE',  ( -0.03478556507500706746, -0.5086691011511474958, -0.08927554178899406445 ) ) ;
#26234=DIRECTION ( 'NONE',  ( 1.000000000000000000, 0.000000000000000000, 0.000000000000000000 ) ) ;
#26239=CARTESIAN_POINT ( 'NONE',  ( 0.03875673594170580410, 0.4622647171927926069, -0.1151965740700868907 ) ) ;
#26246=CARTESIAN_POINT ( 'NONE',  ( -0.03474824846560561203, -0.2421026470131071862, -0.4562934628914087076 ) ) ;
#26252=EDGE_CURVE ( 'NONE', #35830, #5331, #2749, .T. ) ;
#26261=CARTESIAN_POINT ( 'NONE',  ( 0.03474878377840097399, -0.5087732247600297297, -0.08925105102097614929 ) ) ;
#26262=FACE_OUTER_BOUND ( 'NONE', #14012, .T. ) ;
#26282=CARTESIAN_POINT ( 'NONE',  ( 0.05201782277453876474, -0.4527080286589699742, 0.1280848763234518628 ) ) ;
#26292=CARTESIAN_POINT ( 'NONE',  ( 0.04575185649130587145, 0.2311416656438107786, 0.4288096517596615698 ) ) ;
#26302=CARTESIAN_POINT ( 'NONE',  ( -0.03874953289575294724, -0.3062954455724302139, 0.3649061716334319749 ) ) ;
#26306=EDGE_LOOP ( 'NONE', ( #22224, #15791, #37145, #26957 ) ) ;
#26312=CARTESIAN_POINT ( 'NONE',  ( -0.02953079040095652960, 0.5250338024619264354, 0.07436286310882474215 ) ) ;
#26313=EDGE_LOOP ( 'NONE', ( #1553, #36982, #15533, #23634 ) ) ;
#26315=CARTESIAN_POINT ( 'NONE',  ( 0.04582889109739261835, 0.4790149006698649625, -0.08746027838083722528 ) ) ;
#26328=DIRECTION ( 'NONE',  ( -1.000000000000000000, -2.280301054154495132E-31, 1.664003471950577689E-31 ) ) ;
#26336=CARTESIAN_POINT ( 'NONE',  ( 0.05561176441985726804, 0.4442366066780392697, 0.1229089882096652264 ) ) ;
#26345=CIRCLE ( 'NONE', #30261, 0.01500000000000001853 ) ;
#26349=TOROIDAL_SURFACE ( 'NONE', #14490, 0.6154198107346402491, 0.7750185148639454624 ) ;
#26352=CARTESIAN_POINT ( 'NONE',  ( 0.02231181081520623027, -0.07006449514257565014, -0.5077922075898769760 ) ) ;
#26358=ORIENTED_EDGE ( 'NONE', *, *, #22153, .T. ) ;
#26364=CARTESIAN_POINT ( 'NONE',  ( 0.05078493045284276225, 0.4330747843660815999, 0.1920285438096122066 ) ) ;
#26374=VECTOR ( 'NONE', #17887, 39.37007874015748143 ) ;
#26401=EDGE_CURVE ( 'NONE', #10402, #11533, #23121, .T. ) ;
#26416=CARTESIAN_POINT ( 'NONE',  ( 0.05283094505689985010, -0.03968992937477396760, -0.4666439588235277713 ) ) ;
#26418=CARTESIAN_POINT ( 'NONE',  ( -0.04047076529492513175, 0.4923674059679591375, -0.09402950075400676178 ) ) ;
#26427=EDGE_LOOP ( 'NONE', ( #31552, #26685, #37810 ) ) ;
#26428=ORIENTED_EDGE ( 'NONE', *, *, #10189, .T. ) ;
#26446=CARTESIAN_POINT ( 'NONE',  ( 0.04154009738085469305, 0.01731731106881273866, 0.4700109389422700290 ) ) ;
#26447=CARTESIAN_POINT ( 'NONE',  ( -0.04945776359514877929, -0.2513414220725570525, -0.4057848608195684936 ) ) ;
#26448=ORIENTED_EDGE ( 'NONE', *, *, #12996, .F. ) ;
#26457=AXIS2_PLACEMENT_3D ( 'NONE', #26159, #878, #38677 ) ;
#26467=ORIENTED_EDGE ( 'NONE', *, *, #21057, .T. ) ;
#26481=CARTESIAN_POINT ( 'NONE',  ( 0.04047170147977395549, -0.4536011460193543621, 0.2133323880731011479 ) ) ;
#26487=EDGE_CURVE ( 'NONE', #14366, #30357, #15877, .T. ) ;
#26490=TOROIDAL_SURFACE ( 'NONE', #20566, 0.5250000000000000222, 0.01499999999999999944 ) ;
#26492=CARTESIAN_POINT ( 'NONE',  ( 0.02235124290213119647, -0.2417860359143750582, -0.4518977707513310293 ) ) ;
#26508=CARTESIAN_POINT ( 'NONE',  ( -0.04285534776242247434, -0.3459954891507863728, 0.3537381284079030297 ) ) ;
#26511=PLANE ( 'NONE',  #18468 ) ;
#26513=VERTEX_POINT ( 'NONE', #18529 ) ;
#26519=ORIENTED_EDGE ( 'NONE', *, *, #31877, .T. ) ;
#26524=AXIS2_PLACEMENT_3D ( 'NONE', #22172, #15757, #31598 ) ;
#26530=ORIENTED_EDGE ( 'NONE', *, *, #25559, .F. ) ;
#26564=ORIENTED_EDGE ( 'NONE', *, *, #3352, .T. ) ;
#26580=AXIS2_PLACEMENT_3D ( 'NONE', #31124, #6002, #34403 ) ;
#26582=ORIENTED_EDGE ( 'NONE', *, *, #31392, .T. ) ;
#26587=CIRCLE ( 'NONE', #14766, 0.01500000000000002547 ) ;
#26614=ADVANCED_FACE ( 'NONE', ( #32095 ), #6783, .T. ) ;
#26630=DIRECTION ( 'NONE',  ( 1.000000000000000000, 2.341930812374887555E-31, -1.664003471950578127E-31 ) ) ;
#26640=CARTESIAN_POINT ( 'NONE',  ( -0.04139678531769541009, 0.4525211694413263097, -0.1291682248591896620 ) ) ;
#26652=DIRECTION ( 'NONE',  ( 0.000000000000000000, -0.1725921171159288392, 0.9849933812515907494 ) ) ;
#26654=AXIS2_PLACEMENT_3D ( 'NONE', #3459, #19103, #12934 ) ;
#26656=LINE ( 'NONE', #32790, #37781 ) ;
#26658=CARTESIAN_POINT ( 'NONE',  ( -0.05268850283020218989, -0.4442517014320102597, -0.1491954418488743439 ) ) ;
#26667=CARTESIAN_POINT ( 'NONE',  ( -0.04574984450155145793, -0.2311445325521683802, -0.4288136795716587235 ) ) ;
#26670=CARTESIAN_POINT ( 'NONE',  ( -0.05634304521267782806, 0.01028123094838855403, -0.4588823192046729837 ) ) ;
#26676=CARTESIAN_POINT ( 'NONE',  ( -0.03664605387828210464, 0.3149102792626774505, 0.3635688186731549920 ) ) ;
#26685=ORIENTED_EDGE ( 'NONE', *, *, #36722, .F. ) ;
#26686=CIRCLE ( 'NONE', #6306, 0.01500000000000004455 ) ;
#26688=EDGE_LOOP ( 'NONE', ( #11890, #36210, #2728 ) ) ;
#26696=VERTEX_POINT ( 'NONE', #38665 ) ;
#26701=CARTESIAN_POINT ( 'NONE',  ( 0.04946426091936331065, -0.4635716124040255570, 0.1136627969334474547 ) ) ;
#26721=CARTESIAN_POINT ( 'NONE',  ( -0.03174036153404242999, -0.3664551212196091035, 0.3753291932915900353 ) ) ;
#26728=CARTESIAN_POINT ( 'NONE',  ( 0.03303737228521891334, 0.2303602220530218125, -0.4672390599430968350 ) ) ;
#26731=VERTEX_POINT ( 'NONE', #13968 ) ;
#26733=VECTOR ( 'NONE', #19212, 39.37007874015748143 ) ;
#26745=CARTESIAN_POINT ( 'NONE',  ( 0.03158843595483477179, 0.4482533282648965556, 0.2030547983902457332 ) ) ;
#26752=CARTESIAN_POINT ( 'NONE',  ( -0.01548846960707524721, 0.09061086148576029398, -0.5171215251571035232 ) ) ;
#26753=DIRECTION ( 'NONE',  ( 0.000000000000000000, -0.5877852522924855716, 0.8090169943749384585 ) ) ;
#26767=ORIENTED_EDGE ( 'NONE', *, *, #23412, .T. ) ;
#26769=ORIENTED_EDGE ( 'NONE', *, *, #10795, .F. ) ;
#26777=ORIENTED_EDGE ( 'NONE', *, *, #128, .T. ) ;
#26820=EDGE_LOOP ( 'NONE', ( #32310, #14776, #22317, #17458 ) ) ;
#26832=CARTESIAN_POINT ( 'NONE',  ( -0.05491348488830481017, 0.4316112672892382651, -0.1667783590291073981 ) ) ;
#26839=DIRECTION ( 'NONE',  ( 1.000000000000000000, -1.681422630952717046E-11, 5.294072836416690161E-12 ) ) ;
#26844=CARTESIAN_POINT ( 'NONE',  ( 0.04582713223189449625, -0.4790191777205495827, -0.08746099429787949908 ) ) ;
#26847=CARTESIAN_POINT ( 'NONE',  ( -0.03301200226531658677, 0.2303790867044800128, -0.4673050311136111024 ) ) ;
#26848=LINE ( 'NONE', #16970, #25866 ) ;
#26860=ORIENTED_EDGE ( 'NONE', *, *, #39057, .T. ) ;
#26867=CARTESIAN_POINT ( 'NONE',  ( 0.02953079040095700838, 0.2329676531120518090, 0.4763574306556300764 ) ) ;
#26868=DIRECTION ( 'NONE',  ( 0.000000000000000000, -0.5877852522924748024, -0.8090169943749461190 ) ) ;
#26869=DIRECTION ( 'NONE',  ( -1.000000000000000000, -2.280301054154495132E-31, 1.664003471950577689E-31 ) ) ;
#26874=CARTESIAN_POINT ( 'NONE',  ( -0.05082303569918705799, -0.2375724430107435947, -0.4097459652473651182 ) ) ;
#26891=CARTESIAN_POINT ( 'NONE',  ( 0.02881408050861556172, -0.4517606495562037083, 0.2100211630561500953 ) ) ;
#26897=DIRECTION ( 'NONE',  ( 0.000000000000000000, 0.9510565162951443163, 0.3090169943749759840 ) ) ;
#26900=DIRECTION ( 'NONE',  ( 1.000000000000000000, 0.000000000000000000, 0.000000000000000000 ) ) ;
#26902=CARTESIAN_POINT ( 'NONE',  ( 0.05201782277453504549, 0.2617104306118889223, 0.3909705171288710424 ) ) ;
#26913=CARTESIAN_POINT ( 'NONE',  ( 0.1499999999999996614, -0.09319974324248556097, 0.5318964258758792640 ) ) ;
#26917=CARTESIAN_POINT ( 'NONE',  ( -0.05083665881509066842, 0.2375940621857685897, -0.4096919151850460517 ) ) ;
#26937=CARTESIAN_POINT ( 'NONE',  ( 0.04582897286455926006, 0.06484386734940718322, -0.4825967645925798299 ) ) ;
#26941=CARTESIAN_POINT ( 'NONE',  ( 0.03309060444528770517, 0.2303206394829958592, -0.4671006372792953498 ) ) ;
#26942=CARTESIAN_POINT ( 'NONE',  ( -0.1399999999999997358, 0.000000000000000000, 0.000000000000000000 ) ) ;
#26949=CARTESIAN_POINT ( 'NONE',  ( 2.915087563824520450E-32, -4.527947890665461248E-17, -0.2149999999999999967 ) ) ;
#26952=CARTESIAN_POINT ( 'NONE',  ( 0.03868649100028153515, 0.03360400204099701221, -0.4753701585314239475 ) ) ;
#26954=VERTEX_POINT ( 'NONE', #21999 ) ;
#26956=DIRECTION ( 'NONE',  ( 1.000000000000000000, -2.532387540469236772E-12, -8.550494110633229256E-14 ) ) ;
#26957=ORIENTED_EDGE ( 'NONE', *, *, #12927, .F. ) ;
#26962=ORIENTED_EDGE ( 'NONE', *, *, #10652, .F. ) ;
#26966=CARTESIAN_POINT ( 'NONE',  ( -0.02235124290213020420, -0.5044963136724034403, -0.09030809412322339524 ) ) ;
#26979=AXIS2_PLACEMENT_3D ( 'NONE', #22936, #4573, #35267 ) ;
#26988=FACE_OUTER_BOUND ( 'NONE', #17893, .T. ) ;
#27002=CARTESIAN_POINT ( 'NONE',  ( 0.01896931156525321488, 0.07379981600434322442, -0.5147676832640546429 ) ) ;
#27011=ORIENTED_EDGE ( 'NONE', *, *, #32300, .T. ) ;
#27014=ORIENTED_EDGE ( 'NONE', *, *, #21404, .F. ) ;
#27030=DIRECTION ( 'NONE',  ( -1.416619696839557091E-11, -0.5877852522924708056, 0.8090169943749491166 ) ) ;
#27034=CARTESIAN_POINT ( 'NONE',  ( 0.03309060444528726802, -0.5154120966056443542, -0.07470591001490078931 ) ) ;
#27039=CARTESIAN_POINT ( 'NONE',  ( -0.04945776359515825088, -0.4418538386403662033, -0.1805520672786481706 ) ) ;
#27042=DIRECTION ( 'NONE',  ( 2.280301054154496446E-31, -1.000000000000000000, 4.555315873022819131E-16 ) ) ;
#27045=CARTESIAN_POINT ( 'NONE',  ( 0.02953079040095673430, -0.2329676531120430660, 0.4763574306556350169 ) ) ;
#27050=CARTESIAN_POINT ( 'NONE',  ( 0.02872242845529806091, 0.5252126300208209697, -0.08844866507292881153 ) ) ;
#27054=CARTESIAN_POINT ( 'NONE',  ( -0.05083674528492013178, -0.04859289555129394506, -0.4711018118971389557 ) ) ;
#27062=CARTESIAN_POINT ( 'NONE',  ( -0.02869712619511932336, 0.3396447909410118537, 0.3648221446286663006 ) ) ;
#27063=CARTESIAN_POINT ( 'NONE',  ( 0.04760578872587347549, 0.04300259564631410403, 0.4803138972567881360 ) ) ;
#27064=CARTESIAN_POINT ( 'NONE',  ( 0.03170874437002394602, -0.4816890803163380586, -0.09938493968693067060 ) ) ;
#27073=ORIENTED_EDGE ( 'NONE', *, *, #30129, .T. ) ;
#27076=CIRCLE ( 'NONE', #18527, 0.5399999999999999245 ) ;
#27086=DIRECTION ( 'NONE',  ( -1.000000000000000000, -2.280301054154495132E-31, 1.664003471950577689E-31 ) ) ;
#27087=CARTESIAN_POINT ( 'NONE',  ( 0.05201840200954328114, -0.4415345355162912377, 0.1624690192511292486 ) ) ;
#27099=TOROIDAL_SURFACE ( 'NONE', #29729, 0.5250000000000000222, 0.01499999999999999944 ) ;
#27104=CARTESIAN_POINT ( 'NONE',  ( -0.02953079040095700838, 0.2329676531120452587, -0.4763574306556336291 ) ) ;
#27116=DIRECTION ( 'NONE',  ( 1.000000000000000000, 0.000000000000000000, 0.000000000000000000 ) ) ;
#27121=CARTESIAN_POINT ( 'NONE',  ( -0.03654364704248847656, 0.2290829176602892370, -0.4574690890339254135 ) ) ;
#27124=ORIENTED_EDGE ( 'NONE', *, *, #14559, .F. ) ;
#27141=AXIS2_PLACEMENT_3D ( 'NONE', #35742, #23005, #38813 ) ;
#27151=CARTESIAN_POINT ( 'NONE',  ( 0.05283710938261031165, 0.4315340639268053224, 0.1819215676045953523 ) ) ;
#27175=B_SPLINE_CURVE_WITH_KNOTS ( 'NONE', 3,
 ( #34459, #24208, #18412, #8540, #18847, #40628, #36936, #21110, #6060, #27895, #18628, #24817, #27297, #37339, #33638, #5451, #15124, #2192 ),
 .UNSPECIFIED., .F., .F.,
 ( 4, 2, 2, 2, 2, 2, 2, 2, 4 ),
 ( 0.000000000000000000, 0.0007746617437634303492, 0.001549323487526860698, 0.002323985231290290939, 0.003098646975053721397, 0.003873308718817151854, 0.004647970462580581878, 0.005422632206344012336, 0.006197293950107442793 ),
 .UNSPECIFIED. ) ;
#27178=FACE_OUTER_BOUND ( 'NONE', #30052, .T. ) ;
#27194=B_SPLINE_CURVE_WITH_KNOTS ( 'NONE', 3,
 ( #13729, #17228, #5077, #1230, #14144, #38821, #1621, #39245, #39639, #36143, #7955, #29993, #1826, #8167, #20746, #33269, #14541, #11473 ),
 .UNSPECIFIED., .F., .F.,
 ( 4, 2, 2, 2, 2, 2, 2, 2, 4 ),
 ( 0.000000000000000000, 0.0007746617437634300239, 0.001549323487526859614, 0.002323985231290289638, 0.003098646975053719228, 0.003873308718817148819, 0.004647970462580579276, 0.005422632206344009734, 0.006197293950107438457 ),
 .UNSPECIFIED. ) ;
#27202=CIRCLE ( 'NONE', #37052, 0.5302738246768086139 ) ;
#27214=CARTESIAN_POINT ( 'NONE',  ( 0.03672447062657592520, -0.04080285735492294313, -0.4790833464420522492 ) ) ;
#27234=PRODUCT ( 'Pulley', 'Pulley', '', ( #37497 ) ) ;
#27237=CARTESIAN_POINT ( 'NONE',  ( -0.03647137243075046498, 0.4543612417835873885, -0.2356044583002107895 ) ) ;
#27252=CARTESIAN_POINT ( 'NONE',  ( -0.02587796518899032269, -1.798561299892753714E-16, -0.5399999999999999245 ) ) ;
#27262=AXIS2_PLACEMENT_3D ( 'NONE', #28310, #24428, #24844 ) ;
#27268=DIRECTION ( 'NONE',  ( 1.000000000000000000, 1.023084414572561287E-11, 1.435532102222559952E-11 ) ) ;
#27271=CARTESIAN_POINT ( 'NONE',  ( -0.01548846960707406760, -0.3688619771572930750, -0.3775276577327001948 ) ) ;
#27279=CARTESIAN_POINT ( 'NONE',  ( 0.04762035657659133281, -0.04295292190959984491, 0.4802795956081307160 ) ) ;
#27280=CARTESIAN_POINT ( 'NONE',  ( 0.03171861681799903465, -0.4702483710821712126, -0.2325697148610222365 ) ) ;
#27287=ADVANCED_FACE ( 'NONE', ( #24413 ), #2780, .F. ) ;
#27289=EDGE_LOOP ( 'NONE', ( #28086, #16359, #2596, #4988 ) ) ;
#27293=EDGE_LOOP ( 'NONE', ( #10436, #24673, #3817, #36536 ) ) ;
#27297=CARTESIAN_POINT ( 'NONE',  ( -0.05083665881508921125, -0.4330284998000982211, 0.1917934360576655506 ) ) ;
#27301=ORIENTED_EDGE ( 'NONE', *, *, #11050, .T. ) ;
#27314=DIRECTION ( 'NONE',  ( -1.355854680848614478E-31, 3.330669073875470114E-16, 1.000000000000000000 ) ) ;
#27319=CARTESIAN_POINT ( 'NONE',  ( 0.01896931156525484205, 0.2428675472501187205, 0.4598342473848836542 ) ) ;
#27334=CARTESIAN_POINT ( 'NONE',  ( 0.01548846960707524721, 0.000000000000000000, 0.000000000000000000 ) ) ;
#27335=ADVANCED_FACE ( 'NONE', ( #34472 ), #27099, .T. ) ;
#27348=DIRECTION ( 'NONE',  ( 0.3468893892380643384, -0.7396492646828627393, 0.5767033179097752482 ) ) ;
#27356=ADVANCED_FACE ( 'NONE', ( #36741 ), #37351, .T. ) ;
#27367=CARTESIAN_POINT ( 'NONE',  ( 0.05561176441985765662, 0.2541700551350243309, -0.3845131534397753792 ) ) ;
#27386=EDGE_CURVE ( 'NONE', #1535, #30357, #33876, .T. ) ;
#27391=EDGE_CURVE ( 'NONE', #30357, #10402, #21194, .T. ) ;
#27393=ORIENTED_EDGE ( 'NONE', *, *, #19596, .F. ) ;
#27402=ORIENTED_EDGE ( 'NONE', *, *, #21404, .T. ) ;
#27405=CARTESIAN_POINT ( 'NONE',  ( -0.04047076529493150165, -0.4923674059679353232, 0.09402950075400964836 ) ) ;
#27417=FACE_OUTER_BOUND ( 'NONE', #6452, .T. ) ;
#27425=CARTESIAN_POINT ( 'NONE',  ( 0.04157078424165680519, 0.01703670724029244729, -0.4699541233906586180 ) ) ;
#27430=ADVANCED_FACE ( 'NONE', ( #12653 ), #14599, .F. ) ;
#27437=ORIENTED_EDGE ( 'NONE', *, *, #18783, .T. ) ;
#27441=CARTESIAN_POINT ( 'NONE',  ( -0.02872242845530527736, 0.4768947642620179894, -0.2371557650701878461 ) ) ;
#27454=FACE_OUTER_BOUND ( 'NONE', #7410, .T. ) ;
#27466=CARTESIAN_POINT ( 'NONE',  ( -0.01548846960707393229, -0.07651041855119014579, 0.5222379212568235562 ) ) ;
#27471=CARTESIAN_POINT ( 'NONE',  ( -0.02953079040095606123, 0.09152108205202102997, -0.5223162075576446295 ) ) ;
#27474=EDGE_LOOP ( 'NONE', ( #21674, #6213, #1189, #16333 ) ) ;
#27475=CARTESIAN_POINT ( 'NONE',  ( -0.04155248107635971244, 0.2901916982059713490, 0.3701002694350333799 ) ) ;
#27476=CARTESIAN_POINT ( 'NONE',  ( 0.05269111014006671451, -0.009103832413163924150, 0.4686064687114369631 ) ) ;
#27480=CARTESIAN_POINT ( 'NONE',  ( 0.04211471441534279242, 0.4486586774158415336, 0.1367340165256794304 ) ) ;
#27491=DIRECTION ( 'NONE',  ( 0.000000000000000000, -0.5877852522924463807, 0.8090169943749667691 ) ) ;
#27498=CARTESIAN_POINT ( 'NONE',  ( -0.01895494625228227870, 0.5124113341948446365, 0.08888305413160398072 ) ) ;
#27501=DIRECTION ( 'NONE',  ( -1.416619696839552729E-11, -0.9510565162951545304, -0.3090169943749445092 ) ) ;
#27505=CARTESIAN_POINT ( 'NONE',  ( -0.05252049209742480629, 0.2682992380086470230, 0.3847779939372228397 ) ) ;
#27507=EDGE_CURVE ( 'NONE', #5616, #24540, #33658, .T. ) ;
#27523=FACE_OUTER_BOUND ( 'NONE', #5252, .T. ) ;
#27535=CARTESIAN_POINT ( 'NONE',  ( -0.02869712619511924009, 0.2420104654861718607, -0.4357576342647250245 ) ) ;
#27536=ORIENTED_EDGE ( 'NONE', *, *, #10239, .T. ) ;
#27556=DIRECTION ( 'NONE',  ( 0.000000000000000000, 3.330669073875470114E-16, 1.000000000000000000 ) ) ;
#27573=DIRECTION ( 'NONE',  ( 0.000000000000000000, -0.9510565162951505336, 0.3090169943749571657 ) ) ;
#27613=CARTESIAN_POINT ( 'NONE',  ( 0.02238826743733072361, -0.06997574608431053611, -0.5076331681966341769 ) ) ;
#27622=EDGE_CURVE ( 'NONE', #39166, #4242, #19868, .T. ) ;
#27625=ORIENTED_EDGE ( 'NONE', *, *, #38305, .F. ) ;
#27628=FACE_OUTER_BOUND ( 'NONE', #37729, .T. ) ;
#27640=VERTEX_POINT ( 'NONE', #29880 ) ;
#27657=DIRECTION ( 'NONE',  ( 1.000000000000000000, 2.280301054154495132E-31, -1.664003471950577689E-31 ) ) ;
#27660=DIRECTION ( 'NONE',  ( -1.000000000000000000, -2.280301054154495132E-31, 1.664003471950577689E-31 ) ) ;
#27662=CARTESIAN_POINT ( 'NONE',  ( -0.03478556507499944855, -0.2420934825333271312, 0.4561854036929733902 ) ) ;
#27663=DIRECTION ( 'NONE',  ( 0.000000000000000000, -0.8090169943749496717, -0.5877852522924700285 ) ) ;
#27664=ORIENTED_EDGE ( 'NONE', *, *, #12184, .F. ) ;
#27665=CARTESIAN_POINT ( 'NONE',  ( -0.04139678531769593051, 0.01699044972118296526, -0.4702883835734110174 ) ) ;
#27670=CARTESIAN_POINT ( 'NONE',  ( -0.01548846960707524721, 0.000000000000000000, 0.000000000000000000 ) ) ;
#27671=CARTESIAN_POINT ( 'NONE',  ( 0.05561310505366701823, -0.4316274075649161324, -0.1617055803010020720 ) ) ;
#27673=CARTESIAN_POINT ( 'NONE',  ( 0.01548846960706664298, -0.5198120922912313757, 0.07362328916749247276 ) ) ;
#27674=CARTESIAN_POINT ( 'NONE',  ( 0.05252049209742985086, 0.4488546425834872844, 0.1362647994370476678 ) ) ;
#27676=CARTESIAN_POINT ( 'NONE',  ( -0.05283710938261081819, -0.3063690517300527993, -0.3541964274677634195 ) ) ;
#27677=ORIENTED_EDGE ( 'NONE', *, *, #6970, .F. ) ;
#27680=CARTESIAN_POINT ( 'NONE',  ( 0.04582705327698215897, 0.06484491888963163364, 0.4826014279685452157 ) ) ;
#27694=DIRECTION ( 'NONE',  ( 1.000000000000000000, 2.280301054154496446E-31, 1.355854680848613603E-31 ) ) ;
#27703=CARTESIAN_POINT ( 'NONE',  ( -0.04047076529492606850, 0.2415772653364889611, 0.4392125161515883502 ) ) ;
#27718=CIRCLE ( 'NONE', #17203, 0.5302738246768092800 ) ;
#27720=DIRECTION ( 'NONE',  ( -1.654489825136704222E-31, 0.9510565162951546414, 0.3090169943749438985 ) ) ;
#27721=CARTESIAN_POINT ( 'NONE',  ( 0.04575106512775098389, 0.2311453587453343173, -0.4288095618640244133 ) ) ;
#27724=FACE_OUTER_BOUND ( 'NONE', #33438, .T. ) ;
#27727=ORIENTED_EDGE ( 'NONE', *, *, #15538, .T. ) ;
#27737=ORIENTED_EDGE ( 'NONE', *, *, #15770, .F. ) ;
#27743=DIRECTION ( 'NONE',  ( 1.000000000000000000, 1.213308482346485395E-12, 2.286601241528059267E-12 ) ) ;
#27761=DIRECTION ( 'NONE',  ( -1.000000000000000000, -2.280301054154495132E-31, 1.664003471950577689E-31 ) ) ;
#27770=DIRECTION ( 'NONE',  ( 1.000000000000000000, 1.671477276948179358E-11, 5.600159359328154813E-12 ) ) ;
#27771=AXIS2_PLACEMENT_3D ( 'NONE', #8260, #24314, #33161 ) ;
#27795=CARTESIAN_POINT ( 'NONE',  ( -0.05076541221973769613, -0.4633004642377251958, 0.09914728473419444355 ) ) ;
#27807=AXIS2_PLACEMENT_3D ( 'NONE', #13124, #32056, #25687 ) ;
#27817=CARTESIAN_POINT ( 'NONE',  ( 0.03170874437002789425, -0.05432941731172213906, -0.4888251740112578014 ) ) ;
#27818=CIRCLE ( 'NONE', #33060, 0.01499999999999995261 ) ;
#27819=AXIS2_PLACEMENT_3D ( 'NONE', #8920, #2961, #8315 ) ;
#27831=EDGE_CURVE ( 'NONE', #37319, #4571, #6077, .T. ) ;
#27836=FACE_OUTER_BOUND ( 'NONE', #6558, .T. ) ;
#27846=CARTESIAN_POINT ( 'NONE',  ( -0.05561176441985817703, -0.2871508736821589136, 0.3605511861568549414 ) ) ;
#27852=ADVANCED_FACE ( 'NONE', ( #68, #9075 ), #9689, .F. ) ;
#27855=EDGE_CURVE ( 'NONE', #9762, #39882, #36296, .T. ) ;
#27862=DIRECTION ( 'NONE',  ( 0.000000000000000000, 3.330669073875470114E-16, 1.000000000000000000 ) ) ;
#27864=CARTESIAN_POINT ( 'NONE',  ( -0.01548846960707517956, -0.3772621329472692908, 0.3651003739303441131 ) ) ;
#27866=CARTESIAN_POINT ( 'NONE',  ( -0.03642997641689543764, -0.08373618209167926763, 0.5050295872266582498 ) ) ;
#27868=AXIS2_PLACEMENT_3D ( 'NONE', #22583, #13513, #6505 ) ;
#27869=ORIENTED_EDGE ( 'NONE', *, *, #35522, .F. ) ;
#27872=CARTESIAN_POINT ( 'NONE',  ( 0.1499999999999994671, -0.5346638663566692928, 0.07572681171513533094 ) ) ;
#27875=CARTESIAN_POINT ( 'NONE',  ( -0.05137569054208909053, 0.02238181648184895539, -0.4716086671401685804 ) ) ;
#27886=CARTESIAN_POINT ( 'NONE',  ( 0.03672309138970048653, 0.4682479968340216847, 0.1092356788912528659 ) ) ;
#27888=CARTESIAN_POINT ( 'NONE',  ( 0.03170874437002830365, -0.3312776501327927003, -0.3635338427919229121 ) ) ;
#27895=CARTESIAN_POINT ( 'NONE',  ( -0.05634301242525709824, -0.4332457820339908894, 0.1515812001271522325 ) ) ;
#27902=AXIS2_PLACEMENT_3D ( 'NONE', #35337, #14330, #14522 ) ;
#27906=AXIS2_PLACEMENT_3D ( 'NONE', #12671, #25235, #37775 ) ;
#27907=CARTESIAN_POINT ( 'NONE',  ( -0.02231181081520786438, 0.4612879682508959078, 0.2235517164227159292 ) ) ;
#27914=CARTESIAN_POINT ( 'NONE',  ( -0.04285534776242195393, 0.2295064659597298717, 0.4383723578020115585 ) ) ;
#27917=FACE_OUTER_BOUND ( 'NONE', #18358, .T. ) ;
#27922=VERTEX_POINT ( 'NONE', #34367 ) ;
#27934=CARTESIAN_POINT ( 'NONE',  ( 0.05076679145661696507, 0.2374648372614248382, -0.4099810879409672149 ) ) ;
#27936=CARTESIAN_POINT ( 'NONE',  ( -0.02587796518899032269, 0.000000000000000000, 0.000000000000000000 ) ) ;
#27949=CARTESIAN_POINT ( 'NONE',  ( 0.01548846960707524721, 0.4638115001430962447, -0.2459753896937880435 ) ) ;
#27956=CARTESIAN_POINT ( 'NONE',  ( -2.372745691485074626E-32, 5.828670879282072084E-17, 0.1749999999999999889 ) ) ;
#27958=CIRCLE ( 'NONE', #1688, 0.01500000000000001853 ) ;
#27959=DIRECTION ( 'NONE',  ( 1.000000000000000000, 2.280301054154495132E-31, -1.664003471950577689E-31 ) ) ;
#27982=CARTESIAN_POINT ( 'NONE',  ( -0.05562144613422675271, -0.4441896308501013246, -0.1229845283801413863 ) ) ;
#27984=DIRECTION ( 'NONE',  ( -1.000000000000000000, -2.341930812374887555E-31, 1.664003471950578127E-31 ) ) ;
#27985=ORIENTED_EDGE ( 'NONE', *, *, #10652, .T. ) ;
#28004=CARTESIAN_POINT ( 'NONE',  ( -0.05634115714581228868, -0.4380405955734085199, 0.1368374331724208914 ) ) ;
#28017=CARTESIAN_POINT ( 'NONE',  ( 0.02881408050861827136, -0.2420347005671091012, 0.4354489374660209244 ) ) ;
#28030=VECTOR ( 'NONE', #4596, 39.37007874015748143 ) ;
#28031=CARTESIAN_POINT ( 'NONE',  ( 0.05634301242525744519, -0.2780425975185431553, 0.3652000572937675882 ) ) ;
#28032=EDGE_LOOP ( 'NONE', ( #30600, #7541, #27437, #14348 ) ) ;
#28034=VERTEX_POINT ( 'NONE', #38859 ) ;
#28059=ORIENTED_EDGE ( 'NONE', *, *, #4205, .F. ) ;
#28073=AXIS2_PLACEMENT_3D ( 'NONE', #38074, #10322, #7397 ) ;
#28076=CARTESIAN_POINT ( 'NONE',  ( -0.05491348488830684327, 0.02524042857556436925, 0.4620240554957945056 ) ) ;
#28082=ORIENTED_EDGE ( 'NONE', *, *, #10795, .T. ) ;
#28083=CARTESIAN_POINT ( 'NONE',  ( -0.04947837552028403613, -0.03507397079374865306, -0.4759739487165542404 ) ) ;
#28085=ORIENTED_EDGE ( 'NONE', *, *, #32338, .T. ) ;
#28086=ORIENTED_EDGE ( 'NONE', *, *, #10798, .F. ) ;
#28092=CARTESIAN_POINT ( 'NONE',  ( 0.05634115714581289930, 0.4380405955734021362, 0.1368374331724312720 ) ) ;
#28094=CARTESIAN_POINT ( 'NONE',  ( 0.05634402396114377570, -0.2613837787620673092, -0.3773006586902102888 ) ) ;
#28095=ORIENTED_EDGE ( 'NONE', *, *, #24402, .T. ) ;
#28097=ORIENTED_EDGE ( 'NONE', *, *, #17686, .T. ) ;
#28108=CARTESIAN_POINT ( 'NONE',  ( -0.04211471441534295201, 0.2826022563027020817, -0.3743350969764919212 ) ) ;
#28114=CARTESIAN_POINT ( 'NONE',  ( -0.03171102739523045527, 0.3312744048890978177, 0.3635303745205920589 ) ) ;
#28135=CARTESIAN_POINT ( 'NONE',  ( 0.04308558661661724548, 0.2425983775171377810, -0.4306836113028226776 ) ) ;
#28146=CARTESIAN_POINT ( 'NONE',  ( 0.1499999999999997724, 0.2306506793134120714, 0.4716198300880287131 ) ) ;
#28149=ORIENTED_EDGE ( 'NONE', *, *, #32895, .T. ) ;
#28150=ORIENTED_EDGE ( 'NONE', *, *, #15801, .T. ) ;
#28156=CARTESIAN_POINT ( 'NONE',  ( -0.01548846960707531660, -0.3772621329472692908, -0.3651003739303438911 ) ) ;
#28166=EDGE_CURVE ( 'NONE', #4225, #16603, #33102, .T. ) ;
#28180=CARTESIAN_POINT ( 'NONE',  ( -0.02953079040095707777, -0.5250338024619269905, -0.07436286310882420092 ) ) ;
#28182=CARTESIAN_POINT ( 'NONE',  ( 0.1499999999999993561, 0.000000000000000000, 0.000000000000000000 ) ) ;
#28185=CARTESIAN_POINT ( 'NONE',  ( 0.000000000000000000, 0.000000000000000000, 0.000000000000000000 ) ) ;
#28193=VERTEX_POINT ( 'NONE', #33493 ) ;
#28198=CARTESIAN_POINT ( 'NONE',  ( -0.05616044724337241473, -0.4336395721329119879, 0.1516614036261227927 ) ) ;
#28208=CARTESIAN_POINT ( 'NONE',  ( 0.05201840200955108739, -0.2617120493658864344, 0.3909676859878761790 ) ) ;
#28213=CARTESIAN_POINT ( 'NONE',  ( -0.02238826743733216343, 0.4611641377668438957, 0.2234181651772507715 ) ) ;
#28221=DIRECTION ( 'NONE',  ( -0.3468893892380667254, -0.2594111197898709698, 0.9013177145509825294 ) ) ;
#28226=DIRECTION ( 'NONE',  ( -1.000000000000000000, -2.280301054154495132E-31, 1.664003471950577689E-31 ) ) ;
#28227=( BOUNDED_SURFACE ( )  B_SPLINE_SURFACE ( 3, 2, ( 
 ( #22560, #6687, #32394 ),
 ( #4218, #25444, #7087 ),
 ( #34880, #25848, #28511 ),
 ( #1178, #6895, #38366 ),
 ( #35477, #22958, #10593 ),
 ( #9990, #16183, #28725 ),
 ( #976, #7498, #388 ),
 ( #16368, #20077, #37975 ),
 ( #13677, #9785, #13491 ),
 ( #22356, #26055, #586 ),
 ( #13079, #28907, #10205 ),
 ( #26239, #25635, #19657 ),
 ( #35091, #19468, #32001 ),
 ( #22771, #35295, #32193 ),
 ( #7282, #4007, #16571 ),
 ( #38576, #19859, #16784 ),
 ( #4598, #11205, #30135 ),
 ( #36094, #27050, #23772 ) ),
 .UNSPECIFIED., .F., .F., .T. ) 
 B_SPLINE_SURFACE_WITH_KNOTS ( ( 4, 2, 2, 2, 2, 2, 2, 2, 4 ),
 ( 3, 3 ),
 ( -0.001532620576208853364, -0.0007637936630077653581, 5.033250193322647351E-06, 0.0007738601633944106528, 0.001542687076595498658, 0.002311513989796586989, 0.003080340902997674886, 0.003849167816198762783, 0.004617994729399850680 ),
 ( 0.000000000000000000, 1.000000000000000000 ),
 .UNSPECIFIED. ) 
 GEOMETRIC_REPRESENTATION_ITEM ( )  RATIONAL_B_SPLINE_SURFACE ( (
 ( 1.000000000000000000, 0.7283825911960453148, 1.000000000000000000),
 ( 1.000000000000000000, 0.7404385082113110750, 1.000000000000000000),
 ( 1.000000000000000000, 0.7521504257739634047, 1.000000000000000000),
 ( 1.000000000000000000, 0.7744497410760246003, 1.000000000000000000),
 ( 1.000000000000000000, 0.7845654757373008437, 1.000000000000000000),
 ( 1.000000000000000000, 0.8022083990893182914, 1.000000000000000000),
 ( 1.000000000000000000, 0.8094167424698777147, 1.000000000000000000),
 ( 1.000000000000000000, 0.8194491993617203374, 1.000000000000000000),
 ( 1.000000000000000000, 0.8220634900780806609, 1.000000000000000000),
 ( 1.000000000000000000, 0.8220705070823161043, 1.000000000000000000),
 ( 1.000000000000000000, 0.8194468812482857967, 1.000000000000000000),
 ( 1.000000000000000000, 0.8094220769837565665, 1.000000000000000000),
 ( 1.000000000000000000, 0.8022659121984583308, 1.000000000000000000),
 ( 1.000000000000000000, 0.7845681159036421715, 1.000000000000000000),
 ( 1.000000000000000000, 0.7744426415184756385, 1.000000000000000000),
 ( 1.000000000000000000, 0.7522890290929223900, 1.000000000000000000),
 ( 1.000000000000000000, 0.7403540167214975876, 1.000000000000000000),
 ( 1.000000000000000000, 0.7283825911960206678, 1.000000000000000000) ) ) 
 REPRESENTATION_ITEM ( '' )  SURFACE ( )  );
#28256=CARTESIAN_POINT ( 'NONE',  ( -0.03877220711930370878, 0.03321538116298803495, 0.4752084053751550186 ) ) ;
#28273=CARTESIAN_POINT ( 'NONE',  ( 0.05634490452572782360, 0.4348542811545040854, 0.1466173361067543424 ) ) ;
#28278=ORIENTED_EDGE ( 'NONE', *, *, #29559, .F. ) ;
#28280=CARTESIAN_POINT ( 'NONE',  ( 0.1499999999999994671, -0.5198120922912051745, 0.07362328916749301400 ) ) ;
#28291=CARTESIAN_POINT ( 'NONE',  ( -0.05283102792148795107, 0.2421768296208693105, 0.4008516595826041029 ) ) ;
#28293=CARTESIAN_POINT ( 'NONE',  ( -0.03174036153405623839, -0.4702001351683494090, -0.2325364317535350001 ) ) ;
#28294=TOROIDAL_SURFACE ( 'NONE', #5934, 0.5250000000000000222, 0.01499999999999999944 ) ;
#28299=CARTESIAN_POINT ( 'NONE',  ( -0.05543910610525158017, 0.2544236545520490167, 0.3848133000241384383 ) ) ;
#28305=B_SPLINE_CURVE_WITH_KNOTS ( 'NONE', 3,
 ( #29744, #5048, #23597, #17403, #1799, #26874, #39405, #2580, #24604, #18004, #1982, #27676, #30354, #34046, #37332, #14927, #24390, #24003 ),
 .UNSPECIFIED., .F., .F.,
 ( 4, 2, 2, 2, 2, 2, 2, 2, 4 ),
 ( 0.000000000000000000, 0.0007746617437634291566, 0.001549323487526858313, 0.002323985231290287470, 0.003098646975053716626, 0.003873308718817145783, 0.004647970462580574939, 0.005422632206344004530, 0.006197293950107433252 ),
 .UNSPECIFIED. ) ;
#28310=CARTESIAN_POINT ( 'NONE',  ( 0.1499999999999993283, 0.3232818887608624459, -0.4449593469062196882 ) ) ;
#28319=CARTESIAN_POINT ( 'NONE',  ( 0.04575185649130700943, 0.3363955107642143116, -0.3523382570435943384 ) ) ;
#28327=AXIS2_PLACEMENT_3D ( 'NONE', #31248, #27743, #14572 ) ;
#28332=CIRCLE ( 'NONE', #2054, 0.2149999999999999967 ) ;
#28337=ORIENTED_EDGE ( 'NONE', *, *, #35051, .F. ) ;
#28376=CARTESIAN_POINT ( 'NONE',  ( 0.04582889109739201466, -0.2312034125369023252, -0.4285435303321084577 ) ) ;
#28379=CARTESIAN_POINT ( 'NONE',  ( -0.02953079040095693900, -0.4684706630666107263, -0.2484463060367401721 ) ) ;
#28396=EDGE_LOOP ( 'NONE', ( #37378, #17995, #38727, #58 ) ) ;
#28401=CARTESIAN_POINT ( 'NONE',  ( -0.02235124290213139076, -0.07000983313419636977, -0.5077112423787091267 ) ) ;
#28407=CARTESIAN_POINT ( 'NONE',  ( 0.1399999999999994582, 0.2149999999999997469, -5.463695987328526437E-16 ) ) ;
#28416=AXIS2_PLACEMENT_3D ( 'NONE', #34162, #33977, #278 ) ;
#28417=CARTESIAN_POINT ( 'NONE',  ( -0.05269111014005918581, 0.4484844745756846884, 0.1361491033660743311 ) ) ;
#28432=AXIS2_PLACEMENT_3D ( 'NONE', #3853, #22607, #13320 ) ;
#28441=CARTESIAN_POINT ( 'NONE',  ( -0.05283710938261110268, -0.2421875768565582288, 0.4008269984734637026 ) ) ;
#28442=VERTEX_POINT ( 'NONE', #22612 ) ;
#28443=VECTOR ( 'NONE', #30031, 39.37007874015748854 ) ;
#28451=CARTESIAN_POINT ( 'NONE',  ( 0.01548846960712783535, -0.5203207976466778240, -0.08861466064782558272 ) ) ;
#28459=APPLICATION_CONTEXT ( 'configuration controlled 3d designs of mechanical parts and assemblies' ) ;
#28460=CARTESIAN_POINT ( 'NONE',  ( -0.05076541221973600304, -0.04887304573182980894, 0.4712631214448610439 ) ) ;
#28475=CARTESIAN_POINT ( 'NONE',  ( -0.01548846960707524721, 0.000000000000000000, 0.000000000000000000 ) ) ;
#28477=CARTESIAN_POINT ( 'NONE',  ( 0.05616044724337368454, 0.4336395721329034947, 0.1516614036261331178 ) ) ;
#28479=CARTESIAN_POINT ( 'NONE',  ( 0.03301162916267817715, -0.2303793641368927225, -0.4673060013142924518 ) ) ;
#28482=VERTEX_POINT ( 'NONE', #35141 ) ;
#28487=CARTESIAN_POINT ( 'NONE',  ( 0.03309058451312577726, 0.08822157290690298137, 0.5132714794726482843 ) ) ;
#28491=CARTESIAN_POINT ( 'NONE',  ( 0.1499999999999993561, -0.3880410510314710182, 0.3755318131855027719 ) ) ;
#28499=CARTESIAN_POINT ( 'NONE',  ( -0.04582713223189541912, 0.2312054150958166299, 0.4285473768184982490 ) ) ;
#28511=CARTESIAN_POINT ( 'NONE',  ( 0.03643058821097026889, 0.4544345964805225901, -0.2356993163710955352 ) ) ;
#28516=AXIS2_PLACEMENT_3D ( 'NONE', #23655, #26328, #10682 ) ;
#28519=EDGE_LOOP ( 'NONE', ( #31021, #5508, #34851, #7288 ) ) ;
#28520=DIRECTION ( 'NONE',  ( 0.000000000000000000, -2.697841949839120611E-14, -1.000000000000000000 ) ) ;
#28532=CARTESIAN_POINT ( 'NONE',  ( 0.04285427992854337620, 0.3459934409501857489, -0.3537438177964267183 ) ) ;
#28535=DIRECTION ( 'NONE',  ( 1.000000000000000000, -8.054771744420970720E-13, -1.518808759990548047E-12 ) ) ;
#28541=EDGE_LOOP ( 'NONE', ( #18521, #7734, #7882 ) ) ;
#28590=CARTESIAN_POINT ( 'NONE',  ( -0.04155248107635972632, 0.01723053523177093399, 0.4699878081388670914 ) ) ;
#28591=CARTESIAN_POINT ( 'NONE',  ( 0.04155248107635921284, 0.2623121065566131893, 0.3903559784317156556 ) ) ;
#28593=CARTESIAN_POINT ( 'NONE',  ( 0.01548846960712797240, -0.3688619771571953754, -0.3775276577326278082 ) ) ;
#28594=EDGE_LOOP ( 'NONE', ( #4032, #6491, #39881 ) ) ;
#28608=EDGE_CURVE ( 'NONE', #37954, #33895, #35016, .T. ) ;
#28612=CARTESIAN_POINT ( 'NONE',  ( -0.03662792686184396240, 0.04111994379180689690, -0.4792679903722392165 ) ) ;
#28620=DIRECTION ( 'NONE',  ( 1.000000000000000000, 0.000000000000000000, 0.000000000000000000 ) ) ;
#28630=CARTESIAN_POINT ( 'NONE',  ( -0.04760578872587735433, 0.4435171289962510643, 0.1893230556938514941 ) ) ;
#28659=CARTESIAN_POINT ( 'NONE',  ( -0.04582889109739251426, -0.2312034125369010207, 0.4285435303321099565 ) ) ;
#28660=VERTEX_POINT ( 'NONE', #35745 ) ;
#28669=CARTESIAN_POINT ( 'NONE',  ( 0.03664605387828179933, -0.4430871221163645290, -0.1871485295462639309 ) ) ;
#28675=B_SPLINE_CURVE_WITH_KNOTS ( 'NONE', 3,
 ( #1616, #20736, #26492, #19909, #11252, #36138, #7948, #32656, #39240, #39028, #23434, #4651, #20521, #1030, #33262, #13541, #32445, #33056 ),
 .UNSPECIFIED., .F., .F.,
 ( 4, 2, 2, 2, 2, 2, 2, 2, 4 ),
 ( 0.0003425652276237501682, 0.001007165397454255675, 0.001671765567284761020, 0.002336365737115266364, 0.003000965906945771925, 0.003665566076776277486, 0.004330166246606782614, 0.004994766416437288609, 0.005659366586267793736 ),
 .UNSPECIFIED. ) ;
#28676=CARTESIAN_POINT ( 'NONE',  ( -0.02869942827333585647, 0.4892109928530948282, -0.09550568247005984668 ) ) ;
#28677=CARTESIAN_POINT ( 'NONE',  ( -0.01896968469603592389, 0.07379952543979995117, 0.5147668824877569271 ) ) ;
#28692=CARTESIAN_POINT ( 'NONE',  ( 0.05269191099235399217, 0.4442874273374635141, 0.1490603884548275249 ) ) ;
#28694=CARTESIAN_POINT ( 'NONE',  ( 0.04575185649130820292, -0.2311416656438095019, -0.4288096517596551305 ) ) ;
#28701=EDGE_LOOP ( 'NONE', ( #11975, #6377, #13195, #7620 ) ) ;
#28715=CARTESIAN_POINT ( 'NONE',  ( -0.05634301242525831949, 0.2780425975185427667, 0.3652000572937671996 ) ) ;
#28718=CARTESIAN_POINT ( 'NONE',  ( 0.08978098643734198914, 1.231844511688120125E-16, 0.3698489655878005045 ) ) ;
#28721=( BOUNDED_SURFACE ( )  B_SPLINE_SURFACE ( 3, 2, ( 
 ( #27466, #37121, #34024 ),
 ( #18601, #5826, #18386 ),
 ( #30936, #9123, #27866 ),
 ( #16332, #9547, #40604 ),
 ( #10153, #31541, #35254 ),
 ( #21905, #37721, #28460 ),
 ( #22309, #9742, #34828 ),
 ( #335, #15521, #24969 ),
 ( #34430, #37501, #3169 ),
 ( #12421, #37932, #2975 ),
 ( #3357, #22724, #18819 ),
 ( #31158, #7053, #28871 ),
 ( #31752, #6636, #9326 ),
 ( #6250, #31361, #19012 ),
 ( #15709, #25803, #28076 ),
 ( #28256, #34640, #12617 ),
 ( #6438, #120, #25180 ),
 ( #19213, #25591, #22123 ),
 ( #15915, #9942, #12840 ),
 ( #3571, #25400, #16140 ),
 ( #28677, #6845, #544 ),
 ( #13041, #38118, #22512 ) ),
 .UNSPECIFIED., .F., .F., .T. ) 
 B_SPLINE_SURFACE_WITH_KNOTS ( ( 4, 2, 2, 2, 2, 2, 2, 2, 2, 2, 4 ),
 ( 3, 3 ),
 ( 0.002013519961495850458, 0.002780892266055758240, 0.003548264570615665588, 0.004315636875175573803, 0.004699323027455527477, 0.005083009179735481151, 0.005466695332015434824, 0.005850381484295388498, 0.006617753788855296714, 0.007385126093415204929, 0.008152498397975112276 ),
 ( 0.000000000000000000, 1.000000000000000000 ),
 .UNSPECIFIED. ) 
 GEOMETRIC_REPRESENTATION_ITEM ( )  RATIONAL_B_SPLINE_SURFACE ( (
 ( 1.000000000000000000, 0.7283825911960383204, 1.000000000000000000),
 ( 1.000000000000000000, 0.7404375345927353136, 1.000000000000000000),
 ( 1.000000000000000000, 0.7521483142435556601, 1.000000000000000000),
 ( 1.000000000000000000, 0.7744460733776885597, 1.000000000000000000),
 ( 1.000000000000000000, 0.7845612039380673863, 1.000000000000000000),
 ( 1.000000000000000000, 0.8022035258263486845, 1.000000000000000000),
 ( 1.000000000000000000, 0.8093965293322147314, 1.000000000000000000),
 ( 1.000000000000000000, 0.8169028692725253116, 1.000000000000000000),
 ( 1.000000000000000000, 0.8188329634861961637, 1.000000000000000000),
 ( 1.000000000000000000, 0.8214004505365417597, 1.000000000000000000),
 ( 1.000000000000000000, 0.8220602406261303674, 1.000000000000000000),
 ( 1.000000000000000000, 0.8220736605435321476, 1.000000000000000000),
 ( 1.000000000000000000, 0.8214126668415498989, 1.000000000000000000),
 ( 1.000000000000000000, 0.8188520474558501627, 1.000000000000000000),
 ( 1.000000000000000000, 0.8169545908333391004, 1.000000000000000000),
 ( 1.000000000000000000, 0.8094771004221675836, 1.000000000000000000),
 ( 1.000000000000000000, 0.8022723753808758129, 1.000000000000000000),
 ( 1.000000000000000000, 0.7845733350636272529, 1.000000000000000000),
 ( 1.000000000000000000, 0.7744472902496011280, 1.000000000000000000),
 ( 1.000000000000000000, 0.7522916829160717356, 1.000000000000000000),
 ( 1.000000000000000000, 0.7403553004667872139, 1.000000000000000000),
 ( 1.000000000000000000, 0.7283825911960402077, 1.000000000000000000) ) ) 
 REPRESENTATION_ITEM ( '' )  SURFACE ( )  );
#28725=CARTESIAN_POINT ( 'NONE',  ( 0.05076679145662148229, 0.4330939261214885594, -0.1921033382362662412 ) ) ;
#28733=CARTESIAN_POINT ( 'NONE',  ( -0.05561170715395130637, -0.02038383341412248334, 0.4604752114371309379 ) ) ;
#28734=ORIENTED_EDGE ( 'NONE', *, *, #36470, .F. ) ;
#28735=CARTESIAN_POINT ( 'NONE',  ( -0.01895884884825219802, -0.2428741539084911250, -0.4598572020609195121 ) ) ;
#28751=VERTEX_POINT ( 'NONE', #38523 ) ;
#28759=DIRECTION ( 'NONE',  ( 1.000000000000000000, 2.280301054154495132E-31, -1.664003471950577689E-31 ) ) ;
#28761=CYLINDRICAL_SURFACE ( 'NONE', #33569, 0.01500000000000005843 ) ;
#28770=CARTESIAN_POINT ( 'NONE',  ( -0.01548846960721190873, 0.4730347584884290191, -0.2341461249027944058 ) ) ;
#28788=CARTESIAN_POINT ( 'NONE',  ( -0.03664605387828190342, 0.04106737781738832582, 0.4792329708773127583 ) ) ;
#28798=CARTESIAN_POINT ( 'NONE',  ( -0.04155248107635823446, -0.4416604393009568863, 0.1616214326753697139 ) ) ;
#28799=FACE_OUTER_BOUND ( 'NONE', #29294, .T. ) ;
#28807=ADVANCED_FACE ( 'NONE', ( #29331 ), #28227, .T. ) ;
#28827=CARTESIAN_POINT ( 'NONE',  ( -0.05279755784604217572, 0.4315508301037739858, 0.1821553064136667566 ) ) ;
#28830=DIRECTION ( 'NONE',  ( 0.000000000000000000, -0.9510565162951568619, -0.3090169943749376258 ) ) ;
#28832=DIRECTION ( 'NONE',  ( -1.000000000000000000, -2.341930812374887555E-31, 1.664003471950578127E-31 ) ) ;
#28837=ORIENTED_EDGE ( 'NONE', *, *, #39683, .T. ) ;
#28850=ORIENTED_EDGE ( 'NONE', *, *, #34396, .T. ) ;
#28859=CARTESIAN_POINT ( 'NONE',  ( 0.05083665881508948187, -0.4630607685881619751, 0.09936361682460788380 ) ) ;
#28862=DIRECTION ( 'NONE',  ( 1.000000000000000000, -7.012307549337885980E-13, -2.434866152052794803E-12 ) ) ;
#28870=CARTESIAN_POINT ( 'NONE',  ( -0.03662792686184409424, 0.4685177067346118496, -0.1089945633920606921 ) ) ;
#28871=CARTESIAN_POINT ( 'NONE',  ( -0.05634490452572834401, 0.005064009952713930708, 0.4588782462578064880 ) ) ;
#28876=ORIENTED_EDGE ( 'NONE', *, *, #39057, .F. ) ;
#28883=CARTESIAN_POINT ( 'NONE',  ( 0.03171102739522826258, 0.4481073524712099188, 0.2027236177532184824 ) ) ;
#28884=CARTESIAN_POINT ( 'NONE',  ( 0.03875523708677781898, -0.3062771359410657035, -0.3649060648845485200 ) ) ;
#28898=ADVANCED_FACE ( 'NONE', ( #16317 ), #19791, .T. ) ;
#28899=CARTESIAN_POINT ( 'NONE',  ( -0.05544444631433822351, 0.2544607094502333577, -0.3847718460475671454 ) ) ;
#28907=CARTESIAN_POINT ( 'NONE',  ( 0.05201782277452383224, 0.4527080286589780234, -0.1280848763234450904 ) ) ;
#28910=CARTESIAN_POINT ( 'NONE',  ( 0.03868649100028160454, -0.3066017772948808062, 0.3648306000529322746 ) ) ;
#28925=DIRECTION ( 'NONE',  ( -1.664003471950567617E-31, -0.8983234858820536850, 0.4393346272634515159 ) ) ;
#28938=AXIS2_PLACEMENT_3D ( 'NONE', #4615, #38996, #33022 ) ;
#28949=AXIS2_PLACEMENT_3D ( 'NONE', #2586, #33863, #15339 ) ;
#28966=CARTESIAN_POINT ( 'NONE',  ( 0.03650581953630530757, -0.2290855126858360180, 0.4575806651622388865 ) ) ;
#28971=DIRECTION ( 'NONE',  ( 2.682900528199988315E-31, -0.9510565162951527540, 0.3090169943749503378 ) ) ;
#28973=AXIS2_PLACEMENT_3D ( 'NONE', #21144, #18054, #30607 ) ;
#28974=DIRECTION ( 'NONE',  ( 2.532366176626899733E-12, -0.3090169943749518366, -0.9510565162951520879 ) ) ;
#28985=ORIENTED_EDGE ( 'NONE', *, *, #2430, .T. ) ;
#28994=VECTOR ( 'NONE', #32219, 39.37007874015748143 ) ;
#28999=EDGE_CURVE ( 'NONE', #16603, #4682, #20024, .T. ) ;
#29004=CARTESIAN_POINT ( 'NONE',  ( 0.05634304521267768928, -2.731847993664263218E-15, -0.4588823192046729837 ) ) ;
#29008=CARTESIAN_POINT ( 'NONE',  ( 0.1499999999999994671, 0.5198120922912046193, -0.07362328916749301400 ) ) ;
#29012=CARTESIAN_POINT ( 'NONE',  ( 0.01896931156526606224, -0.3622781579086280512, 0.3730773604463891169 ) ) ;
#29016=DIRECTION ( 'NONE',  ( 4.622231866529356468E-33, -0.6954292836768481978, -0.7185945389471769529 ) ) ;
#29017=CARTESIAN_POINT ( 'NONE',  ( -0.01548846960707503904, 0.5203207976467937312, 0.08861466064782108631 ) ) ;
#29068=EDGE_CURVE ( 'NONE', #13737, #35448, #17319, .T. ) ;
#29081=CARTESIAN_POINT ( 'NONE',  ( 0.01548846960707524721, 0.000000000000000000, 0.000000000000000000 ) ) ;
#29086=CARTESIAN_POINT ( 'NONE',  ( -0.02872242845530520450, 0.5252126300208032061, -0.08844866507292868663 ) ) ;
#29098=DIRECTION ( 'NONE',  ( -1.000000000000000000, -2.341930812374887555E-31, 1.664003471950578127E-31 ) ) ;
#29100=EDGE_CURVE ( 'NONE', #3369, #35103, #8073, .T. ) ;
#29109=CIRCLE ( 'NONE', #11370, 0.01499999999999995781 ) ;
#29111=CARTESIAN_POINT ( 'NONE',  ( -0.01548846960712804005, -0.07651041855114824874, 0.5222379212567086482 ) ) ;
#29118=CARTESIAN_POINT ( 'NONE',  ( 0.02235124290213094667, -0.3550643254722144482, 0.3695962758878555410 ) ) ;
#29120=CIRCLE ( 'NONE', #10069, 0.01499999999999999424 ) ;
#29127=CARTESIAN_POINT ( 'NONE',  ( -0.03309058451312555521, -0.08822157290689428000, 0.5132714794726503937 ) ) ;
#29149=AXIS2_PLACEMENT_3D ( 'NONE', #20009, #25994, #1115 ) ;
#29158=AXIS2_PLACEMENT_3D ( 'NONE', #9239, #21814, #11733 ) ;
#29172=CARTESIAN_POINT ( 'NONE',  ( 0.04762035657658417187, 0.2475516194925301006, 0.4138014489398430529 ) ) ;
#29178=CIRCLE ( 'NONE', #21971, 0.01499999999999996128 ) ;
#29180=EDGE_CURVE ( 'NONE', #19277, #26731, #31756, .T. ) ;
#29187=CARTESIAN_POINT ( 'NONE',  ( 0.04293701532779508473, -0.3457382709204475102, -0.3536859687696385368 ) ) ;
#29190=DIRECTION ( 'NONE',  ( 1.000000000000000000, 7.012307549337720382E-13, 2.434866152052798842E-12 ) ) ;
#29194=ORIENTED_EDGE ( 'NONE', *, *, #29100, .T. ) ;
#29201=AXIS2_PLACEMENT_3D ( 'NONE', #34528, #18911, #3255 ) ;
#29210=CARTESIAN_POINT ( 'NONE',  ( -0.03868264068766699704, 0.03360988006412133494, -0.4753775160315154569 ) ) ;
#29226=CARTESIAN_POINT ( 'NONE',  ( 0.04157078424165575742, -0.2900150886686562179, 0.3701869471361556307 ) ) ;
#29228=AXIS2_PLACEMENT_3D ( 'NONE', #37545, #2804, #37353 ) ;
#29232=CARTESIAN_POINT ( 'NONE',  ( -0.02953079040095693900, -0.2329676531120430660, 0.4763574306556350169 ) ) ;
#29233=CARTESIAN_POINT ( 'NONE',  ( 0.01548846960707524721, 0.000000000000000000, 0.000000000000000000 ) ) ;
#29247=AXIS2_PLACEMENT_3D ( 'NONE', #31963, #38728, #9945 ) ;
#29248=ORIENTED_EDGE ( 'NONE', *, *, #7728, .T. ) ;
#29274=( NAMED_UNIT ( * ) PLANE_ANGLE_UNIT ( ) SI_UNIT ( $, .RADIAN. ) );
#29279=CARTESIAN_POINT ( 'NONE',  ( 0.03159140494779963393, -0.4819881711443563810, -0.09921162977303815689 ) ) ;
#29280=ADVANCED_FACE ( 'NONE', ( #31668 ), #15431, .T. ) ;
#29294=EDGE_LOOP ( 'NONE', ( #12864, #4442, #23141 ) ) ;
#29297=ORIENTED_EDGE ( 'NONE', *, *, #20595, .F. ) ;
#29298=EDGE_LOOP ( 'NONE', ( #24945, #33416, #11700, #37365 ) ) ;
#29304=CARTESIAN_POINT ( 'NONE',  ( -0.03170752374382806299, 0.4816921673044415875, -0.09938322573837012064 ) ) ;
#29312=FACE_OUTER_BOUND ( 'NONE', #38203, .T. ) ;
#29319=AXIS2_PLACEMENT_3D ( 'NONE', #10442, #25684, #19316 ) ;
#29320=CARTESIAN_POINT ( 'NONE',  ( -0.04762200653274661216, 0.2475542241873639471, -0.4137947767340805494 ) ) ;
#29321=EDGE_CURVE ( 'NONE', #5083, #37512, #37219, .T. ) ;
#29323=CARTESIAN_POINT ( 'NONE',  ( -0.04947837552028493818, -0.4635165785490879542, -0.1137267105574193415 ) ) ;
#29330=DIRECTION ( 'NONE',  ( 0.000000000000000000, -0.5877852522924736922, -0.8090169943749470072 ) ) ;
#29331=FACE_OUTER_BOUND ( 'NONE', #19827, .T. ) ;
#29335=CARTESIAN_POINT ( 'NONE',  ( 0.04230188431063450216, -0.2683773510969773013, 0.3842417364743009323 ) ) ;
#29336=CARTESIAN_POINT ( 'NONE',  ( -0.03170752374382824340, -0.2433701302032818536, -0.4274053688542764351 ) ) ;
#29340=PLANE ( 'NONE',  #24650 ) ;
#29342=CARTESIAN_POINT ( 'NONE',  ( -0.02953079040095680369, -0.09152108205201929525, 0.5223162075576431862 ) ) ;
#29346=ORIENTED_EDGE ( 'NONE', *, *, #21057, .F. ) ;
#29348=FACE_OUTER_BOUND ( 'NONE', #4432, .T. ) ;
#29350=B_SPLINE_CURVE_WITH_KNOTS ( 'NONE', 3,
 ( #30193, #2023, #11685, #24053, #36160, #36579, #39864, #30610, #36762, #4888, #5277, #14552, #26917, #17455, #20950, #27121, #17842, #21150 ),
 .UNSPECIFIED., .F., .F.,
 ( 4, 2, 2, 2, 2, 2, 2, 2, 4 ),
 ( 0.000000000000000000, 0.0007746617437634293734, 0.001549323487526858747, 0.002323985231290287903, 0.003098646975053717494, 0.003873308718817147084, 0.004647970462580575807, 0.005422632206344005397, 0.006197293950107434987 ),
 .UNSPECIFIED. ) ;
#29351=DIRECTION ( 'NONE',  ( -0.000000000000000000, 0.8090169943749540016, 0.5877852522924639223 ) ) ;
#29354=DIRECTION ( 'NONE',  ( 0.000000000000000000, 0.7185945389473167300, -0.6954292836767037578 ) ) ;
#29370=CARTESIAN_POINT ( 'NONE',  ( 0.03875523708677968554, -0.4416911308383527079, 0.1785246905291560660 ) ) ;
#29378=DIRECTION ( 'NONE',  ( 1.000000000000000000, -2.099003099963423122E-12, 1.419325098918972248E-12 ) ) ;
#29379=CARTESIAN_POINT ( 'NONE',  ( -0.01548846960707517956, -0.09061086148575756005, -0.5171215251571035232 ) ) ;
#29382=CARTESIAN_POINT ( 'NONE',  ( 0.04946288932099754398, 0.3082365379450883736, 0.3644333945507121642 ) ) ;
#29388=EDGE_CURVE ( 'NONE', #35103, #24257, #31324, .T. ) ;
#29392=CARTESIAN_POINT ( 'NONE',  ( -0.03170752374382538458, -0.3312811549923266874, 0.3635342706644953403 ) ) ;
#29409=CARTESIAN_POINT ( 'NONE',  ( -0.01548846960712831414, -0.5203207976466733831, 0.08861466064782504148 ) ) ;
#29422=CARTESIAN_POINT ( 'NONE',  ( 0.04582713223189478768, 0.4790191777205491386, 0.08746099429787712598 ) ) ;
#29441=ADVANCED_FACE ( 'NONE', ( #38836 ), #1243, .T. ) ;
#29456=ORIENTED_EDGE ( 'NONE', *, *, #2096, .T. ) ;
#29489=DIRECTION ( 'NONE',  ( 0.000000000000000000, 0.5877852522924961187, 0.8090169943749307979 ) ) ;
#29497=CARTESIAN_POINT ( 'NONE',  ( -0.05489899477340622752, 0.4472784955204432422, -0.1186631084353777094 ) ) ;
#29522=CARTESIAN_POINT ( 'NONE',  ( 0.02231181081520604292, -0.2417894035777214679, 0.4519954025055065716 ) ) ;
#29523=CARTESIAN_POINT ( 'NONE',  ( -0.02881302694829455252, -0.2420344415834868312, -0.4354517411081167966 ) ) ;
#29534=CARTESIAN_POINT ( 'NONE',  ( 0.1499999999999996336, 0.07651041855119851409, 0.5222379212568192264 ) ) ;
#29559=EDGE_CURVE ( 'NONE', #28660, #19775, #8382, .T. ) ;
#29572=CARTESIAN_POINT ( 'NONE',  ( 0.05201840200954800653, 0.2909588945328520637, 0.3697186091640849437 ) ) ;
#29580=CARTESIAN_POINT ( 'NONE',  ( -0.03877220711930361857, -0.2524486846094400883, 0.4039751870151983559 ) ) ;
#29583=ADVANCED_FACE ( 'NONE', ( #11487 ), #38357, .T. ) ;
#29588=EDGE_CURVE ( 'NONE', #5909, #26696, #29178, .T. ) ;
#29590=CIRCLE ( 'NONE', #15137, 0.01500000000000004455 ) ;
#29592=VERTEX_POINT ( 'NONE', #33280 ) ;
#29594=EDGE_CURVE ( 'NONE', #13090, #11795, #29350, .T. ) ;
#29599=AXIS2_PLACEMENT_3D ( 'NONE', #25090, #27770, #9448 ) ;
#29605=EDGE_LOOP ( 'NONE', ( #13107, #30617, #21653 ) ) ;
#29608=CARTESIAN_POINT ( 'NONE',  ( 0.02235124290213184178, 0.4612278572487581441, 0.2234747101372496769 ) ) ;
#29621=AXIS2_PLACEMENT_3D ( 'NONE', #14878, #18160, #33576 ) ;
#29631=CARTESIAN_POINT ( 'NONE',  ( 0.03662792686184383056, -0.04111994379180358705, -0.4792679903722390500 ) ) ;
#29635=EDGE_LOOP ( 'NONE', ( #7089, #8617, #26530 ) ) ;
#29641=ADVANCED_FACE ( 'NONE', ( #23453 ), #12729, .T. ) ;
#29664=DIRECTION ( 'NONE',  ( -1.000000000000000000, -2.280301054154495132E-31, 1.664003471950577689E-31 ) ) ;
#29667=DIRECTION ( 'NONE',  ( -3.543711097672501380E-32, -0.8983234858819668656, -0.4393346272636287630 ) ) ;
#29670=DIRECTION ( 'NONE',  ( 1.000000000000000000, 2.280301054154495132E-31, -1.664003471950577689E-31 ) ) ;
#29687=FACE_BOUND ( 'NONE', #36777, .T. ) ;
#29688=ORIENTED_EDGE ( 'NONE', *, *, #33140, .T. ) ;
#29698=CARTESIAN_POINT ( 'NONE',  ( -0.05544444631433655818, 0.4320262549500590299, -0.1617187101067759925 ) ) ;
#29710=FACE_OUTER_BOUND ( 'NONE', #5950, .T. ) ;
#29714=CARTESIAN_POINT ( 'NONE',  ( -0.04230258372739828521, -0.4469760454808830441, -0.1407869694282971595 ) ) ;
#29715=CIRCLE ( 'NONE', #1493, 0.5400000000000007017 ) ;
#29720=AXIS2_PLACEMENT_3D ( 'NONE', #24723, #62, #15041 ) ;
#29725=CARTESIAN_POINT ( 'NONE',  ( -0.04085667396267326362, -0.2598928711944282766, -0.3937292009461462738 ) ) ;
#29729=AXIS2_PLACEMENT_3D ( 'NONE', #18855, #40229, #39836 ) ;
#29733=CARTESIAN_POINT ( 'NONE',  ( 0.05283710938261058226, 0.2421875768565610598, 0.4008269984734613711 ) ) ;
#29735=AXIS2_PLACEMENT_3D ( 'NONE', #20586, #25965, #4329 ) ;
#29737=CARTESIAN_POINT ( 'NONE',  ( 0.03303737228521301528, 0.08827089426066951627, 0.5134066811673415609 ) ) ;
#29742=LINE ( 'NONE', #19881, #14743 ) ;
#29743=FACE_OUTER_BOUND ( 'NONE', #26313, .T. ) ;
#29744=CARTESIAN_POINT ( 'NONE',  ( -0.02953079040095693900, -0.2329676531120485339, -0.4763574306556319637 ) ) ;
#29760=CARTESIAN_POINT ( 'NONE',  ( 0.04230170315643919099, -0.4483301424763386223, 0.1366247710447600627 ) ) ;
#29766=DIRECTION ( 'NONE',  ( 1.000000000000000000, 2.280301054154495132E-31, -1.664003471950577689E-31 ) ) ;
#29773=DIRECTION ( 'NONE',  ( -2.563099466555618830E-12, -0.9510565162951529761, 0.3090169943749491166 ) ) ;
#29777=CARTESIAN_POINT ( 'NONE',  ( 0.04157078424165463332, 0.2624491172974852682, 0.3902147976630855331 ) ) ;
#29779=ADVANCED_FACE ( 'NONE', ( #38183 ), #409, .T. ) ;
#29787=CARTESIAN_POINT ( 'NONE',  ( -0.04230258372739723050, -0.2720195588163292211, 0.3815939145425439327 ) ) ;
#29796=CARTESIAN_POINT ( 'NONE',  ( 0.02872242845530435101, 0.2464193076120115011, -0.4721747535844857957 ) ) ;
#29802=CARTESIAN_POINT ( 'NONE',  ( 0.05283710938261075574, 0.4560492058803797266, -0.1064717188025600253 ) ) ;
#29807=CIRCLE ( 'NONE', #37670, 0.3698489655878011706 ) ;
#29810=CARTESIAN_POINT ( 'NONE',  ( -0.03868264068766654601, -0.3066108573455318953, 0.3648330973802367261 ) ) ;
#29826=LINE ( 'NONE', #38862, #14070 ) ;
#29827=CARTESIAN_POINT ( 'NONE',  ( 0.05634301242525737580, 0.4332457820339863930, 0.1515812001271573117 ) ) ;
#29840=DIRECTION ( 'NONE',  ( 0.9378410757839554801, -0.2807814858886596432, -0.2039996905746410405 ) ) ;
#29845=ADVANCED_FACE ( 'NONE', ( #26262 ), #37991, .T. ) ;
#29859=DIRECTION ( 'NONE',  ( 0.000000000000000000, 3.330669073875470114E-16, 1.000000000000000000 ) ) ;
#29862=CARTESIAN_POINT ( 'NONE',  ( 0.08978098643734212791, 1.231844511688112729E-16, 0.3698489655877988391 ) ) ;
#29880=CARTESIAN_POINT ( 'NONE',  ( -0.01548846960721245516, -0.3688619771570368910, -0.3775276577325204497 ) ) ;
#29903=VERTEX_POINT ( 'NONE', #38998 ) ;
#29905=DIRECTION ( 'NONE',  ( 1.571558834619978106E-31, 0.9849933812516250553, 0.1725921171157334399 ) ) ;
#29914=CARTESIAN_POINT ( 'NONE',  ( -0.01899468245560449395, 0.5123206680798557677, -0.08888613072388730496 ) ) ;
#29926=CARTESIAN_POINT ( 'NONE',  ( 0.05283710938261045043, -0.4315340639268043232, -0.1819215676045972951 ) ) ;
#29932=CARTESIAN_POINT ( 'NONE',  ( -0.04211812644076706746, -0.4486350089847107592, -0.1367863764325146780 ) ) ;
#29940=DIRECTION ( 'NONE',  ( 0.3468893892380647270, -0.9373665302208729067, 0.03180785525186742568 ) ) ;
#29944=FACE_OUTER_BOUND ( 'NONE', #186, .T. ) ;
#29946=CARTESIAN_POINT ( 'NONE',  ( -0.05544444631433736309, -0.2873070878496327141, -0.3609075552494494521 ) ) ;
#29955=CARTESIAN_POINT ( 'NONE',  ( 0.05634301242525759784, 0.2614060064472222833, 0.3772872482281158790 ) ) ;
#29972=DIRECTION ( 'NONE',  ( 1.000000000000000000, 2.280301054154495132E-31, -1.664003471950577689E-31 ) ) ;
#29979=CARTESIAN_POINT ( 'NONE',  ( 0.04308611741967688369, -0.4845711164929068504, 0.09763251765260519410 ) ) ;
#29986=CARTESIAN_POINT ( 'NONE',  ( -0.01548846960707416127, 0.2450655194479873511, 0.4674710490749285352 ) ) ;
#29993=CARTESIAN_POINT ( 'NONE',  ( -0.05283710938261126921, 0.4315340639268049339, -0.1819215676045952412 ) ) ;
#29998=CARTESIAN_POINT ( 'NONE',  ( -0.05634490452572801095, -0.2656249956367415233, 0.3742168499392072301 ) ) ;
#30010=EDGE_CURVE ( 'NONE', #12964, #4682, #20643, .T. ) ;
#30012=ORIENTED_EDGE ( 'NONE', *, *, #10188, .T. ) ;
#30015=ORIENTED_EDGE ( 'NONE', *, *, #29594, .T. ) ;
#30024=ADVANCED_FACE ( 'NONE', ( #1583 ), #17398, .T. ) ;
#30031=DIRECTION ( 'NONE',  ( 0.3515883117872520836, 4.264480453763185162E-16, 0.9361547195921142706 ) ) ;
#30033=CARTESIAN_POINT ( 'NONE',  ( 0.02953079040095700838, 0.2329676531120452587, -0.4763574306556336291 ) ) ;
#30036=DIRECTION ( 'NONE',  ( 0.000000000000000000, -0.5877852522924936762, -0.8090169943749325743 ) ) ;
#30050=VERTEX_POINT ( 'NONE', #39401 ) ;
#30051=CARTESIAN_POINT ( 'NONE',  ( 0.01548846960703768524, 0.5198120922912046193, -0.07362328916749273644 ) ) ;
#30052=EDGE_LOOP ( 'NONE', ( #14992, #25980, #25502, #5443 ) ) ;
#30055=EDGE_LOOP ( 'NONE', ( #11024, #14723, #40482 ) ) ;
#30077=CARTESIAN_POINT ( 'NONE',  ( 0.01548846960707528191, -0.4638115001430989648, 0.2459753896937853235 ) ) ;
#30081=DIRECTION ( 'NONE',  ( 0.000000000000000000, -0.1725921171157282497, -0.9849933812516257214 ) ) ;
#30085=DIRECTION ( 'NONE',  ( 0.000000000000000000, -0.8090169943749413450, 0.5877852522924816858 ) ) ;
#30091=CARTESIAN_POINT ( 'NONE',  ( 0.04762035657658860582, 0.04295292190960727646, -0.4802795956081228335 ) ) ;
#30092=EDGE_LOOP ( 'NONE', ( #22640, #7355, #34229 ) ) ;
#30097=DIRECTION ( 'NONE',  ( -2.563099466555627715E-12, 0.000000000000000000, -1.000000000000000000 ) ) ;
#30109=DIRECTION ( 'NONE',  ( 0.000000000000000000, 3.330669073875470114E-16, 1.000000000000000000 ) ) ;
#30121=CARTESIAN_POINT ( 'NONE',  ( 0.05083665881508981493, -0.4330284998000932251, -0.1917934360576678821 ) ) ;
#30126=CARTESIAN_POINT ( 'NONE',  ( -0.04285561529641267187, -0.4878360864744967218, -0.08281661244626055407 ) ) ;
#30127=ADVANCED_FACE ( 'NONE', ( #742 ), #16756, .T. ) ;
#30129=EDGE_CURVE ( 'NONE', #28034, #13311, #32362, .T. ) ;
#30135=CARTESIAN_POINT ( 'NONE',  ( 0.03301162916267637998, 0.5156255563253913099, -0.07469829950278911168 ) ) ;
#30139=CARTESIAN_POINT ( 'NONE',  ( -0.01548846960707490547, 0.09061086148575973886, 0.5171215251571029681 ) ) ;
#30148=CARTESIAN_POINT ( 'NONE',  ( 0.03301162916267982167, -0.08829475514028595207, 0.5134720893088395854 ) ) ;
#30149=CARTESIAN_POINT ( 'NONE',  ( 0.04047170147977369181, -0.4923646673433203502, -0.09403053665140553852 ) ) ;
#30158=DIRECTION ( 'NONE',  ( -0.3468893892380664479, -0.7396492646828669582, 0.5767033179097683648 ) ) ;
#30159=VERTEX_POINT ( 'NONE', #2128 ) ;
#30164=LINE ( 'NONE', #30574, #8659 ) ;
#30172=CARTESIAN_POINT ( 'NONE',  ( 0.03474878377839876742, -0.4640666366555541433, 0.2268437812334336001 ) ) ;
#30183=CARTESIAN_POINT ( 'NONE',  ( 0.04155248107635942795, 0.2901916982059709604, -0.3701002694350334910 ) ) ;
#30192=DIRECTION ( 'NONE',  ( 0.000000000000000000, -0.3090169943749502823, -0.9510565162951527540 ) ) ;
#30193=CARTESIAN_POINT ( 'NONE',  ( -0.02953079040095652960, 0.3810518745593862167, -0.3687679460475775106 ) ) ;
#30205=CARTESIAN_POINT ( 'NONE',  ( 0.1499999999999994671, 0.4730347584886748780, -0.2341461249029861691 ) ) ;
#30207=VERTEX_POINT ( 'NONE', #20441 ) ;
#30215=SPHERICAL_SURFACE ( 'NONE', #15911, 0.01499999999999999944 ) ;
#30226=DIRECTION ( 'NONE',  ( 1.000000000000000000, -1.998486013202569589E-12, -1.557674999835046357E-12 ) ) ;
#30248=VERTEX_POINT ( 'NONE', #10995 ) ;
#30258=DIRECTION ( 'NONE',  ( 0.000000000000000000, -0.8090169943749413450, 0.5877852522924816858 ) ) ;
#30261=AXIS2_PLACEMENT_3D ( 'NONE', #36159, #39256, #24052 ) ;
#30266=AXIS2_PLACEMENT_3D ( 'NONE', #30723, #2544, #24562 ) ;
#30278=CARTESIAN_POINT ( 'NONE',  ( 0.04229974373173313318, -0.008638059335310385375, -0.4686103131113881770 ) ) ;
#30283=CIRCLE ( 'NONE', #36859, 0.5400000000000017009 ) ;
#30294=AXIS2_PLACEMENT_3D ( 'NONE', #599, #3826, #25458 ) ;
#30302=CIRCLE ( 'NONE', #23739, 0.01499999999999995087 ) ;
#30303=CARTESIAN_POINT ( 'NONE',  ( -0.03301200226531787046, 0.4610556019031730735, -0.2426442821262900229 ) ) ;
#30304=VERTEX_POINT ( 'NONE', #39359 ) ;
#30333=CARTESIAN_POINT ( 'NONE',  ( -0.01548846960688955027, -0.09061086148592201184, 0.5171215251575769223 ) ) ;
#30334=DIRECTION ( 'NONE',  ( 0.000000000000000000, -0.9510565162951630791, 0.3090169943749180859 ) ) ;
#30343=CARTESIAN_POINT ( 'NONE',  ( 0.05634307799789379373, 0.2780413953411660088, 0.3652007531760546044 ) ) ;
#30344=EDGE_CURVE ( 'NONE', #17096, #40212, #997, .T. ) ;
#30347=CARTESIAN_POINT ( 'NONE',  ( 0.04946426091937480840, -0.4418466283164439456, -0.1805254228051831888 ) ) ;
#30354=CARTESIAN_POINT ( 'NONE',  ( -0.05083665881509014106, -0.3162195626322033548, -0.3525671453250078247 ) ) ;
#30357=VERTEX_POINT ( 'NONE', #2733 ) ;
#30360=CIRCLE ( 'NONE', #3424, 0.5302738246768107233 ) ;
#30363=AXIS2_PLACEMENT_3D ( 'NONE', #871, #13378, #25955 ) ;
#30366=CARTESIAN_POINT ( 'NONE',  ( 0.000000000000000000, 0.000000000000000000, 0.000000000000000000 ) ) ;
#30369=ORIENTED_EDGE ( 'NONE', *, *, #35580, .T. ) ;
#30390=SHAPE_REPRESENTATION ( 'Pulley', ( #27819 ), #12683 ) ;
#30413=ADVANCED_FACE ( 'NONE', ( #40573 ), #2537, .F. ) ;
#30424=FACE_OUTER_BOUND ( 'NONE', #38139, .T. ) ;
#30425=AXIS2_PLACEMENT_3D ( 'NONE', #30839, #27761, #24890 ) ;
#30433=CARTESIAN_POINT ( 'NONE',  ( 0.02953079040095687308, 0.5250338024619264354, -0.07436286310882528339 ) ) ;
#30434=CARTESIAN_POINT ( 'NONE',  ( 0.05082303569918638492, 0.2375724430107445106, -0.4097459652473644520 ) ) ;
#30437=CARTESIAN_POINT ( 'NONE',  ( -0.02953079040095639429, 0.4684706630666080063, -0.2484463060367437248 ) ) ;
#30447=CARTESIAN_POINT ( 'NONE',  ( 0.01548846960703826464, 0.4638115001431027951, 0.2459753896937752204 ) ) ;
#30459=DIRECTION ( 'NONE',  ( -1.000000000000000000, -2.341930812374887555E-31, 1.664003471950578127E-31 ) ) ;
#30469=ORIENTED_EDGE ( 'NONE', *, *, #33373, .T. ) ;
#30486=CARTESIAN_POINT ( 'NONE',  ( 0.03474878377839887844, -0.2421023663934862569, 0.4562919991932272157 ) ) ;
#30489=FACE_OUTER_BOUND ( 'NONE', #32265, .T. ) ;
#30493=CARTESIAN_POINT ( 'NONE',  ( 0.05078310099560752466, 0.04880952477023812325, -0.4712228254505121394 ) ) ;
#30495=ORIENTED_EDGE ( 'NONE', *, *, #21009, .F. ) ;
#30505=ORIENTED_EDGE ( 'NONE', *, *, #37100, .F. ) ;
#30526=ADVANCED_FACE ( 'NONE', ( #27628 ), #34191, .T. ) ;
#30532=CARTESIAN_POINT ( 'NONE',  ( -0.1499999999999996336, 0.000000000000000000, 0.000000000000000000 ) ) ;
#30549=AXIS2_PLACEMENT_3D ( 'NONE', #20571, #14576, #24076 ) ;
#30550=CARTESIAN_POINT ( 'NONE',  ( 0.8248651029816849167, -1.296087829716116640E-16, -0.6154198107346400271 ) ) ;
#30551=ORIENTED_EDGE ( 'NONE', *, *, #16734, .F. ) ;
#30556=CARTESIAN_POINT ( 'NONE',  ( 0.1499999999999994671, -0.5346638663566677385, -0.07572681171513533094 ) ) ;
#30557=CARTESIAN_POINT ( 'NONE',  ( 0.04308558661660993883, 0.05688326490871552232, 0.4910261092774150793 ) ) ;
#30558=CARTESIAN_POINT ( 'NONE',  ( 0.04230170315644234819, -0.4430127298718438689, -0.1529900842779738368 ) ) ;
#30562=CARTESIAN_POINT ( 'NONE',  ( 0.04085667396267503998, 0.4547700361314893081, 0.1255037944140956763 ) ) ;
#30574=CARTESIAN_POINT ( 'NONE',  ( 0.1499999999999997724, 0.2372406987223678043, 0.4850946823762586901 ) ) ;
#30575=PRODUCT_DEFINITION_FORMATION_WITH_SPECIFIED_SOURCE ( 'ANY', '', #27234, .NOT_KNOWN. ) ;
#30576=ORIENTED_EDGE ( 'NONE', *, *, #21435, .T. ) ;
#30584=FACE_BOUND ( 'NONE', #25473, .T. ) ;
#30590=CARTESIAN_POINT ( 'NONE',  ( -0.05544444631433702309, 0.2873070878496298830, 0.3609075552494527828 ) ) ;
#30600=ORIENTED_EDGE ( 'NONE', *, *, #16755, .T. ) ;
#30606=ORIENTED_EDGE ( 'NONE', *, *, #16326, .F. ) ;
#30607=DIRECTION ( 'NONE',  ( -0.9378410757839559242, -0.2807814858886551468, 0.2039996905746456479 ) ) ;
#30610=CARTESIAN_POINT ( 'NONE',  ( -0.05561176441985835051, 0.2871508736821605789, -0.3605511861568530541 ) ) ;
#30616=DIRECTION ( 'NONE',  ( 0.000000000000000000, -0.3090169943749502823, -0.9510565162951527540 ) ) ;
#30617=ORIENTED_EDGE ( 'NONE', *, *, #32808, .F. ) ;
#30618=CARTESIAN_POINT ( 'NONE',  ( -0.02235124290213130402, 0.2417860359143760851, -0.4518977707513310293 ) ) ;
#30627=VECTOR ( 'NONE', #10142, 39.37007874015748143 ) ;
#30668=CYLINDRICAL_SURFACE ( 'NONE', #33025, 0.5400000000000012568 ) ;
#30682=CARTESIAN_POINT ( 'NONE',  ( -0.04211471441534140464, -0.4486586774158462521, 0.1367340165256737128 ) ) ;
#30702=CARTESIAN_POINT ( 'NONE',  ( 0.02872242845530412203, -0.07817994906156924828, -0.5268390348591153183 ) ) ;
#30708=DIRECTION ( 'NONE',  ( 0.9378410757839557021, -0.1072489841977670583, 0.3300784330442384507 ) ) ;
#30717=B_SPLINE_CURVE_WITH_KNOTS ( 'NONE', 3,
 ( #33419, #7902, #14484, #23578, #27054, #36292, #39583, #20473, #36097, #14298 ),
 .UNSPECIFIED., .F., .F.,
 ( 4, 2, 2, 2, 4 ),
 ( 0.003098629625065147525, 0.003873295706325722860, 0.004647961787586298195, 0.005422627868846873964, 0.006197293950107448865 ),
 .UNSPECIFIED. ) ;
#30718=CARTESIAN_POINT ( 'NONE',  ( -0.01548846960707524721, 0.000000000000000000, 0.000000000000000000 ) ) ;
#30723=CARTESIAN_POINT ( 'NONE',  ( 0.01548846960707524721, 0.000000000000000000, 0.000000000000000000 ) ) ;
#30725=CARTESIAN_POINT ( 'NONE',  ( -0.02953079040095693900, -0.3810518745593846068, 0.3687679460475796756 ) ) ;
#30728=CARTESIAN_POINT ( 'NONE',  ( 0.05634307799789356475, -0.4395998308137145094, -0.1320249839696048810 ) ) ;
#30732=DIRECTION ( 'NONE',  ( 0.000000000000000000, 0.5877852522924520429, 0.8090169943749627723 ) ) ;
#30742=AXIS2_PLACEMENT_3D ( 'NONE', #40015, #25207, #27491 ) ;
#30743=CARTESIAN_POINT ( 'NONE',  ( -0.01548846960707477016, 0.5198120922912068398, -0.07362328916748536733 ) ) ;
#30746=CARTESIAN_POINT ( 'NONE',  ( -0.02881329448201542381, -0.2420398234037506313, 0.4354480552436106322 ) ) ;
#30749=CARTESIAN_POINT ( 'NONE',  ( -0.05186792262757321942, 0.01796889665935373290, -0.4704835727131216339 ) ) ;
#30754=DIRECTION ( 'NONE',  ( -1.000000000000000000, -2.280301054154495132E-31, 1.664003471950577689E-31 ) ) ;
#30755=DIRECTION ( 'NONE',  ( 0.000000000000000000, 3.330669073875470114E-16, 1.000000000000000000 ) ) ;
#30760=CARTESIAN_POINT ( 'NONE',  ( 0.03474878377840979332, -0.3591457335720762423, -0.3712550153170212641 ) ) ;
#30762=ORIENTED_EDGE ( 'NONE', *, *, #10628, .F. ) ;
#30780=DIRECTION ( 'NONE',  ( -1.000000000000000000, -2.280301054154495132E-31, 1.664003471950577689E-31 ) ) ;
#30785=CARTESIAN_POINT ( 'NONE',  ( -0.04308449196698682648, 0.2425978208598493779, 0.4306872647601522885 ) ) ;
#30794=EDGE_CURVE ( 'NONE', #24301, #28660, #7519, .T. ) ;
#30800=LINE ( 'NONE', #24648, #1604 ) ;
#30806=CARTESIAN_POINT ( 'NONE',  ( 0.03674078017396244927, 0.3145504785376027068, -0.3636064179578474276 ) ) ;
#30809=ORIENTED_EDGE ( 'NONE', *, *, #10810, .F. ) ;
#30811=ORIENTED_EDGE ( 'NONE', *, *, #35622, .T. ) ;
#30816=ORIENTED_EDGE ( 'NONE', *, *, #35622, .F. ) ;
#30818=EDGE_CURVE ( 'NONE', #30159, #17702, #15444, .T. ) ;
#30839=CARTESIAN_POINT ( 'NONE',  ( -0.02953079040095700838, 0.000000000000000000, 0.000000000000000000 ) ) ;
#30842=CARTESIAN_POINT ( 'NONE',  ( 0.08978098643734198914, -7.789101598130623152E-17, -0.3698489655878005045 ) ) ;
#30847=ORIENTED_EDGE ( 'NONE', *, *, #10741, .T. ) ;
#30853=CARTESIAN_POINT ( 'NONE',  ( -0.01548846960707386464, -0.07651041855118967394, -0.5222379212568238893 ) ) ;
#30857=FACE_OUTER_BOUND ( 'NONE', #17404, .T. ) ;
#30873=CARTESIAN_POINT ( 'NONE',  ( -0.05544444631433556592, -0.4320262549500628046, 0.1617187101067735222 ) ) ;
#30895=CARTESIAN_POINT ( 'NONE',  ( 0.03303737228521604757, -0.08827089426067215305, -0.5134066811673330122 ) ) ;
#30901=CARTESIAN_POINT ( 'NONE',  ( -0.01548846960707524721, 0.2306506793134044109, -0.4716198300880319882 ) ) ;
#30910=CARTESIAN_POINT ( 'NONE',  ( -0.02242905165738729237, 0.4611019942560653506, -0.2233384654055181051 ) ) ;
#30918=CARTESIAN_POINT ( 'NONE',  ( -0.05082303569918694003, -0.3162776479886612035, 0.3525632866555290512 ) ) ;
#30934=CARTESIAN_POINT ( 'NONE',  ( 0.02953079040095687308, -0.4684706630666107263, -0.2484463060367401721 ) ) ;
#30936=CARTESIAN_POINT ( 'NONE',  ( -0.02238765564325341170, -0.06997643758148942850, 0.5076344429488280907 ) ) ;
#30937=CIRCLE ( 'NONE', #13841, 0.01499999999999996302 ) ;
#30943=CIRCLE ( 'NONE', #18469, 0.01499999999999999424 ) ;
#30946=CARTESIAN_POINT ( 'NONE',  ( -0.05252049209742370300, 0.009108187116141133396, -0.4689942714594979023 ) ) ;
#30952=CARTESIAN_POINT ( 'NONE',  ( -0.06980746140711623082, 0.000000000000000000, 0.000000000000000000 ) ) ;
#30953=CARTESIAN_POINT ( 'NONE',  ( 0.05279905671745278167, -0.4315505476814280317, -0.1821453894719594346 ) ) ;
#30956=CARTESIAN_POINT ( 'NONE',  ( 0.03642997641689302291, 0.5061875831641746704, 0.07642488348723125435 ) ) ;
#30960=VECTOR ( 'NONE', #16818, 39.37007874015748143 ) ;
#30963=CARTESIAN_POINT ( 'NONE',  ( 0.04293694706340187017, 0.07181688488226882494, 0.4893579783150006635 ) ) ;
#30969=UNCERTAINTY_MEASURE_WITH_UNIT (LENGTH_MEASURE( 1.000000000000000082E-05 ), #14030, 'distance_accuracy_value', 'NONE');
#30970=CYLINDRICAL_SURFACE ( 'NONE', #28516, 0.2149999999999999967 ) ;
#30977=DIRECTION ( 'NONE',  ( 1.664003471950577032E-31, 3.330669073875470114E-16, 1.000000000000000000 ) ) ;
#30982=CARTESIAN_POINT ( 'NONE',  ( -0.01548846960707545191, -0.5198120922912051745, -0.07362328916749329155 ) ) ;
#30984=CARTESIAN_POINT ( 'NONE',  ( -0.02881302694829528457, 0.2420344415834884688, 0.4354517411081153533 ) ) ;
#30989=CARTESIAN_POINT ( 'NONE',  ( 0.01895884884825208352, 0.2428741539084919021, -0.4598572020609182354 ) ) ;
#31005=CARTESIAN_POINT ( 'NONE',  ( 0.03478489236951484015, 0.3590487419276194303, -0.3712145292148960607 ) ) ;
#31006=VECTOR ( 'NONE', #7912, 39.37007874015748143 ) ;
#31014=ORIENTED_EDGE ( 'NONE', *, *, #15538, .F. ) ;
#31021=ORIENTED_EDGE ( 'NONE', *, *, #33823, .F. ) ;
#31059=CARTESIAN_POINT ( 'NONE',  ( -0.04293701532779534841, -0.4432143466407583721, -0.2195216604697256546 ) ) ;
#31061=CARTESIAN_POINT ( 'NONE',  ( -0.02953079040095571081, -0.09152108205201821278, -0.5223162075576460728 ) ) ;
#31065=CARTESIAN_POINT ( 'NONE',  ( 0.03159140494780130620, 0.4482517543799765525, -0.2030416442520428522 ) ) ;
#31079=CARTESIAN_POINT ( 'NONE',  ( -0.05137569054208774438, -0.4554428576828106201, 0.1244487204292429872 ) ) ;
#31083=DIRECTION ( 'NONE',  ( 1.000000000000000000, 2.341930812374887555E-31, -1.664003471950578127E-31 ) ) ;
#31089=DIRECTION ( 'NONE',  ( 1.000000000000000000, -8.638708177629702698E-13, 2.382021192243033701E-12 ) ) ;
#31094=CARTESIAN_POINT ( 'NONE',  ( 0.04047170147977612042, -0.2415774042519004960, 0.4392095914548704294 ) ) ;
#31116=CARTESIAN_POINT ( 'NONE',  ( -0.1499999999999996336, 0.1249999999999999029, 0.000000000000000000 ) ) ;
#31124=CARTESIAN_POINT ( 'NONE',  ( -0.02953079040095700838, 0.000000000000000000, 0.000000000000000000 ) ) ;
#31132=AXIS2_PLACEMENT_3D ( 'NONE', #9730, #13031, #22300 ) ;
#31136=CARTESIAN_POINT ( 'NONE',  ( -0.03309057659885157598, -0.2303206601891022998, 0.4671007096900186006 ) ) ;
#31145=DIRECTION ( 'NONE',  ( 0.000000000000000000, 0.9510565162951525320, -0.3090169943749502268 ) ) ;
#31158=CARTESIAN_POINT ( 'NONE',  ( -0.04230258372739675865, 0.004226829447875481149, 0.4686050468223225129 ) ) ;
#31160=CIRCLE ( 'NONE', #4214, 0.01499999999999995608 ) ;
#31164=CARTESIAN_POINT ( 'NONE',  ( -0.03171893264487114783, -0.2437375926088059808, 0.4645571062479570412 ) ) ;
#31167=CARTESIAN_POINT ( 'NONE',  ( -0.05491348488830673918, -0.02524042857556412292, -0.4620240554957946721 ) ) ;
#31176=CARTESIAN_POINT ( 'NONE',  ( 0.01548846960707409362, 0.5203207976467955076, 0.08861466064782100305 ) ) ;
#31178=CARTESIAN_POINT ( 'NONE',  ( 0.01548846960706596991, -0.2450655194479906540, -0.4674710490749469649 ) ) ;
#31182=CARTESIAN_POINT ( 'NONE',  ( 0.05634304521267755744, 1.092739197465705287E-15, 0.4588823192046724841 ) ) ;
#31196=AXIS2_PLACEMENT_3D ( 'NONE', #1624, #2425, #14961 ) ;
#31198=CARTESIAN_POINT ( 'NONE',  ( -0.01548846960688914087, 0.4638115001434989226, 0.2459753896940841955 ) ) ;
#31203=AXIS2_PLACEMENT_3D ( 'NONE', #19566, #22872, #32096 ) ;
#31205=CARTESIAN_POINT ( 'NONE',  ( -0.04229883635637872452, 0.2719170545448755805, 0.3816769773555939160 ) ) ;
#31210=CARTESIAN_POINT ( 'NONE',  ( 0.03159140494780101477, 0.2432984029592191733, -0.4277399113045144419 ) ) ;
#31211=DIRECTION ( 'NONE',  ( 1.000000000000000000, 2.341930812374887555E-31, -1.664003471950578127E-31 ) ) ;
#31213=CYLINDRICAL_SURFACE ( 'NONE', #27262, 0.08139150547213661047 ) ;
#31220=CIRCLE ( 'NONE', #2965, 0.5400000000000004796 ) ;
#31232=EDGE_LOOP ( 'NONE', ( #36164, #21323, #13247 ) ) ;
#31234=AXIS2_PLACEMENT_3D ( 'NONE', #9214, #27959, #5520 ) ;
#31248=CARTESIAN_POINT ( 'NONE',  ( -0.01548846960707524721, -0.4638115001430989648, 0.2459753896937853235 ) ) ;
#31264=AXIS2_PLACEMENT_3D ( 'NONE', #38066, #6578, #22453 ) ;
#31291=ORIENTED_EDGE ( 'NONE', *, *, #16187, .F. ) ;
#31296=FACE_OUTER_BOUND ( 'NONE', #1691, .T. ) ;
#31308=CARTESIAN_POINT ( 'NONE',  ( 0.04946288932099399821, -0.2513464261306892489, 0.4057664802068525201 ) ) ;
#31315=CARTESIAN_POINT ( 'NONE',  ( -0.03474878377839595717, 0.4640666366555314948, 0.2268437812334333226 ) ) ;
#31321=CARTESIAN_POINT ( 'NONE',  ( -0.01548846960707490547, 0.5198120922912062847, -0.07362328916748482610 ) ) ;
#31324=B_SPLINE_CURVE_WITH_KNOTS ( 'NONE', 3,
 ( #9449, #25091, #12745, #3091, #15633, #37627, #22030, #28591, #31467, #3274, #2121, #15828, #25308, #12960, #25506, #17738, #14655, #26129 ),
 .UNSPECIFIED., .F., .F.,
 ( 4, 2, 2, 2, 2, 2, 2, 2, 4 ),
 ( 0.0003425652276237403562, 0.001007165397454252856, 0.001671765567284765356, 0.002336365737115277640, 0.003000965906945790573, 0.003665566076776302640, 0.004330166246606815574, 0.004994766416437328507, 0.005659366586267840574 ),
 .UNSPECIFIED. ) ;
#31349=ORIENTED_EDGE ( 'NONE', *, *, #35580, .F. ) ;
#31361=CARTESIAN_POINT ( 'NONE',  ( -0.05187277790672430861, 0.01792103310037021849, 0.4704724753798314452 ) ) ;
#31366=CARTESIAN_POINT ( 'NONE',  ( -0.02872242845530528429, -0.2464193076120088921, 0.4721747535844859067 ) ) ;
#31370=CARTESIAN_POINT ( 'NONE',  ( -0.04047161733259106720, -0.06271464429809672780, -0.4973245071804597850 ) ) ;
#31379=CARTESIAN_POINT ( 'NONE',  ( 0.02881329448200726714, 0.4517642754607847921, 0.2100174381954101610 ) ) ;
#31381=CARTESIAN_POINT ( 'NONE',  ( 0.02872242845529755437, -0.2464193076120163306, -0.4721747535845037258 ) ) ;
#31392=EDGE_CURVE ( 'NONE', #20992, #20650, #10584, .T. ) ;
#31397=CARTESIAN_POINT ( 'NONE',  ( -0.03170752374382516253, 0.3312811549923315169, -0.3635342706644930089 ) ) ;
#31403=CARTESIAN_POINT ( 'NONE',  ( -0.01548846960707460536, 0.3688619771572935746, 0.3775276577326980854 ) ) ;
#31422=CARTESIAN_POINT ( 'NONE',  ( 0.03474878377840454752, 0.2421023663934840364, -0.4562919991932258279 ) ) ;
#31463=ORIENTED_EDGE ( 'NONE', *, *, #1219, .T. ) ;
#31464=CARTESIAN_POINT ( 'NONE',  ( 0.03650581953630544635, -0.3643937567481972950, -0.3592734714612038638 ) ) ;
#31467=CARTESIAN_POINT ( 'NONE',  ( 0.04229956186878620905, 0.2683474741743152592, 0.3842687663629376082 ) ) ;
#31473=ORIENTED_EDGE ( 'NONE', *, *, #11667, .T. ) ;
#31483=CIRCLE ( 'NONE', #19003, 0.01500000000000000291 ) ;
#31485=CARTESIAN_POINT ( 'NONE',  ( -0.03474824846560085195, -0.5087747035359800885, 0.08925086559847709988 ) ) ;
#31490=DIRECTION ( 'NONE',  ( 2.532366176626906196E-12, 0.3090169943749446757, -0.9510565162951545304 ) ) ;
#31493=CARTESIAN_POINT ( 'NONE',  ( 0.04047043078436834973, -0.3430608037303031765, 0.3654822131371281979 ) ) ;
#31497=CARTESIAN_POINT ( 'NONE',  ( -0.02953079040095606816, 0.4684706630666136684, 0.2484463060367380904 ) ) ;
#31511=CARTESIAN_POINT ( 'NONE',  ( 0.1399999999999994582, -6.554815759418801904E-17, -0.2526340763130725531 ) ) ;
#31520=ADVANCED_FACE ( 'NONE', ( #40430 ), #15730, .T. ) ;
#31534=CARTESIAN_POINT ( 'NONE',  ( 0.04229956186878621599, -0.4429651807893704718, -0.1531492745855136950 ) ) ;
#31541=CARTESIAN_POINT ( 'NONE',  ( -0.04308449196698887346, -0.05688586270224561120, 0.4910287377915159568 ) ) ;
#31543=ORIENTED_EDGE ( 'NONE', *, *, #26401, .T. ) ;
#31546=AXIS2_PLACEMENT_3D ( 'NONE', #6359, #32250, #28971 ) ;
#31552=ORIENTED_EDGE ( 'NONE', *, *, #6663, .T. ) ;
#31557=CARTESIAN_POINT ( 'NONE',  ( 0.03301200226530935644, 0.4610556019031807895, 0.2426442821263211647 ) ) ;
#31558=CARTESIAN_POINT ( 'NONE',  ( 0.01548846960707524721, 0.3772621329473435647, -0.3651003739302673967 ) ) ;
#31565=EDGE_LOOP ( 'NONE', ( #11590, #25303, #11086 ) ) ;
#31567=DIRECTION ( 'NONE',  ( 1.000000000000000000, 2.341930812374887555E-31, -1.664003471950578127E-31 ) ) ;
#31578=CARTESIAN_POINT ( 'NONE',  ( -0.05076541221973554507, 0.3165406372985248851, -0.3525330185552898454 ) ) ;
#31579=EDGE_CURVE ( 'NONE', #11533, #24870, #27958, .T. ) ;
#31581=CARTESIAN_POINT ( 'NONE',  ( -0.01548846960707375361, -0.4730347584886793189, -0.2341461249029842817 ) ) ;
#31588=AXIS2_PLACEMENT_3D ( 'NONE', #1431, #30192, #14157 ) ;
#31598=DIRECTION ( 'NONE',  ( 4.410796239770416717E-15, -0.9901182710308658041, -0.1402348365095101024 ) ) ;
#31605=CARTESIAN_POINT ( 'NONE',  ( -0.04582705327698315817, -0.06484491888962914952, 0.4826014279685451047 ) ) ;
#31610=CARTESIAN_POINT ( 'NONE',  ( 0.1499999999999994671, -0.5203207976467941753, 0.08861466064782175245 ) ) ;
#31612=CARTESIAN_POINT ( 'NONE',  ( 0.05561310505366983542, 0.2871713500421194110, -0.3605322861779143295 ) ) ;
#31614=AXIS2_PLACEMENT_3D ( 'NONE', #7, #34097, #5899 ) ;
#31638=CARTESIAN_POINT ( 'NONE',  ( -0.01548846960707524721, 0.000000000000000000, 0.000000000000000000 ) ) ;
#31641=ADVANCED_FACE ( 'NONE', ( #3939 ), #708, .T. ) ;
#31645=FACE_OUTER_BOUND ( 'NONE', #16349, .T. ) ;
#31652=DIRECTION ( 'NONE',  ( -0.3468893892380657817, -0.7770416411310581140, 0.5252371270030266048 ) ) ;
#31654=LINE ( 'NONE', #6746, #3491 ) ;
#31658=CIRCLE ( 'NONE', #21151, 0.5302738246768105013 ) ;
#31665=CARTESIAN_POINT ( 'NONE',  ( 0.05082303569918651676, -0.3162776479886611480, -0.3525632866555280520 ) ) ;
#31668=FACE_OUTER_BOUND ( 'NONE', #8291, .T. ) ;
#31672=CIRCLE ( 'NONE', #6688, 0.5302738246768088359 ) ;
#31683=DIRECTION ( 'NONE',  ( 1.000000000000000000, 0.000000000000000000, 0.000000000000000000 ) ) ;
#31685=CARTESIAN_POINT ( 'NONE',  ( -0.04155248107635951815, -0.01723053523176999030, -0.4699878081388675355 ) ) ;
#31690=CARTESIAN_POINT ( 'NONE',  ( 0.1499999999999994948, 0.4638115001431033502, 0.2459753896937746653 ) ) ;
#31705=CARTESIAN_POINT ( 'NONE',  ( -0.04047170147978008253, 0.4536011460193690725, 0.2133323880731032574 ) ) ;
#31713=DIRECTION ( 'NONE',  ( 1.000000000000000000, 2.280301054154496446E-31, 1.355854680848613603E-31 ) ) ;
#31722=ORIENTED_EDGE ( 'NONE', *, *, #3712, .F. ) ;
#31726=CARTESIAN_POINT ( 'NONE',  ( 0.01548846960721225047, -0.5203207976464844231, 0.08861466064783186936 ) ) ;
#31727=ORIENTED_EDGE ( 'NONE', *, *, #31770, .F. ) ;
#31738=DIRECTION ( 'NONE',  ( -1.725633230170962886E-31, -0.4685245517978552932, 0.8834504764629530493 ) ) ;
#31751=CARTESIAN_POINT ( 'NONE',  ( -0.04155248107635974020, 0.4416604393009535556, -0.1616214326753681041 ) ) ;
#31752=CARTESIAN_POINT ( 'NONE',  ( -0.04211812644076826789, 0.008544267401289764793, 0.4689465636496595868 ) ) ;
#31756=CIRCLE ( 'NONE', #14020, 0.01500000000000000638 ) ;
#31758=ORIENTED_EDGE ( 'NONE', *, *, #12355, .T. ) ;
#31766=VECTOR ( 'NONE', #1136, 39.37007874015748143 ) ;
#31770=EDGE_CURVE ( 'NONE', #29903, #1932, #39105, .T. ) ;
#31772=DIRECTION ( 'NONE',  ( -3.235562306570549665E-32, 0.6954292836767010932, 0.7185945389473191725 ) ) ;
#31773=CARTESIAN_POINT ( 'NONE',  ( 0.05634206451479712580, -0.2780979935378002366, -0.3651623763481146034 ) ) ;
#31785=CIRCLE ( 'NONE', #14039, 0.01500000000000001506 ) ;
#31793=CARTESIAN_POINT ( 'NONE',  ( -0.02238765564325451152, 0.3549921663302683106, -0.3695537732572939937 ) ) ;
#31796=CARTESIAN_POINT ( 'NONE',  ( -0.04760454375022137724, -0.4435184909896772165, -0.1893283029546962704 ) ) ;
#31799=DIRECTION ( 'NONE',  ( 0.000000000000000000, 0.8090169943749455639, -0.5877852522924756906 ) ) ;
#31808=CARTESIAN_POINT ( 'NONE',  ( 0.02231181081520633436, 0.07006449514257805100, 0.5077922075898764209 ) ) ;
#31829=AXIS2_PLACEMENT_3D ( 'NONE', #18420, #27694, #24624 ) ;
#31847=DIRECTION ( 'NONE',  ( 1.707404996040163180E-15, -0.1725921171157359935, -0.9849933812516245002 ) ) ;
#31855=DIRECTION ( 'NONE',  ( 2.532366176626896502E-12, -1.000000000000000000, -5.691349986800531115E-16 ) ) ;
#31863=CIRCLE ( 'NONE', #24009, 0.3698489655878011706 ) ;
#31872=EDGE_CURVE ( 'NONE', #3229, #28482, #13501, .T. ) ;
#31877=EDGE_CURVE ( 'NONE', #25200, #3242, #23379, .T. ) ;
#31891=ORIENTED_EDGE ( 'NONE', *, *, #39607, .F. ) ;
#31909=CARTESIAN_POINT ( 'NONE',  ( 0.03478489236950594449, -0.3590487419276154335, 0.3712145292149066078 ) ) ;
#31914=CARTESIAN_POINT ( 'NONE',  ( -0.05201782277453367159, 0.4527080286589615921, 0.1280848763234634091 ) ) ;
#31945=DIRECTION ( 'NONE',  ( 0.3468893892380796595, -0.7396492646830092887, -0.5767033179095778506 ) ) ;
#31952=DIRECTION ( 'NONE',  ( 1.000000000000000000, 2.280301054154495132E-31, -1.664003471950577689E-31 ) ) ;
#31963=CARTESIAN_POINT ( 'NONE',  ( -0.02953079040095700838, 0.000000000000000000, 0.000000000000000000 ) ) ;
#31970=VERTEX_POINT ( 'NONE', #16876 ) ;
#31980=ORIENTED_EDGE ( 'NONE', *, *, #12184, .T. ) ;
#31994=CARTESIAN_POINT ( 'NONE',  ( -0.05489899477340578343, 0.2921074789649996672, -0.3589041746640609931 ) ) ;
#31995=CARTESIAN_POINT ( 'NONE',  ( -0.04047076529491829000, -0.4536027527280144800, -0.2133348358548762813 ) ) ;
#32001=CARTESIAN_POINT ( 'NONE',  ( 0.05078310099560631730, 0.4632425114130949151, -0.09919524461158422957 ) ) ;
#32011=CARTESIAN_POINT ( 'NONE',  ( -0.05082294681499039540, -0.04864283519431539249, 0.4711332289091956782 ) ) ;
#32024=ORIENTED_EDGE ( 'NONE', *, *, #3352, .F. ) ;
#32039=DIRECTION ( 'NONE',  ( 0.000000000000000000, -0.3090169943749375148, 0.9510565162951567508 ) ) ;
#32043=FACE_OUTER_BOUND ( 'NONE', #8076, .T. ) ;
#32050=EDGE_CURVE ( 'NONE', #14981, #33895, #36782, .T. ) ;
#32056=DIRECTION ( 'NONE',  ( -1.000000000000000000, -2.280301054154495132E-31, 1.664003471950577689E-31 ) ) ;
#32065=CARTESIAN_POINT ( 'NONE',  ( 0.02953079040095673430, -0.2329676531120430660, 0.4763574306556350169 ) ) ;
#32070=DIRECTION ( 'NONE',  ( -2.563099466555624080E-12, -0.5877852522924748024, -0.8090169943749461190 ) ) ;
#32071=EDGE_LOOP ( 'NONE', ( #16537, #30469, #31014, #32127 ) ) ;
#32084=CARTESIAN_POINT ( 'NONE',  ( -0.03868264068766696234, -0.4624969084406944098, 0.1149348357506064511 ) ) ;
#32092=CARTESIAN_POINT ( 'NONE',  ( -0.04230188431063494625, 0.008729788072059678147, -0.4686063437799716791 ) ) ;
#32095=FACE_OUTER_BOUND ( 'NONE', #2547, .T. ) ;
#32096=DIRECTION ( 'NONE',  ( -0.9378410757839561462, -0.2807814858886641951, -0.2039996905746319089 ) ) ;
#32104=CARTESIAN_POINT ( 'NONE',  ( 0.04575185649130927845, -0.3363955107642125353, 0.3523382570435877326 ) ) ;
#32111=CARTESIAN_POINT ( 'NONE',  ( -0.03171861681797786409, 0.5171399723077546584, 0.08825220573715056305 ) ) ;
#32113=EDGE_CURVE ( 'NONE', #4242, #33794, #2642, .T. ) ;
#32127=ORIENTED_EDGE ( 'NONE', *, *, #36722, .T. ) ;
#32128=ADVANCED_FACE ( 'NONE', ( #30424 ), #21169, .T. ) ;
#32133=ORIENTED_EDGE ( 'NONE', *, *, #15583, .T. ) ;
#32184=CARTESIAN_POINT ( 'NONE',  ( -0.04229883635637934902, 0.2789693855191321403, -0.3765531589812268209 ) ) ;
#32193=CARTESIAN_POINT ( 'NONE',  ( 0.04575185649130717597, 0.4792489163483486525, -0.08731931755211801149 ) ) ;
#32196=CARTESIAN_POINT ( 'NONE',  ( 0.04229956186878594537, -0.2825373843407186225, 0.3739591931584704820 ) ) ;
#32205=ORIENTED_EDGE ( 'NONE', *, *, #1221, .F. ) ;
#32219=DIRECTION ( 'NONE',  ( 1.000000000000000000, 2.280301054154495132E-31, -1.664003471950577689E-31 ) ) ;
#32238=CARTESIAN_POINT ( 'NONE',  ( 0.04946426091936848013, 0.2513512500265263072, 0.4057590668656822497 ) ) ;
#32244=VECTOR ( 'NONE', #34610, 39.37007874015748143 ) ;
#32250=DIRECTION ( 'NONE',  ( 1.000000000000000000, 2.280301054154495132E-31, -1.664003471950577689E-31 ) ) ;
#32252=AXIS2_PLACEMENT_3D ( 'NONE', #23339, #7675, #20239 ) ;
#32260=EDGE_CURVE ( 'NONE', #27640, #35830, #40151, .T. ) ;
#32264=EDGE_CURVE ( 'NONE', #19390, #10166, #6635, .T. ) ;
#32265=EDGE_LOOP ( 'NONE', ( #19549, #11932, #460, #7570 ) ) ;
#32270=ADVANCED_FACE ( 'NONE', ( #3453 ), #28761, .T. ) ;
#32300=EDGE_CURVE ( 'NONE', #30159, #20992, #24408, .T. ) ;
#32310=ORIENTED_EDGE ( 'NONE', *, *, #24778, .F. ) ;
#32319=EDGE_CURVE ( 'NONE', #13520, #16165, #10032, .T. ) ;
#32320=EDGE_CURVE ( 'NONE', #13940, #11991, #4575, .T. ) ;
#32323=ADVANCED_FACE ( 'NONE', ( #19510 ), #36144, .T. ) ;
#32338=EDGE_CURVE ( 'NONE', #12540, #37319, #5946, .T. ) ;
#32341=CARTESIAN_POINT ( 'NONE',  ( 0.03158843595483527833, -0.4482533282648944462, -0.2030547983902471210 ) ) ;
#32348=CARTESIAN_POINT ( 'NONE',  ( -0.03868649100028190291, 0.4417196792138938788, -0.1788567627196049059 ) ) ;
#32354=ORIENTED_EDGE ( 'NONE', *, *, #39607, .T. ) ;
#32362=LINE ( 'NONE', #4188, #7488 ) ;
#32366=ORIENTED_EDGE ( 'NONE', *, *, #2407, .T. ) ;
#32373=CARTESIAN_POINT ( 'NONE',  ( 0.06980746140711582837, 0.000000000000000000, 0.000000000000000000 ) ) ;
#32381=CARTESIAN_POINT ( 'NONE',  ( -0.01548846960707455332, 0.2450655194479865739, -0.4674710490749279246 ) ) ;
#32383=CARTESIAN_POINT ( 'NONE',  ( -0.05489899477340617201, -0.4316043292239965523, -0.1669032320049002316 ) ) ;
#32387=B_SPLINE_CURVE_WITH_KNOTS ( 'NONE', 3,
 ( #38775, #35312, #785, #19873, #38589, #1190, #10606, #22970, #20094, #13293, #23180, #10826, #6701, #10411, #35491, #3637, #28735, #597 ),
 .UNSPECIFIED., .F., .F.,
 ( 4, 2, 2, 2, 2, 2, 2, 2, 4 ),
 ( -0.002633528389679661366, -0.001975271857855668677, -0.001317015326031676205, -0.0006587587942076789625, -5.022623836819367638E-07, 0.0006577542694403155227, 0.001316010801264312982, 0.001974267333088309574, 0.002632523864912307034 ),
 .UNSPECIFIED. ) ;
#32388=ADVANCED_FACE ( 'NONE', ( #14600 ), #14393, .F. ) ;
#32392=CARTESIAN_POINT ( 'NONE',  ( -0.01548846960707477016, 0.4638115001430995199, 0.2459753896937826034 ) ) ;
#32394=CARTESIAN_POINT ( 'NONE',  ( 0.02953079040095510019, 0.4684706630666146121, -0.2484463060367390341 ) ) ;
#32398=CARTESIAN_POINT ( 'NONE',  ( 0.02869942827333496829, -0.2420058122830158198, 0.4357544236535315640 ) ) ;
#32419=CARTESIAN_POINT ( 'NONE',  ( 0.01548846960707528191, -0.3772621329473441198, 0.3651003739302687290 ) ) ;
#32430=DIRECTION ( 'NONE',  ( -0.3468893892380665034, 0.9373665302208726846, -0.03180785525185936963 ) ) ;
#32432=VERTEX_POINT ( 'NONE', #37021 ) ;
#32434=CARTESIAN_POINT ( 'NONE',  ( 0.01548846960706616940, -0.5203207976468143814, 0.08861466064781831076 ) ) ;
#32443=CIRCLE ( 'NONE', #960, 0.01500000000000000291 ) ;
#32445=CARTESIAN_POINT ( 'NONE',  ( 0.01895884884825209393, -0.3622979475331352117, -0.3730907371368787917 ) ) ;
#32449=CARTESIAN_POINT ( 'NONE',  ( 0.03303737228521357733, 0.3731855291841458810, 0.3634704002369245623 ) ) ;
#32464=CARTESIAN_POINT ( 'NONE',  ( -0.01548846960707524721, 0.000000000000000000, 0.000000000000000000 ) ) ;
#32476=CARTESIAN_POINT ( 'NONE',  ( -0.04229956186878531393, -0.4429651807893734139, 0.1531492745855153881 ) ) ;
#32478=B_SPLINE_CURVE_WITH_KNOTS ( 'NONE', 3,
 ( #503, #2059, #20587, #13784, #33121, #14593, #26952, #4929, #36620, #17678, #20186, #1682, #29631, #39099, #39486, #26352, #38878, #33507 ),
 .UNSPECIFIED., .F., .F.,
 ( 4, 2, 2, 2, 2, 2, 2, 2, 4 ),
 ( 0.0003425652276237360736, 0.001007165397454251772, 0.001671765567284767525, 0.002336365737115283711, 0.003000965906945799247, 0.003665566076776314783, 0.004330166246606831186, 0.004994766416437346722, 0.005659366586267862258 ),
 .UNSPECIFIED. ) ;
#32483=CARTESIAN_POINT ( 'NONE',  ( -0.02881329448201180518, -0.4517642754607882338, 0.2100174381954052760 ) ) ;
#32504=CARTESIAN_POINT ( 'NONE',  ( 0.01548846960721252282, 0.3688619771570336159, -0.3775276577325234473 ) ) ;
#32518=VECTOR ( 'NONE', #34012, 39.37007874015748854 ) ;
#32551=CIRCLE ( 'NONE', #26003, 0.01499999999999999424 ) ;
#32572=ORIENTED_EDGE ( 'NONE', *, *, #24981, .T. ) ;
#32580=CARTESIAN_POINT ( 'NONE',  ( -0.04308449196698830447, 0.4845747790794809329, -0.09763455429601648750 ) ) ;
#32597=CARTESIAN_POINT ( 'NONE',  ( -0.05491348488830476854, 0.2511509903618529549, -0.3886212643843935943 ) ) ;
#32598=CARTESIAN_POINT ( 'NONE',  ( -0.05252049209742622876, -0.4432254733698156590, -0.1535896008539242019 ) ) ;
#32599=CARTESIAN_POINT ( 'NONE',  ( -0.01548846960707504251, -0.09319974324248665731, 0.5318964258758798191 ) ) ;
#32602=ADVANCED_FACE ( 'NONE', ( #9140 ), #19397, .T. ) ;
#32606=AXIS2_PLACEMENT_3D ( 'NONE', #27949, #27348, #8807 ) ;
#32612=CARTESIAN_POINT ( 'NONE',  ( -0.04760454375021574980, -0.2475296122118676723, -0.4138634427292607887 ) ) ;
#32647=ORIENTED_EDGE ( 'NONE', *, *, #25092, .T. ) ;
#32656=CARTESIAN_POINT ( 'NONE',  ( 0.04155248107635917121, -0.2623121065566118570, -0.3903559784317167658 ) ) ;
#32660=CARTESIAN_POINT ( 'NONE',  ( 0.02238826743733428673, 0.3549908576167664087, 0.3695531484129505051 ) ) ;
#32669=CARTESIAN_POINT ( 'NONE',  ( -0.04140212552917707511, -0.2627138686861280048, 0.3904233130033950561 ) ) ;
#32701=FACE_OUTER_BOUND ( 'NONE', #26212, .T. ) ;
#32710=DIRECTION ( 'NONE',  ( -1.000000000000000000, -2.280301054154495132E-31, 1.664003471950577689E-31 ) ) ;
#32726=CARTESIAN_POINT ( 'NONE',  ( 0.03478556507499377948, 0.4639967941987065969, 0.2267627654641998503 ) ) ;
#32742=CARTESIAN_POINT ( 'NONE',  ( -0.1399999999999997358, 0.000000000000000000, 0.000000000000000000 ) ) ;
#32745=CARTESIAN_POINT ( 'NONE',  ( 0.01548846960707497486, -0.2372406987223574237, 0.4850946823762633531 ) ) ;
#32748=SHAPE_REPRESENTATION_RELATIONSHIP ( 'NONE' , 'NONE' ,  #30390, #16697 ) ;
#32755=EDGE_CURVE ( 'NONE', #9503, #1137, #24572, .T. ) ;
#32767=ORIENTED_EDGE ( 'NONE', *, *, #25287, .F. ) ;
#32771=FACE_OUTER_BOUND ( 'NONE', #19237, .T. ) ;
#32774=CARTESIAN_POINT ( 'NONE',  ( -0.04085667396267504692, 0.4547700361314930273, -0.1255037944140887374 ) ) ;
#32790=CARTESIAN_POINT ( 'NONE',  ( 2.372745691485074899E-32, -7.971802777789931753E-17, -0.1749999999999999889 ) ) ;
#32796=ADVANCED_FACE ( 'NONE', ( #38916 ), #20015, .T. ) ;
#32802=CARTESIAN_POINT ( 'NONE',  ( -0.05634490452573009955, -0.2738187358595995380, -0.3682637492038659532 ) ) ;
#32808=EDGE_CURVE ( 'NONE', #17096, #26041, #2888, .T. ) ;
#32811=CARTESIAN_POINT ( 'NONE',  ( -0.01548846960721252282, 0.3688619771570396666, 0.3775276577325177296 ) ) ;
#32833=VERTEX_POINT ( 'NONE', #32745 ) ;
#32835=CARTESIAN_POINT ( 'NONE',  ( 0.05279755784604210633, -0.4315508301037762617, 0.1821553064136585132 ) ) ;
#32843=CIRCLE ( 'NONE', #32941, 0.01499999999999994740 ) ;
#32845=ADVANCED_FACE ( 'NONE', ( #26988 ), #1910, .T. ) ;
#32846=CARTESIAN_POINT ( 'NONE',  ( -0.01548846960707477016, 0.4770632572900446178, -0.2530032579707474083 ) ) ;
#32850=CARTESIAN_POINT ( 'NONE',  ( 0.05561375719525510353, 0.2871676730027915569, 0.3605331597494266793 ) ) ;
#32856=CARTESIAN_POINT ( 'NONE',  ( -0.1499999999999996336, 4.163336342344336410E-17, 0.1249999999999999584 ) ) ;
#32858=CARTESIAN_POINT ( 'NONE',  ( -0.05252359774140241688, -0.2683439431814180764, 0.3847367734645306125 ) ) ;
#32865=CARTESIAN_POINT ( 'NONE',  ( 0.01548846960707514486, -0.4638115001430951345, 0.2459753896937915962 ) ) ;
#32867=AXIS2_PLACEMENT_3D ( 'NONE', #35313, #7102, #21968 ) ;
#32873=FACE_OUTER_BOUND ( 'NONE', #39450, .T. ) ;
#32885=DIRECTION ( 'NONE',  ( 0.000000000000000000, 0.4393346272634469085, 0.8983234858820557944 ) ) ;
#32890=DIRECTION ( 'NONE',  ( -1.000000000000000000, -2.280301054154495132E-31, 1.664003471950577689E-31 ) ) ;
#32891=CARTESIAN_POINT ( 'NONE',  ( 0.1399999999999994582, -4.527947890665460015E-17, -0.2150000000000000244 ) ) ;
#32895=EDGE_CURVE ( 'NONE', #6931, #16637, #32443, .T. ) ;
#32907=AXIS2_PLACEMENT_3D ( 'NONE', #17215, #27086, #4452 ) ;
#32919=ORIENTED_EDGE ( 'NONE', *, *, #23932, .T. ) ;
#32923=CARTESIAN_POINT ( 'NONE',  ( -0.01895884884825181985, -0.4667865995382943223, -0.2292744456225760119 ) ) ;
#32932=ORIENTED_EDGE ( 'NONE', *, *, #12679, .F. ) ;
#32933=AXIS2_PLACEMENT_3D ( 'NONE', #28156, #35136, #34719 ) ;
#32941=AXIS2_PLACEMENT_3D ( 'NONE', #20990, #33321, #36201 ) ;
#32945=DIRECTION ( 'NONE',  ( 0.000000000000000000, 3.330669073875470114E-16, 1.000000000000000000 ) ) ;
#32952=CARTESIAN_POINT ( 'NONE',  ( -0.01548846960707524721, -0.4638115001430989648, 0.2459753896937853235 ) ) ;
#32958=EDGE_CURVE ( 'NONE', #4624, #23581, #16687, .T. ) ;
#32961=CIRCLE ( 'NONE', #17838, 0.5400000000000015898 ) ;
#32966=CIRCLE ( 'NONE', #17843, 0.5302738246768088359 ) ;
#32968=ORIENTED_EDGE ( 'NONE', *, *, #5019, .T. ) ;
#32988=ORIENTED_EDGE ( 'NONE', *, *, #8922, .F. ) ;
#32989=CARTESIAN_POINT ( 'NONE',  ( 0.05562144613422614903, -0.4316454521248588860, -0.1615915407302030427 ) ) ;
#32993=CARTESIAN_POINT ( 'NONE',  ( -0.03171893264487282704, -0.5171391213725057279, -0.08825218502846603197 ) ) ;
#33007=CARTESIAN_POINT ( 'NONE',  ( 0.000000000000000000, 0.000000000000000000, 0.000000000000000000 ) ) ;
#33009=VERTEX_POINT ( 'NONE', #10090 ) ;
#33011=CARTESIAN_POINT ( 'NONE',  ( 2.372745691485074352E-32, -3.685538980774211798E-17, -0.1749999999999999889 ) ) ;
#33018=CARTESIAN_POINT ( 'NONE',  ( -0.04230188431063483523, 0.2683773510969766352, 0.3842417364743013763 ) ) ;
#33022=DIRECTION ( 'NONE',  ( 2.532366176626898926E-12, -0.8090169943749432324, 0.5877852522924789103 ) ) ;
#33023=CARTESIAN_POINT ( 'NONE',  ( 0.02953079040095537774, -0.5250338024619286559, -0.07436286310882828099 ) ) ;
#33025=AXIS2_PLACEMENT_3D ( 'NONE', #37026, #30459, #15438 ) ;
#33036=ADVANCED_FACE ( 'NONE', ( #37876 ), #34770, .T. ) ;
#33044=ORIENTED_EDGE ( 'NONE', *, *, #35326, .F. ) ;
#33046=CARTESIAN_POINT ( 'NONE',  ( 0.02242828275839356053, -0.5043161982043002922, 0.09034400517546492537 ) ) ;
#33051=CARTESIAN_POINT ( 'NONE',  ( 0.01548846960707524721, 0.4770632572900446178, -0.2530032579707474083 ) ) ;
#33055=FACE_OUTER_BOUND ( 'NONE', #1693, .T. ) ;
#33056=CARTESIAN_POINT ( 'NONE',  ( 0.01548846960712797240, -0.3688619771571953754, -0.3775276577326278082 ) ) ;
#33060=AXIS2_PLACEMENT_3D ( 'NONE', #3262, #31652, #822 ) ;
#33066=ADVANCED_FACE ( 'NONE', ( #3298 ), #3528, .T. ) ;
#33069=CARTESIAN_POINT ( 'NONE',  ( -0.02881302694830073854, -0.3393464602395944163, 0.3647504210684007764 ) ) ;
#33077=DIRECTION ( 'NONE',  ( 1.000000000000000000, 2.280301054154495132E-31, -1.664003471950577689E-31 ) ) ;
#33081=ORIENTED_EDGE ( 'NONE', *, *, #6182, .F. ) ;
#33084=ORIENTED_EDGE ( 'NONE', *, *, #34396, .F. ) ;
#33085=FACE_OUTER_BOUND ( 'NONE', #29298, .T. ) ;
#33086=AXIS2_PLACEMENT_3D ( 'NONE', #33007, #33224, #38766 ) ;
#33102=LINE ( 'NONE', #17482, #28443 ) ;
#33103=FACE_OUTER_BOUND ( 'NONE', #30092, .T. ) ;
#33110=CARTESIAN_POINT ( 'NONE',  ( 0.03158843595483465383, -0.4819971762524432601, 0.09920191295802863185 ) ) ;
#33121=CARTESIAN_POINT ( 'NONE',  ( 0.03158843595483495220, 0.05459869295506127734, -0.4890616322892840651 ) ) ;
#33122=VECTOR ( 'NONE', #7290, 39.37007874015748143 ) ;
#33128=CARTESIAN_POINT ( 'NONE',  ( 0.1499999999999996059, -0.2450655194479835486, -0.4674710490749285907 ) ) ;
#33133=LINE ( 'NONE', #17693, #5409 ) ;
#33140=EDGE_CURVE ( 'NONE', #4078, #5225, #31785, .T. ) ;
#33151=AXIS2_PLACEMENT_3D ( 'NONE', #16260, #10675, #25516 ) ;
#33161=DIRECTION ( 'NONE',  ( 0.000000000000000000, -0.8834504764630435325, 0.4685245517976845409 ) ) ;
#33166=LENGTH_MEASURE_WITH_UNIT ( LENGTH_MEASURE( 0.02539999999999999897 ), #22917 );
#33176=CARTESIAN_POINT ( 'NONE',  ( 0.04285427992853951124, 0.07198917448059898028, -0.4895546022328390312 ) ) ;
#33195=DIRECTION ( 'NONE',  ( 1.000000000000000000, 0.000000000000000000, 0.000000000000000000 ) ) ;
#33207=DIRECTION ( 'NONE',  ( 0.000000000000000000, -0.9901182710308955581, 0.1402348365092997984 ) ) ;
#33210=CARTESIAN_POINT ( 'NONE',  ( 0.03309060444528783701, -0.4608881774262347242, 0.2425132784556429388 ) ) ;
#33212=CARTESIAN_POINT ( 'NONE',  ( -0.03877220711930347286, -0.4622141677842752649, -0.1152577684344557041 ) ) ;
#33215=AXIS2_PLACEMENT_3D ( 'NONE', #26942, #39680, #33714 ) ;
#33224=DIRECTION ( 'NONE',  ( -1.000000000000000000, -2.280301054154495132E-31, 1.664003471950577689E-31 ) ) ;
#33232=CARTESIAN_POINT ( 'NONE',  ( -0.03868264068766689295, 0.2522289290439786447, 0.4043438810462527955 ) ) ;
#33233=CARTESIAN_POINT ( 'NONE',  ( 0.05561310505366609536, -0.02041094169099977318, 0.4604718309744721405 ) ) ;
#33235=CARTESIAN_POINT ( 'NONE',  ( 0.03303737228521689412, -0.5155559760688823712, -0.07470078032051498396 ) ) ;
#33243=DIRECTION ( 'NONE',  ( 0.9378410757839558132, -0.2807814858886552578, 0.2039996905746457034 ) ) ;
#33254=CARTESIAN_POINT ( 'NONE',  ( 0.01899496522503697424, -0.4667215747137393733, 0.2292237458735815747 ) ) ;
#33261=CARTESIAN_POINT ( 'NONE',  ( 0.000000000000000000, 0.000000000000000000, 0.000000000000000000 ) ) ;
#33262=CARTESIAN_POINT ( 'NONE',  ( 0.02869942827333502033, -0.3396431753871653192, -0.3648167270360652692 ) ) ;
#33265=CARTESIAN_POINT ( 'NONE',  ( 0.03171861681796823984, 0.2437378752574358431, 0.4645579091361449753 ) ) ;
#33267=CARTESIAN_POINT ( 'NONE',  ( 0.01548846960721252282, 0.3688619771570336159, -0.3775276577325234473 ) ) ;
#33269=CARTESIAN_POINT ( 'NONE',  ( -0.03654364704248880963, 0.4542255574219845049, -0.2354487068768210956 ) ) ;
#33280=CARTESIAN_POINT ( 'NONE',  ( 0.02953079040095673430, -0.5250338024619269905, -0.07436286310882420092 ) ) ;
#33282=CARTESIAN_POINT ( 'NONE',  ( -0.05561176441985811458, 0.4316390549698259083, 0.1616802657107478947 ) ) ;
#33309=CARTESIAN_POINT ( 'NONE',  ( 0.04293317454820629736, 0.4432234940308290017, 0.2195257349118415469 ) ) ;
#33321=DIRECTION ( 'NONE',  ( -0.3468893892380672250, 0.2594111197898656962, -0.9013177145509837507 ) ) ;
#33332=VERTEX_POINT ( 'NONE', #7799 ) ;
#33334=CARTESIAN_POINT ( 'NONE',  ( -0.04155248107635943489, -0.4523094957185400666, -0.1288470070525131739 ) ) ;
#33349=EDGE_CURVE ( 'NONE', #32833, #2287, #13429, .T. ) ;
#33352=EDGE_CURVE ( 'NONE', #4242, #15491, #29826, .T. ) ;
#33354=DIRECTION ( 'NONE',  ( 0.000000000000000000, -3.330669073875470114E-16, -1.000000000000000000 ) ) ;
#33367=ADVANCED_FACE ( 'NONE', ( #33103 ), #4507, .T. ) ;
#33371=CARTESIAN_POINT ( 'NONE',  ( 0.03170953572518742797, 0.05433194795445773356, -0.4888234031312626016 ) ) ;
#33373=EDGE_CURVE ( 'NONE', #35103, #11876, #35740, .T. ) ;
#33387=DIRECTION ( 'NONE',  ( -1.000000000000000000, -2.341930812374887555E-31, 1.664003471950578127E-31 ) ) ;
#33390=DIRECTION ( 'NONE',  ( 1.000000000000000000, 0.000000000000000000, 0.000000000000000000 ) ) ;
#33402=DIRECTION ( 'NONE',  ( 1.000000000000000000, 2.341930812374887555E-31, -1.664003471950578127E-31 ) ) ;
#33407=CARTESIAN_POINT ( 'NONE',  ( 0.02953079040095728247, 0.000000000000000000, 0.000000000000000000 ) ) ;
#33416=ORIENTED_EDGE ( 'NONE', *, *, #15503, .F. ) ;
#33418=CARTESIAN_POINT ( 'NONE',  ( 1.694818351060767277E-32, -2.632527843410151064E-17, -0.1249999999999999584 ) ) ;
#33419=CARTESIAN_POINT ( 'NONE',  ( -0.05634304521267782806, -2.731847993664263218E-15, -0.4588823192046729837 ) ) ;
#33420=CARTESIAN_POINT ( 'NONE',  ( -0.05078493045284371288, -0.3164574661091665853, -0.3525385122722523024 ) ) ;
#33428=CARTESIAN_POINT ( 'NONE',  ( 0.05634206451479407962, 0.01034894336415898355, 0.4588844674656195610 ) ) ;
#33429=CARTESIAN_POINT ( 'NONE',  ( 0.04285427992854141249, -0.4433482162102910240, -0.2197464652568942856 ) ) ;
#33430=DIRECTION ( 'NONE',  ( 1.000000000000000000, 0.000000000000000000, 0.000000000000000000 ) ) ;
#33438=EDGE_LOOP ( 'NONE', ( #18108, #38230, #14657, #24246, #14595, #1534, #20382, #300, #2646, #37248, #24605, #30012, #3788, #39794 ) ) ;
#33486=VERTEX_POINT ( 'NONE', #30433 ) ;
#33493=CARTESIAN_POINT ( 'NONE',  ( 0.01548846960721238578, -0.2450655194478977839, -0.4674710490746283864 ) ) ;
#33496=DIRECTION ( 'NONE',  ( -0.000000000000000000, 0.3090169943749569437, 0.9510565162951504226 ) ) ;
#33501=CARTESIAN_POINT ( 'NONE',  ( 0.01895884884825056391, -0.4667865995382994293, 0.2292744456225715155 ) ) ;
#33507=CARTESIAN_POINT ( 'NONE',  ( 0.01548846960712797240, -0.07651041855115535417, -0.5222379212567069828 ) ) ;
#33514=ORIENTED_EDGE ( 'NONE', *, *, #17594, .F. ) ;
#33521=ORIENTED_EDGE ( 'NONE', *, *, #21065, .T. ) ;
#33522=CYLINDRICAL_SURFACE ( 'NONE', #13969, 0.2149999999999999967 ) ;
#33525=CARTESIAN_POINT ( 'NONE',  ( -0.01895494625228063071, -0.5124113341948476341, -0.08888305413160664525 ) ) ;
#33530=ORIENTED_EDGE ( 'NONE', *, *, #15583, .F. ) ;
#33540=CIRCLE ( 'NONE', #20428, 0.2149999999999999967 ) ;
#33547=DIRECTION ( 'NONE',  ( -1.000000000000000000, -2.341930812374887555E-31, 1.664003471950578127E-31 ) ) ;
#33556=CARTESIAN_POINT ( 'NONE',  ( 0.05201782277453716880, 0.01807851807932257804, -0.4701313241416041344 ) ) ;
#33560=ORIENTED_EDGE ( 'NONE', *, *, #32319, .T. ) ;
#33569=AXIS2_PLACEMENT_3D ( 'NONE', #431, #6525, #25675 ) ;
#33576=DIRECTION ( 'NONE',  ( 0.000000000000000000, -0.9510565162951529761, 0.3090169943749491166 ) ) ;
#33582=CARTESIAN_POINT ( 'NONE',  ( -0.03171102739523483371, 0.4481073524712024247, -0.2027236177532017181 ) ) ;
#33583=ORIENTED_EDGE ( 'NONE', *, *, #11931, .F. ) ;
#33588=DIRECTION ( 'NONE',  ( 1.000000000000000000, 0.000000000000000000, 0.000000000000000000 ) ) ;
#33590=ADVANCED_FACE ( 'NONE', ( #31645 ), #9425, .F. ) ;
#33592=ORIENTED_EDGE ( 'NONE', *, *, #1739, .F. ) ;
#33594=CARTESIAN_POINT ( 'NONE',  ( 0.01548846960707524721, 0.5198120922912204955, -0.07362328916738319906 ) ) ;
#33605=AXIS2_PLACEMENT_3D ( 'NONE', #14422, #33547, #5357 ) ;
#33609=CARTESIAN_POINT ( 'NONE',  ( -0.01548846960712810944, 0.3688619771571925998, -0.3775276577326300287 ) ) ;
#33617=CARTESIAN_POINT ( 'NONE',  ( -0.05543910610525118465, 0.02035452233660139595, -0.4608669713610835106 ) ) ;
#33619=ORIENTED_EDGE ( 'NONE', *, *, #33373, .F. ) ;
#33621=CARTESIAN_POINT ( 'NONE',  ( 0.03647060353175621272, -0.08366884794402436321, 0.5049308971818872172 ) ) ;
#33622=CARTESIAN_POINT ( 'NONE',  ( 0.05076679145661966430, -0.4632958555242867593, -0.09915135732236152188 ) ) ;
#33627=CARTESIAN_POINT ( 'NONE',  ( 0.04760454375021537510, 0.4700983808485068027, 0.1075238135162369518 ) ) ;
#33638=CARTESIAN_POINT ( 'NONE',  ( -0.04293317454820552020, -0.4432234940308336646, 0.2195257349118416856 ) ) ;
#33643=AXIS2_PLACEMENT_3D ( 'NONE', #12431, #5837, #15323 ) ;
#33650=FACE_OUTER_BOUND ( 'NONE', #22568, .T. ) ;
#33658=CIRCLE ( 'NONE', #3457, 0.01500000000000001853 ) ;
#33669=AXIS2_PLACEMENT_3D ( 'NONE', #17053, #7360, #4896 ) ;
#33677=AXIS2_PLACEMENT_3D ( 'NONE', #6286, #18856, #14745 ) ;
#33702=AXIS2_PLACEMENT_3D ( 'NONE', #2866, #8829, #21409 ) ;
#33714=DIRECTION ( 'NONE',  ( 0.000000000000000000, 3.330669073875469621E-16, 1.000000000000000000 ) ) ;
#33736=AXIS2_PLACEMENT_3D ( 'NONE', #24182, #20688, #2162 ) ;
#33770=CARTESIAN_POINT ( 'NONE',  ( 0.03672447062657864525, -0.2485879206383752038, 0.4115698867982532372 ) ) ;
#33771=ADVANCED_FACE ( 'NONE', ( #37710 ), #33777, .T. ) ;
#33777=CONICAL_SURFACE ( 'NONE', #16724, 0.3698489655878005045, 1.211529128687673262 ) ;
#33789=CARTESIAN_POINT ( 'NONE',  ( -0.01548846960707490547, 0.5198120922912040642, 0.07362328916749247276 ) ) ;
#33791=VECTOR ( 'NONE', #22866, 39.37007874015748143 ) ;
#33793=EDGE_LOOP ( 'NONE', ( #24380, #31473 ) ) ;
#33794=VERTEX_POINT ( 'NONE', #22303 ) ;
#33797=AXIS2_PLACEMENT_3D ( 'NONE', #27936, #24857, #34293 ) ;
#33809=CARTESIAN_POINT ( 'NONE',  ( -0.01548846960721204577, 0.5203207976464816475, 0.08861466064783131424 ) ) ;
#33815=EDGE_CURVE ( 'NONE', #35103, #20340, #39700, .T. ) ;
#33823=EDGE_CURVE ( 'NONE', #39055, #5283, #10710, .T. ) ;
#33837=CARTESIAN_POINT ( 'NONE',  ( -0.04575334816098020063, -0.3363904506959644602, -0.3523376320073989820 ) ) ;
#33839=EDGE_LOOP ( 'NONE', ( #10923, #5321, #2688, #22245 ) ) ;
#33841=CARTESIAN_POINT ( 'NONE',  ( -0.01899468245561106855, -0.3622301702732843576, 0.3730449234618263277 ) ) ;
#33843=ORIENTED_EDGE ( 'NONE', *, *, #35309, .T. ) ;
#33844=CARTESIAN_POINT ( 'NONE',  ( -0.04308745346420374267, -0.05688354191225564876, -0.4910214150057568006 ) ) ;
#33848=CARTESIAN_POINT ( 'NONE',  ( -0.02953079040095700838, 0.000000000000000000, 0.000000000000000000 ) ) ;
#33849=CARTESIAN_POINT ( 'NONE',  ( 0.04575185649130613513, -0.06505045373102469330, 0.4827759578813183849 ) ) ;
#33850=CARTESIAN_POINT ( 'NONE',  ( 0.04762035657657653215, -0.4434998562185943349, -0.1892652133704821049 ) ) ;
#33863=DIRECTION ( 'NONE',  ( -0.3468893892380661148, 0.9373665302208729067, 0.03180785525185500506 ) ) ;
#33875=CARTESIAN_POINT ( 'NONE',  ( -0.03868649100028168086, 0.4624880946332503573, 0.1149381524902354512 ) ) ;
#33876=B_SPLINE_CURVE_WITH_KNOTS ( 'NONE', 3,
 ( #14946, #27498, #2202, #15561, #18234, #40024, #33875, #5864, #8971, #9162, #5679, #21545, #2802, #15349, #18638, #27907, #40447, #12271 ),
 .UNSPECIFIED., .F., .F.,
 ( 4, 2, 2, 2, 2, 2, 2, 2, 4 ),
 ( 0.0003425652276237348809, 0.001007165397454244833, 0.001671765567284754731, 0.002336365737115264629, 0.003000965906945774527, 0.003665566076776284425, 0.004330166246606793889, 0.004994766416437303354, 0.005659366586267813685 ),
 .UNSPECIFIED. ) ;
#33883=CARTESIAN_POINT ( 'NONE',  ( -0.04139678531769643011, 0.2626830136224079237, 0.3904580303439411648 ) ) ;
#33891=CARTESIAN_POINT ( 'NONE',  ( 0.03868649100028150739, 0.3066017772948840814, -0.3648306000529298321 ) ) ;
#33895=VERTEX_POINT ( 'NONE', #1316 ) ;
#33896=CARTESIAN_POINT ( 'NONE',  ( 0.01548846960707524721, 0.4638115001430989648, -0.2459753896937820483 ) ) ;
#33907=CARTESIAN_POINT ( 'NONE',  ( 0.04157078424165694397, 0.2900150886686586604, -0.3701869471361532438 ) ) ;
#33909=CARTESIAN_POINT ( 'NONE',  ( 0.01548846960703782229, -0.4638115001431039053, -0.2459753896937787732 ) ) ;
#33921=DIRECTION ( 'NONE',  ( 1.787262988391350055E-31, 0.8983234858819699742, -0.4393346272636222682 ) ) ;
#33948=VERTEX_POINT ( 'NONE', #39739 ) ;
#33956=ORIENTED_EDGE ( 'NONE', *, *, #4610, .T. ) ;
#33958=DIRECTION ( 'NONE',  ( 0.000000000000000000, 0.5877852522924936762, -0.8090169943749323522 ) ) ;
#33966=ORIENTED_EDGE ( 'NONE', *, *, #15523, .F. ) ;
#33969=CARTESIAN_POINT ( 'NONE',  ( -0.05279185365593582618, -0.4562178057547947585, 0.1062796545748983384 ) ) ;
#33977=DIRECTION ( 'NONE',  ( 2.280301054154496008E-31, -1.000000000000000000, 3.330669073875470114E-16 ) ) ;
#33985=CARTESIAN_POINT ( 'NONE',  ( -0.01548846960712824648, 0.07651041855115098267, -0.5222379212567075379 ) ) ;
#34000=CARTESIAN_POINT ( 'NONE',  ( -0.01548846960707531660, -0.5198120922912100594, 0.07362328916748400731 ) ) ;
#34001=ORIENTED_EDGE ( 'NONE', *, *, #13883, .T. ) ;
#34008=CARTESIAN_POINT ( 'NONE',  ( -0.03309060444528717781, -0.3730661130945393533, 0.3633899800202449182 ) ) ;
#34012=DIRECTION ( 'NONE',  ( 0.3515883117872520836, -3.118021572908016454E-16, -0.9361547195921142706 ) ) ;
#34015=DIRECTION ( 'NONE',  ( -1.000000000000000000, -2.341930812374887555E-31, 1.664003471950578127E-31 ) ) ;
#34024=CARTESIAN_POINT ( 'NONE',  ( -0.02953079040095578714, -0.09152108205201867075, 0.5223162075576457397 ) ) ;
#34031=CARTESIAN_POINT ( 'NONE',  ( -0.03474824846560305158, 0.07233741238827121056, -0.5114535313566268560 ) ) ;
#34033=ORIENTED_EDGE ( 'NONE', *, *, #17578, .F. ) ;
#34035=ADVANCED_FACE ( 'NONE', ( #11154 ), #17537, .T. ) ;
#34038=CARTESIAN_POINT ( 'NONE',  ( 0.01548846960706656839, -0.07651041855119576629, 0.5222379212568392104 ) ) ;
#34039=CARTESIAN_POINT ( 'NONE',  ( 0.03170953572518869085, -0.4481091876101387927, -0.2027274919608517967 ) ) ;
#34043=FACE_OUTER_BOUND ( 'NONE', #4013, .T. ) ;
#34046=CARTESIAN_POINT ( 'NONE',  ( -0.04582889109739218120, -0.3361233334071005996, -0.3523147457849535868 ) ) ;
#34069=CARTESIAN_POINT ( 'NONE',  ( -0.03474824846560758962, 0.2421026470131133479, 0.4562934628913907220 ) ) ;
#34075=LINE ( 'NONE', #40242, #15324 ) ;
#34096=EDGE_CURVE ( 'NONE', #15099, #8761, #23322, .T. ) ;
#34097=DIRECTION ( 'NONE',  ( -2.526820087036053001E-31, -0.1402348365095093807, 0.9901182710308659152 ) ) ;
#34109=CYLINDRICAL_SURFACE ( 'NONE', #12772, 0.1749999999999999889 ) ;
#34143=CARTESIAN_POINT ( 'NONE',  ( 0.04230188431063459237, 0.4429734639576318189, -0.1531098457317254524 ) ) ;
#34150=ORIENTED_EDGE ( 'NONE', *, *, #11803, .T. ) ;
#34154=CARTESIAN_POINT ( 'NONE',  ( -0.02953079040095503774, -0.5250338024619316535, 0.07436286310882278539 ) ) ;
#34156=DIRECTION ( 'NONE',  ( 1.000000000000000000, 0.000000000000000000, 0.000000000000000000 ) ) ;
#34160=ADVANCED_FACE ( 'NONE', ( #24735 ), #4318, .T. ) ;
#34162=CARTESIAN_POINT ( 'NONE',  ( 0.8248651029816849167, 2.049759731064160790E-16, 0.6154198107346400271 ) ) ;
#34163=DIRECTION ( 'NONE',  ( -1.509929076399588311E-31, -0.9849933812516261655, -0.1725921171157266121 ) ) ;
#34177=DIRECTION ( 'NONE',  ( 0.000000000000000000, 3.341771304121709196E-14, -1.000000000000000000 ) ) ;
#34178=ORIENTED_EDGE ( 'NONE', *, *, #9894, .T. ) ;
#34191=SPHERICAL_SURFACE ( 'NONE', #37073, 0.01499999999999999944 ) ;
#34193=VECTOR ( 'NONE', #7298, 39.37007874015748143 ) ;
#34220=CARTESIAN_POINT ( 'NONE',  ( 2.915087563824520997E-32, -9.793929126999060983E-17, -0.2149999999999999967 ) ) ;
#34228=FACE_OUTER_BOUND ( 'NONE', #30055, .T. ) ;
#34229=ORIENTED_EDGE ( 'NONE', *, *, #29180, .F. ) ;
#34230=CARTESIAN_POINT ( 'NONE',  ( -0.01899468245561950625, 0.07378005917298446903, -0.5147132347679479469 ) ) ;
#34237=CARTESIAN_POINT ( 'NONE',  ( 0.04157143636675252052, -0.4522154923419796080, -0.1290233296939804764 ) ) ;
#34257=CIRCLE ( 'NONE', #4668, 0.7750185148639454624 ) ;
#34267=CARTESIAN_POINT ( 'NONE',  ( -0.04085667396267504692, 0.2598928711944307746, 0.3937292009461436648 ) ) ;
#34273=EDGE_CURVE ( 'NONE', #24540, #3369, #10818, .T. ) ;
#34274=CARTESIAN_POINT ( 'NONE',  ( 0.01548846960712814240, 0.2450655194479464116, -0.4674710490748144043 ) ) ;
#34286=AXIS2_PLACEMENT_3D ( 'NONE', #10092, #22668, #16464 ) ;
#34287=EDGE_CURVE ( 'NONE', #13090, #5913, #27818, .T. ) ;
#34291=CARTESIAN_POINT ( 'NONE',  ( 0.05279755784604157898, 0.2420637527537952693, -0.4010259520538080324 ) ) ;
#34293=DIRECTION ( 'NONE',  ( 0.000000000000000000, -3.330669073875470114E-16, -1.000000000000000000 ) ) ;
#34296=ORIENTED_EDGE ( 'NONE', *, *, #38119, .F. ) ;
#34298=FACE_OUTER_BOUND ( 'NONE', #29605, .T. ) ;
#34317=CIRCLE ( 'NONE', #16585, 0.5400000000000012568 ) ;
#34325=EDGE_CURVE ( 'NONE', #11991, #17796, #15336, .T. ) ;
#34335=ORIENTED_EDGE ( 'NONE', *, *, #38819, .F. ) ;
#34336=ORIENTED_EDGE ( 'NONE', *, *, #16281, .T. ) ;
#34341=CARTESIAN_POINT ( 'NONE',  ( -0.05561176441985789948, -0.4316390549698244650, -0.1616802657107529184 ) ) ;
#34347=CARTESIAN_POINT ( 'NONE',  ( 0.01895884884825246863, 0.4667865995382938227, -0.2292744456225718208 ) ) ;
#34350=AXIS2_PLACEMENT_3D ( 'NONE', #6691, #980, #19471 ) ;
#34364=CARTESIAN_POINT ( 'NONE',  ( 0.01548846960707528191, 0.3772621329472709006, 0.3651003739303413931 ) ) ;
#34367=CARTESIAN_POINT ( 'NONE',  ( 0.01548846960707582834, 0.4770632572900484480, 0.2530032579707400253 ) ) ;
#34375=CARTESIAN_POINT ( 'NONE',  ( 0.04760578872587302446, -0.2475315945985540611, 0.4138583970464106421 ) ) ;
#34382=EDGE_CURVE ( 'NONE', #20992, #17702, #16087, .T. ) ;
#34395=ORIENTED_EDGE ( 'NONE', *, *, #33823, .T. ) ;
#34396=EDGE_CURVE ( 'NONE', #36370, #16052, #37652, .T. ) ;
#34402=CARTESIAN_POINT ( 'NONE',  ( 0.04582713223189471829, 0.4389429380065681952, -0.2108029774974885806 ) ) ;
#34403=DIRECTION ( 'NONE',  ( 0.000000000000000000, -0.9510565162951458706, 0.3090169943749713766 ) ) ;
#34417=AXIS2_PLACEMENT_3D ( 'NONE', #2474, #15010, #11916 ) ;
#34420=DIRECTION ( 'NONE',  ( 0.000000000000000000, 2.964295475749157234E-14, 1.000000000000000000 ) ) ;
#34430=CARTESIAN_POINT ( 'NONE',  ( -0.04139678531769536846, -0.01699044972118052277, 0.4702883835734110729 ) ) ;
#34436=DIRECTION ( 'NONE',  ( -2.686534417925915961E-31, 0.5877852522924640333, -0.8090169943749540016 ) ) ;
#34439=CARTESIAN_POINT ( 'NONE',  ( -0.04211812644076821238, -0.008544267401287195668, -0.4689465636496595313 ) ) ;
#34452=CARTESIAN_POINT ( 'NONE',  ( -0.01548846960707517956, -0.2306506793134033284, -0.4716198300880336536 ) ) ;
#34457=CARTESIAN_POINT ( 'NONE',  ( 0.05283094505689992643, 0.03968992937477589661, 0.4666439588235274938 ) ) ;
#34459=CARTESIAN_POINT ( 'NONE',  ( -0.02953079040095707777, -0.5250338024619264354, 0.07436286310882474215 ) ) ;
#34469=CARTESIAN_POINT ( 'NONE',  ( -0.03303708955568269295, 0.3731861634337363953, -0.3634708273687332070 ) ) ;
#34470=AXIS2_PLACEMENT_3D ( 'NONE', #22363, #10403, #28520 ) ;
#34472=FACE_OUTER_BOUND ( 'NONE', #33839, .T. ) ;
#34479=CARTESIAN_POINT ( 'NONE',  ( -0.04285561529641203349, 0.3459893009865078750, 0.3537429040513690448 ) ) ;
#34491=CARTESIAN_POINT ( 'NONE',  ( 0.02953079040095728247, 0.000000000000000000, 0.000000000000000000 ) ) ;
#34500=CARTESIAN_POINT ( 'NONE',  ( 0.03171861681798987531, 0.3665016810530090652, -0.3753647833258712541 ) ) ;
#34509=VERTEX_POINT ( 'NONE', #39031 ) ;
#34511=DIRECTION ( 'NONE',  ( 1.664003471950577032E-31, 3.330669073875470114E-16, 1.000000000000000000 ) ) ;
#34528=CARTESIAN_POINT ( 'NONE',  ( 0.000000000000000000, 0.000000000000000000, 0.000000000000000000 ) ) ;
#34548=CARTESIAN_POINT ( 'NONE',  ( 0.02953079040095673430, -0.2329676531120485339, -0.4763574306556319637 ) ) ;
#34551=CARTESIAN_POINT ( 'NONE',  ( -0.04582713223189510687, -0.4389429380065676400, -0.2108029774974920778 ) ) ;
#34560=ADVANCED_FACE ( 'NONE', ( #39242 ), #1231, .T. ) ;
#34561=ORIENTED_EDGE ( 'NONE', *, *, #19006, .T. ) ;
#34568=ADVANCED_FACE ( 'NONE', ( #27917 ), #4820, .T. ) ;
#34577=CARTESIAN_POINT ( 'NONE',  ( -0.04285534776242611033, -0.4878382857517556404, 0.08280911155782857969 ) ) ;
#34588=CIRCLE ( 'NONE', #5683, 0.1749999999999999889 ) ;
#34594=CARTESIAN_POINT ( 'NONE',  ( -0.04229974373173753938, 0.4430055847546672809, 0.1530238331097821258 ) ) ;
#34610=DIRECTION ( 'NONE',  ( -1.000000000000000000, -2.341930812374887555E-31, 1.664003471950578127E-31 ) ) ;
#34621=CARTESIAN_POINT ( 'NONE',  ( -0.05083665881509043943, -0.2375940621857665636, 0.4096919151850478835 ) ) ;
#34634=DIRECTION ( 'NONE',  ( -1.000000000000000000, -2.280301054154495132E-31, 1.664003471950577689E-31 ) ) ;
#34640=CARTESIAN_POINT ( 'NONE',  ( -0.04947837552028416103, 0.03507397079375183108, 0.4759739487165450256 ) ) ;
#34643=B_SPLINE_CURVE_WITH_KNOTS ( 'NONE', 3,
 ( #39897, #2471, #20581, #2661, #33110, #14380, #15005, #2052, #17489, #39687, #20984, #18095, #18299, #4923, #11309, #40082, #33501, #11911 ),
 .UNSPECIFIED., .F., .F.,
 ( 4, 2, 2, 2, 2, 2, 2, 2, 4 ),
 ( 0.0003425652276237173711, 0.001007165397454238978, 0.001671765567284760586, 0.002336365737115281976, 0.003000965906945803584, 0.003665566076776325191, 0.004330166246606846799, 0.004994766416437368406, 0.005659366586267890013 ),
 .UNSPECIFIED. ) ;
#34651=DIRECTION ( 'NONE',  ( 1.000000000000000000, 1.544378112879830442E-12, 7.552944938426298648E-13 ) ) ;
#34654=CARTESIAN_POINT ( 'NONE',  ( -0.01548846960707490547, 0.5198120922912035091, 0.07362328916749301400 ) ) ;
#34663=CARTESIAN_POINT ( 'NONE',  ( 0.03650577977170427202, 0.08362514765351862500, 0.5048437183011799112 ) ) ;
#34666=DIRECTION ( 'NONE',  ( -1.000000000000000000, -2.341930812374887555E-31, 1.664003471950578127E-31 ) ) ;
#34671=CARTESIAN_POINT ( 'NONE',  ( -0.03650581953630599452, 0.2290855126858387936, 0.4575806651622378318 ) ) ;
#34673=CARTESIAN_POINT ( 'NONE',  ( -0.02238765564325446641, -0.4611651364438438261, -0.2234192167502431769 ) ) ;
#34679=CARTESIAN_POINT ( 'NONE',  ( -0.05187277790672333022, 0.2910352029727566459, 0.3700865090056973394 ) ) ;
#34696=CARTESIAN_POINT ( 'NONE',  ( 0.04157143636675521281, 0.2624507507128696071, -0.3902120892151714759 ) ) ;
#34703=ORIENTED_EDGE ( 'NONE', *, *, #30794, .T. ) ;
#34718=FACE_OUTER_BOUND ( 'NONE', #13315, .T. ) ;
#34719=DIRECTION ( 'NONE',  ( 0.9378410757839547029, 0.2807814858886594211, 0.2039996905746454536 ) ) ;
#34723=B_SPLINE_CURVE_WITH_KNOTS ( 'NONE', 3,
 ( #13165, #35585, #25732, #16881, #29422, #1269, #13773, #26336, #23265, #29827, #8410, #27151, #39892, #39472, #33309, #39282, #24270, #24468 ),
 .UNSPECIFIED., .F., .F.,
 ( 4, 2, 2, 2, 2, 2, 2, 2, 4 ),
 ( 0.000000000000000000, 0.0007746617437634276387, 0.001549323487526855277, 0.002323985231290282699, 0.003098646975053710555, 0.003873308718817138410, 0.004647970462580565398, 0.005422632206343993254, 0.006197293950107421109 ),
 .UNSPECIFIED. ) ;
#34735=CARTESIAN_POINT ( 'NONE',  ( -0.1499999999999996336, 0.000000000000000000, 0.000000000000000000 ) ) ;
#34745=CARTESIAN_POINT ( 'NONE',  ( -0.05634307799789434884, -0.4332460723641310962, -0.1515798417490749894 ) ) ;
#34752=ORIENTED_EDGE ( 'NONE', *, *, #24619, .F. ) ;
#34755=CARTESIAN_POINT ( 'NONE',  ( -0.02235124290212954848, -0.4612278572487644168, 0.2234747101372511757 ) ) ;
#34763=CARTESIAN_POINT ( 'NONE',  ( -0.01548846960721245516, -0.07651041855108924039, -0.5222379212565266826 ) ) ;
#34770=SPHERICAL_SURFACE ( 'NONE', #25900, 0.01499999999999999944 ) ;
#34774=CARTESIAN_POINT ( 'NONE',  ( 0.04285427992854566603, -0.3459934409501838615, 0.3537438177964201125 ) ) ;
#34792=ORIENTED_EDGE ( 'NONE', *, *, #3963, .T. ) ;
#34818=CARTESIAN_POINT ( 'NONE',  ( 0.02231181081520564047, -0.5045902076536123992, -0.09028112709016493376 ) ) ;
#34828=CARTESIAN_POINT ( 'NONE',  ( -0.05279185365593443147, -0.03990109708163243341, 0.4667311364329202461 ) ) ;
#34829=VERTEX_POINT ( 'NONE', #30934 ) ;
#34831=CARTESIAN_POINT ( 'NONE',  ( 0.01548846960707524721, 0.000000000000000000, 0.000000000000000000 ) ) ;
#34844=EDGE_CURVE ( 'NONE', #11318, #28442, #10756, .T. ) ;
#34846=CARTESIAN_POINT ( 'NONE',  ( 0.05281452789367269141, 0.4315450824722586454, 0.1820506770216148984 ) ) ;
#34848=CARTESIAN_POINT ( 'NONE',  ( 0.02953079040094746394, -0.2329676531120573046, -0.4763574306556540017 ) ) ;
#34850=DIRECTION ( 'NONE',  ( -1.000000000000000000, -2.280301054154495132E-31, 1.664003471950577689E-31 ) ) ;
#34851=ORIENTED_EDGE ( 'NONE', *, *, #36156, .F. ) ;
#34865=CARTESIAN_POINT ( 'NONE',  ( -0.04760454375021202361, 0.3171166672795173724, -0.3633054878239675989 ) ) ;
#34866=CARTESIAN_POINT ( 'NONE',  ( 0.1499999999999994948, -0.4638115001430989648, 0.2459753896937853235 ) ) ;
#34880=CARTESIAN_POINT ( 'NONE',  ( 0.02238826743734038255, 0.4611641377668463937, -0.2234181651772549626 ) ) ;
#34894=EDGE_CURVE ( 'NONE', #3242, #1535, #1964, .T. ) ;
#34904=AXIS2_PLACEMENT_3D ( 'NONE', #14994, #24460, #12114 ) ;
#34906=EDGE_LOOP ( 'NONE', ( #16758, #40367, #9655 ) ) ;
#34907=ORIENTED_EDGE ( 'NONE', *, *, #9377, .F. ) ;
#34913=CIRCLE ( 'NONE', #17172, 0.01500000000000003240 ) ;
#34918=CARTESIAN_POINT ( 'NONE',  ( -0.01548846960707490547, 0.09061086148575973886, 0.5171215251571029681 ) ) ;
#34922=FACE_OUTER_BOUND ( 'NONE', #35043, .T. ) ;
#34927=LINE ( 'NONE', #16226, #383 ) ;
#34932=CARTESIAN_POINT ( 'NONE',  ( 0.01548846960707524721, -0.3880410510314797334, -0.3755318131854984420 ) ) ;
#34941=DIRECTION ( 'NONE',  ( 0.000000000000000000, 3.330669073875470114E-16, 1.000000000000000000 ) ) ;
#34949=CARTESIAN_POINT ( 'NONE',  ( 0.01548846960712814240, 0.3688619771571980954, 0.3775276577326248106 ) ) ;
#34957=VERTEX_POINT ( 'NONE', #29232 ) ;
#34963=CARTESIAN_POINT ( 'NONE',  ( -0.01548846960707477016, 0.4638115001430989648, -0.2459753896937820483 ) ) ;
#34967=ORIENTED_EDGE ( 'NONE', *, *, #23535, .F. ) ;
#34969=FACE_OUTER_BOUND ( 'NONE', #15718, .T. ) ;
#34989=CARTESIAN_POINT ( 'NONE',  ( -0.02881195911415162028, 0.4889334074056331247, 0.09563129189200904323 ) ) ;
#34996=CARTESIAN_POINT ( 'NONE',  ( 0.1499999999999993561, 0.000000000000000000, 0.000000000000000000 ) ) ;
#35016=CIRCLE ( 'NONE', #27807, 0.1749999999999999889 ) ;
#35019=EDGE_CURVE ( 'NONE', #23130, #35163, #10106, .T. ) ;
#35021=VECTOR ( 'NONE', #3867, 39.37007874015748143 ) ;
#35036=CARTESIAN_POINT ( 'NONE',  ( -0.03158843595483506322, 0.4482533282648962225, -0.2030547983902464548 ) ) ;
#35043=EDGE_LOOP ( 'NONE', ( #423, #38892, #21810 ) ) ;
#35051=EDGE_CURVE ( 'NONE', #17498, #11318, #8222, .T. ) ;
#35058=ORIENTED_EDGE ( 'NONE', *, *, #12663, .T. ) ;
#35079=CARTESIAN_POINT ( 'NONE',  ( -0.05269191099235902981, 0.2718205810684086177, -0.3817379850160022015 ) ) ;
#35083=DIRECTION ( 'NONE',  ( 0.000000000000000000, 0.5877852522925025580, 0.8090169943749260240 ) ) ;
#35086=AXIS2_PLACEMENT_3D ( 'NONE', #28182, #27984, #12539 ) ;
#35091=CARTESIAN_POINT ( 'NONE',  ( 0.03674078017396296275, 0.4681991728402117303, -0.1092756390057526977 ) ) ;
#35094=CARTESIAN_POINT ( 'NONE',  ( 0.01548846960721255751, -0.3688619771570325612, 0.3775276577325259453 ) ) ;
#35103=VERTEX_POINT ( 'NONE', #24694 ) ;
#35120=EDGE_LOOP ( 'NONE', ( #39153, #37420, #17252, #10186 ) ) ;
#35136=DIRECTION ( 'NONE',  ( -0.3468893892380662258, 0.7770416411310642202, 0.5252371270030176120 ) ) ;
#35140=FACE_OUTER_BOUND ( 'NONE', #13798, .T. ) ;
#35141=CARTESIAN_POINT ( 'NONE',  ( 0.01548846960707511190, -0.2372406987223689145, -0.4850946823762606330 ) ) ;
#35156=LINE ( 'NONE', #6956, #35021 ) ;
#35163=VERTEX_POINT ( 'NONE', #24892 ) ;
#35178=CARTESIAN_POINT ( 'NONE',  ( -0.01895494625228204277, -0.2428766181966267312, 0.4598657641708858157 ) ) ;
#35188=EDGE_CURVE ( 'NONE', #20386, #1061, #36, .T. ) ;
#35191=CARTESIAN_POINT ( 'NONE',  ( -0.03664605387828188954, -0.04106737781738599435, -0.4792329708773129804 ) ) ;
#35200=DIRECTION ( 'NONE',  ( -0.3468893892380670585, 0.3199132558031868578, 0.8816593788960934708 ) ) ;
#35207=DIRECTION ( 'NONE',  ( -3.557093741750344791E-15, 0.1725921171157282497, 0.9849933812516257214 ) ) ;
#35209=CARTESIAN_POINT ( 'NONE',  ( -0.03478489236951871899, 0.5086709597375717040, 0.08927530733454300260 ) ) ;
#35211=CIRCLE ( 'NONE', #7617, 0.5302738246768095021 ) ;
#35213=FACE_OUTER_BOUND ( 'NONE', #16302, .T. ) ;
#35214=ORIENTED_EDGE ( 'NONE', *, *, #500, .F. ) ;
#35215=DIRECTION ( 'NONE',  ( -1.355854680848614260E-31, 3.330669073875470114E-16, 1.000000000000000000 ) ) ;
#35220=ORIENTED_EDGE ( 'NONE', *, *, #26487, .F. ) ;
#35231=ORIENTED_EDGE ( 'NONE', *, *, #22268, .T. ) ;
#35235=ORIENTED_EDGE ( 'NONE', *, *, #27386, .F. ) ;
#35238=CARTESIAN_POINT ( 'NONE',  ( -0.05562150110511286660, 0.02029635476683722128, 0.4604536315446554617 ) ) ;
#35247=CARTESIAN_POINT ( 'NONE',  ( 0.03868649100028236087, -0.4417196792138927131, -0.1788567627196029908 ) ) ;
#35253=CARTESIAN_POINT ( 'NONE',  ( -0.04154009738085516490, 0.4523583096281902916, -0.1287716261385808969 ) ) ;
#35254=CARTESIAN_POINT ( 'NONE',  ( -0.04574984450155272081, -0.06505050184192864848, 0.4827809015761243550 ) ) ;
#35267=DIRECTION ( 'NONE',  ( 0.000000000000000000, -3.330669073875470114E-16, -1.000000000000000000 ) ) ;
#35285=CARTESIAN_POINT ( 'NONE',  ( -0.05138886601527986597, 0.2591656398409026285, -0.3946081992295794039 ) ) ;
#35289=EDGE_LOOP ( 'NONE', ( #27014, #30762, #1537, #37940 ) ) ;
#35294=DIRECTION ( 'NONE',  ( -3.389636702121535101E-31, -0.4685245517976796559, 0.8834504764630461970 ) ) ;
#35295=CARTESIAN_POINT ( 'NONE',  ( 0.04308611741967136727, 0.4845711164928941939, -0.09763251765259810255 ) ) ;
#35298=CARTESIAN_POINT ( 'NONE',  ( 0.02235124290213176892, -0.07000983313419581466, 0.5077112423787075723 ) ) ;
#35309=EDGE_CURVE ( 'NONE', #17498, #34509, #2916, .T. ) ;
#35312=CARTESIAN_POINT ( 'NONE',  ( -0.01895494625228242788, -0.3623053290766977130, -0.3730957266516564674 ) ) ;
#35313=CARTESIAN_POINT ( 'NONE',  ( 0.01548846960707524721, 0.000000000000000000, 0.000000000000000000 ) ) ;
#35314=DIRECTION ( 'NONE',  ( 0.000000000000000000, 3.330669073875469621E-16, 1.000000000000000000 ) ) ;
#35326=EDGE_CURVE ( 'NONE', #16165, #5083, #2252, .T. ) ;
#35337=CARTESIAN_POINT ( 'NONE',  ( 0.1499999999999994671, 0.5230810839623362130, 0.1699593469062180839 ) ) ;
#35363=CARTESIAN_POINT ( 'NONE',  ( 0.02953079040095687308, -0.3810518745593889922, -0.3687679460475752902 ) ) ;
#35365=CARTESIAN_POINT ( 'NONE',  ( -0.01895884884825279129, -0.07380796352548195383, 0.5147901372834200462 ) ) ;
#35368=CYLINDRICAL_SURFACE ( 'NONE', #25222, 0.5400000000000007017 ) ;
#35371=CARTESIAN_POINT ( 'NONE',  ( 0.05082303569918648206, 0.4330427793496112732, -0.1918498709088735932 ) ) ;
#35391=CYLINDRICAL_SURFACE ( 'NONE', #10651, 0.2149999999999999967 ) ;
#35406=EDGE_CURVE ( 'NONE', #33948, #1932, #40464, .T. ) ;
#35409=CARTESIAN_POINT ( 'NONE',  ( -0.01548846960707517956, -0.3880410510314710182, 0.3755318131855027719 ) ) ;
#35420=VERTEX_POINT ( 'NONE', #3034 ) ;
#35441=ORIENTED_EDGE ( 'NONE', *, *, #36090, .F. ) ;
#35446=DIRECTION ( 'NONE',  ( -0.9378410757839559242, 0.1072489841977647268, 0.3300784330442382841 ) ) ;
#35448=VERTEX_POINT ( 'NONE', #19273 ) ;
#35454=CARTESIAN_POINT ( 'NONE',  ( -0.05252049209742535446, 0.4488546425834959441, -0.1362647994370397020 ) ) ;
#35474=CARTESIAN_POINT ( 'NONE',  ( 0.1499999999999993561, 0.2372406987223596164, -0.4850946823762614102 ) ) ;
#35477=CARTESIAN_POINT ( 'NONE',  ( 0.03170874437002939306, 0.4481116538287104878, -0.2027256324086052497 ) ) ;
#35481=CARTESIAN_POINT ( 'NONE',  ( 0.04229956186878614660, -0.008769846780145499829, 0.4686106502047106548 ) ) ;
#35488=CARTESIAN_POINT ( 'NONE',  ( -0.01548846960707545191, -0.5198120922912051745, -0.07362328916749329155 ) ) ;
#35490=ORIENTED_EDGE ( 'NONE', *, *, #30129, .F. ) ;
#35491=CARTESIAN_POINT ( 'NONE',  ( -0.02869942827333507931, -0.2420058122830170133, -0.4357544236535315640 ) ) ;
#35506=LINE ( 'NONE', #36323, #28994 ) ;
#35516=CARTESIAN_POINT ( 'NONE',  ( 0.01896931156526852555, -0.5123785568735317320, 0.08888416637129550879 ) ) ;
#35519=ORIENTED_EDGE ( 'NONE', *, *, #12663, .F. ) ;
#35522=EDGE_CURVE ( 'NONE', #26696, #33794, #3215, .T. ) ;
#35541=CARTESIAN_POINT ( 'NONE',  ( 0.04582889109739276406, -0.3361233334070946599, 0.3523147457849545305 ) ) ;
#35546=ORIENTED_EDGE ( 'NONE', *, *, #20803, .F. ) ;
#35552=CARTESIAN_POINT ( 'NONE',  ( -0.03159140494780145886, -0.05458666898339269852, 0.4890560705835251265 ) ) ;
#35557=CARTESIAN_POINT ( 'NONE',  ( 0.1499999999999993561, 0.000000000000000000, 0.000000000000000000 ) ) ;
#35561=ORIENTED_EDGE ( 'NONE', *, *, #35188, .F. ) ;
#35566=CARTESIAN_POINT ( 'NONE',  ( -0.04229956186878663926, -0.2683474741743150926, 0.3842687663629376082 ) ) ;
#35567=CARTESIAN_POINT ( 'NONE',  ( -0.01548846960707517956, -0.3880410510314797334, -0.3755318131854984420 ) ) ;
#35574=EDGE_CURVE ( 'NONE', #15099, #5283, #7474, .T. ) ;
#35577=DIRECTION ( 'NONE',  ( 1.000000000000000000, 2.341930812374887555E-31, -1.664003471950578127E-31 ) ) ;
#35579=CARTESIAN_POINT ( 'NONE',  ( 0.05634304521267768928, 0.01028134608272430507, -0.4588823192046728727 ) ) ;
#35580=EDGE_CURVE ( 'NONE', #26731, #20917, #11074, .T. ) ;
#35585=CARTESIAN_POINT ( 'NONE',  ( 0.03309060444528726108, 0.5154120966056442432, 0.07470591001490144156 ) ) ;
#35617=AXIS2_PLACEMENT_3D ( 'NONE', #16947, #16342, #25813 ) ;
#35619=VERTEX_POINT ( 'NONE', #20478 ) ;
#35622=EDGE_CURVE ( 'NONE', #33009, #2590, #11026, .T. ) ;
#35648=AXIS2_PLACEMENT_3D ( 'NONE', #3319, #22476, #22692 ) ;
#35673=CIRCLE ( 'NONE', #17931, 0.5400000000000018119 ) ;
#35680=ORIENTED_EDGE ( 'NONE', *, *, #33352, .T. ) ;
#35688=CARTESIAN_POINT ( 'NONE',  ( -0.03301200226531718351, -0.5156245478783716418, -0.07469833545740128811 ) ) ;
#35698=CARTESIAN_POINT ( 'NONE',  ( -0.04139678531769525743, -0.2626830136224073131, -0.3904580303439415534 ) ) ;
#35700=ORIENTED_EDGE ( 'NONE', *, *, #23991, .F. ) ;
#35702=CARTESIAN_POINT ( 'NONE',  ( -0.02953079040095700838, 0.09152108205202039160, -0.5223162075576429642 ) ) ;
#35705=VECTOR ( 'NONE', #6145, 39.37007874015748854 ) ;
#35709=CARTESIAN_POINT ( 'NONE',  ( 0.04285640132273748487, 0.07199195674534319966, 0.4895487002729358439 ) ) ;
#35730=CARTESIAN_POINT ( 'NONE',  ( 0.05561310505366579698, -0.4442420632723498852, 0.1228816621031077888 ) ) ;
#35731=AXIS2_PLACEMENT_3D ( 'NONE', #7567, #7959, #20336 ) ;
#35740=CIRCLE ( 'NONE', #2254, 0.01499999999999995087 ) ;
#35742=CARTESIAN_POINT ( 'NONE',  ( 0.1499999999999993561, 0.000000000000000000, 0.000000000000000000 ) ) ;
#35744=B_SPLINE_CURVE_WITH_KNOTS ( 'NONE', 3,
 ( #40057, #6657, #30618, #27535, #3379, #25419, #39873, #2445, #11693, #12099, #37743, #24449, #36771, #9761, #8801, #21381, #15934, #11498 ),
 .UNSPECIFIED., .F., .F.,
 ( 4, 2, 2, 2, 2, 2, 2, 2, 4 ),
 ( -0.002633528389679740730, -0.001975271857855738500, -0.001317015326031736704, -0.0006587587942077344737, -5.022623837326774254E-07, 0.0006577542694402691188, 0.001316010801264271782, 0.001974267333088273579, 0.002632523864912275375 ),
 .UNSPECIFIED. ) ;
#35745=CARTESIAN_POINT ( 'NONE',  ( 0.1499999999999993561, 4.163336342344336410E-17, 0.1249999999999999584 ) ) ;
#35746=CARTESIAN_POINT ( 'NONE',  ( 0.04230170315644143225, 0.2684795119051849865, 0.3841679273482342949 ) ) ;
#35755=CARTESIAN_POINT ( 'NONE',  ( -0.04229883635638079231, -0.2789693855191311411, 0.3765531589812280977 ) ) ;
#35756=AXIS2_PLACEMENT_3D ( 'NONE', #5295, #15398, #21168 ) ;
#35766=CARTESIAN_POINT ( 'NONE',  ( -0.04582889109739315958, 0.4790149006698655176, 0.08746027838083748895 ) ) ;
#35776=CARTESIAN_POINT ( 'NONE',  ( -0.04154009738085443632, -0.4523583096281919014, 0.1287716261385827843 ) ) ;
#35782=CARTESIAN_POINT ( 'NONE',  ( 0.01548846960707511190, -0.2306506793133099031, -0.4716198300880795613 ) ) ;
#35790=AXIS2_PLACEMENT_3D ( 'NONE', #1671, #20578, #30036 ) ;
#35792=DIRECTION ( 'NONE',  ( 1.000000000000000000, 0.000000000000000000, 0.000000000000000000 ) ) ;
#35793=DIRECTION ( 'NONE',  ( 1.000000000000000000, 2.341930812374887555E-31, -1.664003471950578127E-31 ) ) ;
#35805=ORIENTED_EDGE ( 'NONE', *, *, #29321, .F. ) ;
#35823=CARTESIAN_POINT ( 'NONE',  ( 0.04087116408466945350, 0.4416914123362158384, 0.1656680454788718726 ) ) ;
#35830=VERTEX_POINT ( 'NONE', #15129 ) ;
#35837=ADVANCED_FACE ( 'NONE', ( #5858 ), #30970, .F. ) ;
#35875=CARTESIAN_POINT ( 'NONE',  ( -0.05252359774140372833, 0.4432374118283854969, -0.1535299757497269879 ) ) ;
#35890=CYLINDRICAL_SURFACE ( 'NONE', #3580, 0.01500000000000005669 ) ;
#35894=CARTESIAN_POINT ( 'NONE',  ( -0.03171893264487379849, 0.2437375926088032885, -0.4645571062479579294 ) ) ;
#35896=FACE_OUTER_BOUND ( 'NONE', #10819, .T. ) ;
#35906=CARTESIAN_POINT ( 'NONE',  ( -0.05634115714581187234, -0.2655021207500423142, -0.3743162705049757344 ) ) ;
#35910=DIRECTION ( 'NONE',  ( 1.000000000000000000, 2.410886674703102177E-13, -1.702189702233166186E-12 ) ) ;
#35937=AXIS2_PLACEMENT_3D ( 'NONE', #30333, #27268, #5029 ) ;
#35943=CARTESIAN_POINT ( 'NONE',  ( 0.04946288932099940361, -0.4418470831553522049, 0.1805342557390068325 ) ) ;
#35950=DIRECTION ( 'NONE',  ( 5.264498737790488644E-15, 0.7185945389471800615, 0.6954292836768448671 ) ) ;
#35953=CARTESIAN_POINT ( 'NONE',  ( 0.03474878377840596305, 0.3591457335720743549, 0.3712550153170188216 ) ) ;
#35963=CARTESIAN_POINT ( 'NONE',  ( -0.04047161733260234984, -0.2415827978909579066, 0.4392067210493248997 ) ) ;
#35976=CARTESIAN_POINT ( 'NONE',  ( 0.05634307799789379373, 0.4332460723641315403, -0.1515798417490722971 ) ) ;
#35991=CARTESIAN_POINT ( 'NONE',  ( 0.05083674528491994443, 0.04859289555129429894, -0.4711018118971372903 ) ) ;
#35994=DIRECTION ( 'NONE',  ( 0.000000000000000000, 0.000000000000000000, -1.000000000000000000 ) ) ;
#36009=ORIENTED_EDGE ( 'NONE', *, *, #39683, .F. ) ;
#36014=VERTEX_POINT ( 'NONE', #40632 ) ;
#36024=ORIENTED_EDGE ( 'NONE', *, *, #2430, .F. ) ;
#36071=CARTESIAN_POINT ( 'NONE',  ( -0.05076541221973576712, 0.4633004642377308580, -0.09914728473419241739 ) ) ;
#36082=ORIENTED_EDGE ( 'NONE', *, *, #29388, .T. ) ;
#36087=CARTESIAN_POINT ( 'NONE',  ( -0.04140212552917923311, -0.4524976860274254054, -0.1292082980168287876 ) ) ;
#36090=EDGE_CURVE ( 'NONE', #2531, #4571, #10815, .T. ) ;
#36094=CARTESIAN_POINT ( 'NONE',  ( 0.01548846960706656145, 0.5203207976468126050, -0.08861466064782015650 ) ) ;
#36097=CARTESIAN_POINT ( 'NONE',  ( -0.03309059653085742736, -0.08822156176787991633, -0.5132714489379855971 ) ) ;
#36098=CARTESIAN_POINT ( 'NONE',  ( -0.04211812644076833728, -0.2825523317586257077, -0.3743635450761886863 ) ) ;
#36105=ORIENTED_EDGE ( 'NONE', *, *, #34894, .T. ) ;
#36124=DIRECTION ( 'NONE',  ( -1.000000000000000000, -2.341930812374887555E-31, 1.664003471950578127E-31 ) ) ;
#36127=CARTESIAN_POINT ( 'NONE',  ( 0.02881195911414203767, -0.4889334074056480017, 0.09563129189200124392 ) ) ;
#36132=AXIS2_PLACEMENT_3D ( 'NONE', #2062, #4933, #17290 ) ;
#36138=CARTESIAN_POINT ( 'NONE',  ( 0.03664605387828104993, -0.2484618661253095717, -0.4118464167359250361 ) ) ;
#36143=CARTESIAN_POINT ( 'NONE',  ( -0.05634301242525831949, 0.4332457820339853383, -0.1515812001271586162 ) ) ;
#36144=( BOUNDED_SURFACE ( )  B_SPLINE_SURFACE ( 3, 2, ( 
 ( #6256, #8524, #27471 ),
 ( #34230, #24976, #5832 ),
 ( #9332, #34031, #37510 ),
 ( #5646, #6040, #18608 ),
 ( #17992, #2981, #24801 ),
 ( #36914, #37127, #15531 ),
 ( #15319, #21092, #37320 ),
 ( #18199, #27875, #21696 ),
 ( #27665, #30749, #33617 ),
 ( #21516, #30946, #21913 ),
 ( #39806, #36714, #8726 ),
 ( #18393, #5427, #2373 ),
 ( #34439, #12238, #14916 ),
 ( #2569, #24592, #8940 ),
 ( #15104, #2770, #31167 ),
 ( #39996, #28083, #40611 ),
 ( #12427, #11817, #21303 ),
 ( #9129, #33844, #24191 ),
 ( #18826, #31370, #24378 ),
 ( #40197, #3175, #11633 ),
 ( #12031, #40413, #15716 ),
 ( #30853, #18508, #31061 ) ),
 .UNSPECIFIED., .F., .F., .F. ) 
 B_SPLINE_SURFACE_WITH_KNOTS ( ( 4, 2, 2, 2, 2, 2, 2, 2, 2, 2, 4 ),
 ( 3, 3 ),
 ( 0.002013519961495851326, 0.002780892266055759107, 0.003548264570615667322, 0.004315636875175575538, 0.004699323027455529211, 0.005083009179735483753, 0.005466695332015438294, 0.005850381484295391968, 0.006617753788855299316, 0.007385126093415207531, 0.008152498397975115746 ),
 ( 0.000000000000000000, 1.000000000000000000 ),
 .UNSPECIFIED. ) 
 GEOMETRIC_REPRESENTATION_ITEM ( )  RATIONAL_B_SPLINE_SURFACE ( (
 ( 1.000000000000000000, 0.7283825911960393196, 1.000000000000000000),
 ( 1.000000000000000000, 0.7404375345927475260, 1.000000000000000000),
 ( 1.000000000000000000, 0.7521483142435417824, 1.000000000000000000),
 ( 1.000000000000000000, 0.7744460733777035477, 1.000000000000000000),
 ( 1.000000000000000000, 0.7845612039379376013, 1.000000000000000000),
 ( 1.000000000000000000, 0.8022035258264773594, 1.000000000000000000),
 ( 1.000000000000000000, 0.8093965293320570797, 1.000000000000000000),
 ( 1.000000000000000000, 0.8169028692726044705, 1.000000000000000000),
 ( 1.000000000000000000, 0.8188329634862745454, 1.000000000000000000),
 ( 1.000000000000000000, 0.8214004505364636000, 1.000000000000000000),
 ( 1.000000000000000000, 0.8220602406261303674, 1.000000000000000000),
 ( 1.000000000000000000, 0.8220736605435321476, 1.000000000000000000),
 ( 1.000000000000000000, 0.8214126668415425714, 1.000000000000000000),
 ( 1.000000000000000000, 0.8188520474558570461, 1.000000000000000000),
 ( 1.000000000000000000, 0.8169545908333386564, 1.000000000000000000),
 ( 1.000000000000000000, 0.8094771004221671395, 1.000000000000000000),
 ( 1.000000000000000000, 0.8022723753809033465, 1.000000000000000000),
 ( 1.000000000000000000, 0.7845733350635970549, 1.000000000000000000),
 ( 1.000000000000000000, 0.7744472902495431743, 1.000000000000000000),
 ( 1.000000000000000000, 0.7522916829161283570, 1.000000000000000000),
 ( 1.000000000000000000, 0.7403553004667449144, 1.000000000000000000),
 ( 1.000000000000000000, 0.7283825911960383204, 1.000000000000000000) ) ) 
 REPRESENTATION_ITEM ( '' )  SURFACE ( )  );
#36148=ADVANCED_FACE ( 'NONE', ( #29710 ), #35890, .T. ) ;
#36151=CARTESIAN_POINT ( 'NONE',  ( -0.04139678531769583336, -0.2901741387554249707, 0.3704845587920869154 ) ) ;
#36156=EDGE_CURVE ( 'NONE', #29592, #34829, #10481, .T. ) ;
#36159=CARTESIAN_POINT ( 'NONE',  ( 0.01548846960707511190, -0.2306506793134033284, 0.4716198300880330985 ) ) ;
#36160=CARTESIAN_POINT ( 'NONE',  ( -0.04582713223189560647, 0.3361263728083093150, -0.3523178389613189077 ) ) ;
#36164=ORIENTED_EDGE ( 'NONE', *, *, #3904, .F. ) ;
#36166=DIRECTION ( 'NONE',  ( -1.000000000000000000, -2.280301054154495132E-31, 1.664003471950577689E-31 ) ) ;
#36169=VECTOR ( 'NONE', #5324, 39.37007874015748143 ) ;
#36174=AXIS2_PLACEMENT_3D ( 'NONE', #6109, #25050, #18676 ) ;
#36179=DIRECTION ( 'NONE',  ( 1.848892746611741821E-31, 0.8983234858820565716, -0.4393346272634452432 ) ) ;
#36182=EDGE_CURVE ( 'NONE', #16165, #5331, #13455, .T. ) ;
#36183=CARTESIAN_POINT ( 'NONE',  ( 0.05562150110511221435, 0.02029635476683638168, -0.4604536315446552397 ) ) ;
#36191=CIRCLE ( 'NONE', #22414, 0.01500000000000005843 ) ;
#36195=TOROIDAL_SURFACE ( 'NONE', #39480, 0.5250000000000000222, 0.01499999999999999944 ) ;
#36200=DIRECTION ( 'NONE',  ( -1.000000000000000000, -2.280301054154495132E-31, 1.664003471950577689E-31 ) ) ;
#36201=DIRECTION ( 'NONE',  ( 0.9378410757839559242, 0.1072489841977647962, -0.3300784330442385062 ) ) ;
#36210=ORIENTED_EDGE ( 'NONE', *, *, #15696, .F. ) ;
#36220=ORIENTED_EDGE ( 'NONE', *, *, #27386, .T. ) ;
#36248=EDGE_LOOP ( 'NONE', ( #5136, #7471, #6963, #32647 ) ) ;
#36272=ORIENTED_EDGE ( 'NONE', *, *, #32338, .F. ) ;
#36274=CARTESIAN_POINT ( 'NONE',  ( 0.05082303569918595471, -0.4631054925596488903, -0.09932635337952287757 ) ) ;
#36291=DIRECTION ( 'NONE',  ( 0.000000000000000000, -1.000000000000000000, 3.330669073875470607E-16 ) ) ;
#36292=CARTESIAN_POINT ( 'NONE',  ( -0.04582897286455887842, -0.06484386734940761343, -0.4825967645925829941 ) ) ;
#36293=CARTESIAN_POINT ( 'NONE',  ( -0.04308449196698393990, -0.2425978208598452146, -0.4306872647601475146 ) ) ;
#36296=CIRCLE ( 'NONE', #28416, 0.7750185148639454624 ) ;
#36298=EDGE_CURVE ( 'NONE', #33486, #38078, #16084, .T. ) ;
#36302=CARTESIAN_POINT ( 'NONE',  ( 0.05562144613422628087, 0.2542273817772385258, 0.3844451335760726840 ) ) ;
#36306=CARTESIAN_POINT ( 'NONE',  ( 0.03174060074382504398, -0.5170807408089640456, -0.08825076429300719727 ) ) ;
#36315=EDGE_CURVE ( 'NONE', #11533, #22491, #1769, .T. ) ;
#36320=AXIS2_PLACEMENT_3D ( 'NONE', #32742, #29664, #32945 ) ;
#36322=CARTESIAN_POINT ( 'NONE',  ( 0.05634304521267768928, -2.731847993664263218E-15, -0.4588823192046729837 ) ) ;
#36323=CARTESIAN_POINT ( 'NONE',  ( -2.915087563824520450E-32, 7.160938508832261116E-17, 0.2149999999999999967 ) ) ;
#36332=CARTESIAN_POINT ( 'NONE',  ( 0.03647060353176064668, -0.5060729159580577008, 0.07645842516611485451 ) ) ;
#36347=CARTESIAN_POINT ( 'NONE',  ( 0.04308558661661603117, 0.3346374335305056791, 0.3638133228716420309 ) ) ;
#36369=DIRECTION ( 'NONE',  ( 0.000000000000000000, 0.9510565162951392093, -0.3090169943749916381 ) ) ;
#36370=VERTEX_POINT ( 'NONE', #3553 ) ;
#36371=DIRECTION ( 'NONE',  ( 0.000000000000000000, 0.000000000000000000, 1.000000000000000000 ) ) ;
#36378=DIRECTION ( 'NONE',  ( 0.000000000000000000, 3.330669073875470114E-16, 1.000000000000000000 ) ) ;
#36390=CARTESIAN_POINT ( 'NONE',  ( 0.04293324258486909406, 0.07181764475133010917, -0.4893676133895061842 ) ) ;
#36395=CARTESIAN_POINT ( 'NONE',  ( 0.05283102792148736127, 0.2421768296208689775, -0.4008516595826039364 ) ) ;
#36398=CARTESIAN_POINT ( 'NONE',  ( 0.01548846960703785525, -0.09061086148575045462, 0.5171215251571049665 ) ) ;
#36417=EDGE_LOOP ( 'NONE', ( #10277, #24448, #15874, #30495 ) ) ;
#36428=CARTESIAN_POINT ( 'NONE',  ( -0.02231181081520701784, -0.4612879682508957413, -0.2235517164227203701 ) ) ;
#36449=CARTESIAN_POINT ( 'NONE',  ( 0.08978098643734212791, 0.000000000000000000, 0.000000000000000000 ) ) ;
#36470=EDGE_CURVE ( 'NONE', #25200, #30050, #23958, .T. ) ;
#36478=ORIENTED_EDGE ( 'NONE', *, *, #24046, .T. ) ;
#36500=DIRECTION ( 'NONE',  ( 1.000000000000000000, 0.000000000000000000, 0.000000000000000000 ) ) ;
#36502=CARTESIAN_POINT ( 'NONE',  ( -0.05634490452572749747, -0.4379840114246532634, -0.1369850167785242601 ) ) ;
#36515=SPHERICAL_SURFACE ( 'NONE', #21240, 0.01499999999999999944 ) ;
#36516=CARTESIAN_POINT ( 'NONE',  ( -0.04947837552028281488, -0.3081459059633547826, -0.3644550506195411987 ) ) ;
#36524=CARTESIAN_POINT ( 'NONE',  ( 0.01548846960707511190, -0.2306506793134066036, 0.4716198300880325434 ) ) ;
#36530=CARTESIAN_POINT ( 'NONE',  ( 0.05489899477340703243, 0.4472784955204376911, 0.1186631084353854670 ) ) ;
#36534=CIRCLE ( 'NONE', #18812, 0.01499999999999994567 ) ;
#36536=ORIENTED_EDGE ( 'NONE', *, *, #23058, .T. ) ;
#36564=CARTESIAN_POINT ( 'NONE',  ( 0.01548846960707528191, 0.3772621329472709006, 0.3651003739303413931 ) ) ;
#36579=CARTESIAN_POINT ( 'NONE',  ( -0.05082303569918699554, 0.3162776479886636460, -0.3525632866555268863 ) ) ;
#36591=CARTESIAN_POINT ( 'NONE',  ( -0.01895884884825222924, -0.3622979475331346566, 0.3730907371368802350 ) ) ;
#36620=CARTESIAN_POINT ( 'NONE',  ( 0.04229956186878634783, 0.008769846780144823287, -0.4686106502047103217 ) ) ;
#36625=ORIENTED_EDGE ( 'NONE', *, *, #15767, .F. ) ;
#36632=CARTESIAN_POINT ( 'NONE',  ( -0.01548846960707524721, 0.000000000000000000, 0.000000000000000000 ) ) ;
#36656=ADVANCED_FACE ( 'NONE', ( #22448 ), #16720, .T. ) ;
#36664=FACE_OUTER_BOUND ( 'NONE', #2296, .T. ) ;
#36696=CARTESIAN_POINT ( 'NONE',  ( 0.05561176441985712926, -0.4442366066780392142, -0.1229089882096667807 ) ) ;
#36714=CARTESIAN_POINT ( 'NONE',  ( -0.05268850283020068415, 0.004611971649429206892, -0.4686124025367036650 ) ) ;
#36717=CARTESIAN_POINT ( 'NONE',  ( -0.02231181081520748968, 0.2417894035777240214, 0.4519954025055022973 ) ) ;
#36719=CARTESIAN_POINT ( 'NONE',  ( 0.04047043078436212554, -0.4536058588506475808, -0.2133299978720243073 ) ) ;
#36722=EDGE_CURVE ( 'NONE', #28751, #24257, #39697, .T. ) ;
#36723=CARTESIAN_POINT ( 'NONE',  ( 0.04308449196698531380, 0.4845747790795011944, 0.09763455429601687607 ) ) ;
#36735=ORIENTED_EDGE ( 'NONE', *, *, #7947, .F. ) ;
#36741=FACE_OUTER_BOUND ( 'NONE', #9193, .T. ) ;
#36758=EDGE_LOOP ( 'NONE', ( #33514, #31980, #21143, #19770 ) ) ;
#36762=CARTESIAN_POINT ( 'NONE',  ( -0.05634307799789460558, 0.2780413953411688399, -0.3652007531760524950 ) ) ;
#36768=EDGE_CURVE ( 'NONE', #1061, #2531, #16902, .T. ) ;
#36771=CARTESIAN_POINT ( 'NONE',  ( -0.03662792686184437874, 0.3149733899719671104, -0.3635662525351499585 ) ) ;
#36773=FACE_OUTER_BOUND ( 'NONE', #14328, .T. ) ;
#36777=EDGE_LOOP ( 'NONE', ( #34907, #30809 ) ) ;
#36780=VERTEX_POINT ( 'NONE', #17066 ) ;
#36782=LINE ( 'NONE', #27956, #15102 ) ;
#36795=ORIENTED_EDGE ( 'NONE', *, *, #34096, .F. ) ;
#36801=CARTESIAN_POINT ( 'NONE',  ( 0.1399999999999994582, 0.000000000000000000, 0.000000000000000000 ) ) ;
#36805=EDGE_LOOP ( 'NONE', ( #19926, #31758, #34752, #33592 ) ) ;
#36808=EDGE_LOOP ( 'NONE', ( #35235, #30576, #29297, #39533 ) ) ;
#36810=DIRECTION ( 'NONE',  ( -1.000000000000000000, -2.341930812374887555E-31, 1.664003471950578127E-31 ) ) ;
#36829=CARTESIAN_POINT ( 'NONE',  ( -0.04085667396267264606, -0.4547700361314969131, 0.1255037944140869888 ) ) ;
#36833=DIRECTION ( 'NONE',  ( -0.3468893892380655042, -0.7396492646828789486, -0.5767033179097537099 ) ) ;
#36841=EDGE_CURVE ( 'NONE', #38334, #20390, #15460, .T. ) ;
#36847=CARTESIAN_POINT ( 'NONE',  ( 0.03303737228521855251, -0.2303602220530255040, 0.4672390599430960578 ) ) ;
#36853=CARTESIAN_POINT ( 'NONE',  ( 0.03674078017396287255, 0.04075419261117436964, -0.4790519037776406197 ) ) ;
#36859=AXIS2_PLACEMENT_3D ( 'NONE', #10888, #36166, #36369 ) ;
#36862=VERTEX_POINT ( 'NONE', #4909 ) ;
#36878=CARTESIAN_POINT ( 'NONE',  ( -0.01896968469604467730, 0.4667670904252209652, -0.2292592343991369241 ) ) ;
#36888=VERTEX_POINT ( 'NONE', #18084 ) ;
#36892=EDGE_CURVE ( 'NONE', #3309, #5909, #2974, .T. ) ;
#36895=AXIS2_PLACEMENT_3D ( 'NONE', #20711, #30158, #33243 ) ;
#36904=CARTESIAN_POINT ( 'NONE',  ( 0.01548846960721238578, -0.4730347584884322942, -0.2341461249027902980 ) ) ;
#36911=CARTESIAN_POINT ( 'NONE',  ( -0.03674260963082343762, -0.2486114773148977442, 0.4115095709379189559 ) ) ;
#36914=CARTESIAN_POINT ( 'NONE',  ( -0.03672309138969848119, 0.04080728438229311306, -0.4790859898006342710 ) ) ;
#36917=EDGE_LOOP ( 'NONE', ( #31727, #17045, #38768 ) ) ;
#36919=CARTESIAN_POINT ( 'NONE',  ( 0.04946288932099964647, 0.03516002272508091803, 0.4760097007310892248 ) ) ;
#36936=CARTESIAN_POINT ( 'NONE',  ( -0.05283102792148739596, -0.4560693389104596429, 0.1064538768721983303 ) ) ;
#36951=CARTESIAN_POINT ( 'NONE',  ( -0.05616044724337349026, 0.2782405634116475457, 0.3655497896892119791 ) ) ;
#36955=CARTESIAN_POINT ( 'NONE',  ( 0.08978098643734198914, 0.000000000000000000, 0.000000000000000000 ) ) ;
#36957=CARTESIAN_POINT ( 'NONE',  ( 0.02869712619511934765, 0.3396447909410104660, -0.3648221446286666336 ) ) ;
#36972=CARTESIAN_POINT ( 'NONE',  ( 0.03875523708677872797, 0.2524014508497897102, -0.4040490413287913807 ) ) ;
#36982=ORIENTED_EDGE ( 'NONE', *, *, #8406, .T. ) ;
#36998=AXIS2_PLACEMENT_3D ( 'NONE', #32952, #30085, #4554 ) ;
#37001=DIRECTION ( 'NONE',  ( 1.000000000000000000, 2.280301054154495132E-31, -1.664003471950577689E-31 ) ) ;
#37008=FACE_OUTER_BOUND ( 'NONE', #36758, .T. ) ;
#37021=CARTESIAN_POINT ( 'NONE',  ( -0.1399999999999997358, -6.881499428057815777E-16, -0.2526340763130725531 ) ) ;
#37026=CARTESIAN_POINT ( 'NONE',  ( 0.1499999999999993561, 0.000000000000000000, 0.000000000000000000 ) ) ;
#37027=VERTEX_POINT ( 'NONE', #25482 ) ;
#37041=CARTESIAN_POINT ( 'NONE',  ( -0.05252359774140081400, -0.4432374118283890496, 0.1535299757497308182 ) ) ;
#37052=AXIS2_PLACEMENT_3D ( 'NONE', #22497, #3769, #34420 ) ;
#37067=CARTESIAN_POINT ( 'NONE',  ( 0.03647060353175951564, 0.08366884794402459913, -0.5049308971818783354 ) ) ;
#37068=ORIENTED_EDGE ( 'NONE', *, *, #8646, .F. ) ;
#37073=AXIS2_PLACEMENT_3D ( 'NONE', #2941, #15494, #37475 ) ;
#37076=AXIS2_PLACEMENT_3D ( 'NONE', #3249, #32039, #9630 ) ;
#37083=CARTESIAN_POINT ( 'NONE',  ( 0.01548846960707528191, 0.2306506793134000532, -0.4716198300880355410 ) ) ;
#37096=ORIENTED_EDGE ( 'NONE', *, *, #35309, .F. ) ;
#37100=EDGE_CURVE ( 'NONE', #38078, #19390, #34927, .T. ) ;
#37114=DIRECTION ( 'NONE',  ( -1.000000000000000000, -2.280301054154495132E-31, 1.664003471950577689E-31 ) ) ;
#37118=DIRECTION ( 'NONE',  ( 1.000000000000000000, 0.000000000000000000, 0.000000000000000000 ) ) ;
#37121=CARTESIAN_POINT ( 'NONE',  ( -0.02872242845530483327, -0.07817994906156928991, 0.5268390348591148742 ) ) ;
#37123=ORIENTED_EDGE ( 'NONE', *, *, #2962, .T. ) ;
#37125=CARTESIAN_POINT ( 'NONE',  ( -0.02953079040095600225, -0.3810518745593856060, 0.3687679460475811744 ) ) ;
#37127=CARTESIAN_POINT ( 'NONE',  ( -0.04760454375020840151, 0.04300716520882287563, -0.4803168140823134702 ) ) ;
#37132=CARTESIAN_POINT ( 'NONE',  ( 0.04575106512774732015, 0.06504741310981214386, 0.4827780559048400755 ) ) ;
#37134=CARTESIAN_POINT ( 'NONE',  ( 0.02881195911414813696, -0.4517660987406161843, -0.2100205058914844103 ) ) ;
#37138=CARTESIAN_POINT ( 'NONE',  ( 0.02872242845530460428, 0.5252126300208033172, 0.08844866507292861724 ) ) ;
#37145=ORIENTED_EDGE ( 'NONE', *, *, #14163, .T. ) ;
#37153=ORIENTED_EDGE ( 'NONE', *, *, #34844, .T. ) ;
#37163=DIRECTION ( 'NONE',  ( 1.000000000000000000, -3.624433060062967676E-13, 2.563064096159671966E-12 ) ) ;
#37165=CARTESIAN_POINT ( 'NONE',  ( -0.04575334816097949980, 0.3363904506959767282, 0.3523376320073900447 ) ) ;
#37169=AXIS2_PLACEMENT_3D ( 'NONE', #17164, #4210, #26234 ) ;
#37170=CARTESIAN_POINT ( 'NONE',  ( 0.03301162916267962738, 0.2303793641368860612, 0.4673060013142916191 ) ) ;
#37181=ORIENTED_EDGE ( 'NONE', *, *, #29068, .T. ) ;
#37186=CARTESIAN_POINT ( 'NONE',  ( 0.05634402396114654432, 0.2780622203583519858, -0.3651830615696467497 ) ) ;
#37211=B_SPLINE_CURVE_WITH_KNOTS ( 'NONE', 3,
 ( #30033, #26941, #17869, #1861, #14375, #30434, #36395, #27367, #20786, #2262, #5113, #14801, #25281, #9426, #15195, #3072, #9035, #37604 ),
 .UNSPECIFIED., .F., .F.,
 ( 4, 2, 2, 2, 2, 2, 2, 2, 4 ),
 ( -0.003133633995111165162, -0.002350221109836696590, -0.001566808224562228451, -0.0007833953392877598780, 1.754598670826099105E-08, 0.0007834304312611764000, 0.001566843316535645406, 0.002350256201810114413, 0.003133669087084581684 ),
 .UNSPECIFIED. ) ;
#37219=B_SPLINE_CURVE_WITH_KNOTS ( 'NONE', 3,
 ( #28379, #5184, #45, #31059, #34551, #37846, #12536, #34341, #34745, #6362, #27982, #18932, #9660, #462, #22229, #40522, #245, #28180 ),
 .UNSPECIFIED., .F., .F.,
 ( 4, 2, 2, 2, 2, 2, 2, 2, 4 ),
 ( 0.000000000000000000, 0.0007746617437634281808, 0.001549323487526856362, 0.002323985231290284434, 0.003098646975053712723, 0.003873308718817141012, 0.004647970462580568868, 0.005422632206343997591, 0.006197293950107425446 ),
 .UNSPECIFIED. ) ;
#37235=CARTESIAN_POINT ( 'NONE',  ( 0.1499999999999993561, 0.000000000000000000, 0.000000000000000000 ) ) ;
#37241=DIRECTION ( 'NONE',  ( 1.000000000000000000, 2.280301054154495132E-31, -1.664003471950577689E-31 ) ) ;
#37248=ORIENTED_EDGE ( 'NONE', *, *, #22056, .T. ) ;
#37268=CARTESIAN_POINT ( 'NONE',  ( 0.05082303569918614206, -0.2375724430107425122, 0.4097459652473660063 ) ) ;
#37299=CARTESIAN_POINT ( 'NONE',  ( 0.01548846960712797240, 0.5203207976466739382, 0.08861466064782476393 ) ) ;
#37301=CYLINDRICAL_SURFACE ( 'NONE', #24538, 0.5400000000000017009 ) ;
#37319=VERTEX_POINT ( 'NONE', #5866 ) ;
#37320=CARTESIAN_POINT ( 'NONE',  ( -0.05279185365593419554, 0.03990109708163099012, -0.4667311364329210233 ) ) ;
#37324=SPHERICAL_SURFACE ( 'NONE', #13935, 0.01499999999999999944 ) ;
#37330=CARTESIAN_POINT ( 'NONE',  ( 0.05543910610525055321, 0.4446004295725627387, 0.1230574251923951118 ) ) ;
#37332=CARTESIAN_POINT ( 'NONE',  ( -0.04293317454820666512, -0.3457449726441630400, -0.3536934093827145964 ) ) ;
#37339=CARTESIAN_POINT ( 'NONE',  ( -0.04582889109739119587, -0.4389390569944067177, 0.2108010426992260600 ) ) ;
#37346=ADVANCED_FACE ( 'NONE', ( #8553 ), #2410, .T. ) ;
#37351=CYLINDRICAL_SURFACE ( 'NONE', #15291, 0.01500000000000001159 ) ;
#37353=DIRECTION ( 'NONE',  ( 0.000000000000000000, -0.9510565162951504226, 0.3090169943749569437 ) ) ;
#37357=CARTESIAN_POINT ( 'NONE',  ( -0.05076541221973871615, 0.2374623881706967587, 0.4099867295868513950 ) ) ;
#37365=ORIENTED_EDGE ( 'NONE', *, *, #12510, .F. ) ;
#37375=CARTESIAN_POINT ( 'NONE',  ( 0.03647060353175536618, 0.3644804546768194431, -0.3593183619073302415 ) ) ;
#37377=DIRECTION ( 'NONE',  ( 2.532366176626897310E-12, -0.8090169943749517811, -0.5877852522924670309 ) ) ;
#37378=ORIENTED_EDGE ( 'NONE', *, *, #8982, .F. ) ;
#37392=ORIENTED_EDGE ( 'NONE', *, *, #32958, .T. ) ;
#37396=ORIENTED_EDGE ( 'NONE', *, *, #9894, .F. ) ;
#37420=ORIENTED_EDGE ( 'NONE', *, *, #36315, .F. ) ;
#37429=EDGE_LOOP ( 'NONE', ( #3803, #32354, #22644, #5678 ) ) ;
#37430=CARTESIAN_POINT ( 'NONE',  ( 0.02869942827333582178, 0.4519168387192257219, -0.2102852866807453092 ) ) ;
#37444=CARTESIAN_POINT ( 'NONE',  ( -0.04211812644076767115, -0.4433543613217511004, 0.1530385388104371636 ) ) ;
#37454=TOROIDAL_SURFACE ( 'NONE', #32867, 0.5250000000000000222, 0.01499999999999999944 ) ;
#37455=CARTESIAN_POINT ( 'NONE',  ( 0.04285640132274435438, -0.2295067898340903967, 0.4383690285535427056 ) ) ;
#37473=CARTESIAN_POINT ( 'NONE',  ( -0.02953079040095700838, 0.000000000000000000, 0.000000000000000000 ) ) ;
#37475=DIRECTION ( 'NONE',  ( 1.000000000000000000, 0.000000000000000000, 0.000000000000000000 ) ) ;
#37479=VERTEX_POINT ( 'NONE', #11570 ) ;
#37482=TOROIDAL_SURFACE ( 'NONE', #13204, 0.5250000000000000222, 0.01499999999999999944 ) ;
#37485=CARTESIAN_POINT ( 'NONE',  ( -0.04293317454820668594, -0.2295413494973332635, 0.4381202835071946189 ) ) ;
#37497=PRODUCT_CONTEXT ( 'NONE', #28459, 'mechanical' ) ;
#37499=CIRCLE ( 'NONE', #31614, 0.01500000000000002894 ) ;
#37501=CARTESIAN_POINT ( 'NONE',  ( -0.05186792262757373290, -0.01796889665935117592, 0.4704835727131218004 ) ) ;
#37505=DIRECTION ( 'NONE',  ( 1.000000000000000000, 2.280301054154495132E-31, -1.664003471950577689E-31 ) ) ;
#37510=CARTESIAN_POINT ( 'NONE',  ( -0.03642997641688962979, 0.08373618209168329218, -0.5050295872266733488 ) ) ;
#37512=VERTEX_POINT ( 'NONE', #11759 ) ;
#37521=CARTESIAN_POINT ( 'NONE',  ( 0.03171861681798098659, -0.2437378752574246299, -0.4645579091361444757 ) ) ;
#37539=CARTESIAN_POINT ( 'NONE',  ( -0.03672309138970014653, 0.3146134659443282633, -0.3636027875696382083 ) ) ;
#37545=CARTESIAN_POINT ( 'NONE',  ( 0.1499999999999993561, 0.000000000000000000, 0.000000000000000000 ) ) ;
#37548=CARTESIAN_POINT ( 'NONE',  ( -0.01896968469603047686, 0.3622774521524885771, 0.3730768833943122753 ) ) ;
#37568=AXIS2_PLACEMENT_3D ( 'NONE', #29008, #35793, #35994 ) ;
#37571=CARTESIAN_POINT ( 'NONE',  ( 0.05078310099560659485, 0.3164655623698883202, -0.3525377550954976180 ) ) ;
#37604=CARTESIAN_POINT ( 'NONE',  ( 0.02953079040095700838, 0.3810518745593862167, -0.3687679460475775106 ) ) ;
#37627=CARTESIAN_POINT ( 'NONE',  ( 0.03664605387828134830, 0.2484618661253114036, 0.4118464167359231487 ) ) ;
#37648=ORIENTED_EDGE ( 'NONE', *, *, #2962, .F. ) ;
#37652=CIRCLE ( 'NONE', #19915, 0.01500000000000004628 ) ;
#37653=CARTESIAN_POINT ( 'NONE',  ( -0.01899468245561876031, -0.5123206680798518819, 0.08888613072388566738 ) ) ;
#37670=AXIS2_PLACEMENT_3D ( 'NONE', #831, #38824, #16632 ) ;
#37675=CARTESIAN_POINT ( 'NONE',  ( -2.915087563824520450E-32, 7.160938508832261116E-17, 0.2149999999999999967 ) ) ;
#37708=CARTESIAN_POINT ( 'NONE',  ( 0.03309057659885075720, -0.5154121718708735145, 0.07470590733143715745 ) ) ;
#37710=FACE_OUTER_BOUND ( 'NONE', #6597, .T. ) ;
#37721=CARTESIAN_POINT ( 'NONE',  ( -0.04760454375020965745, -0.04300716520882088417, 0.4803168140823217969 ) ) ;
#37729=EDGE_LOOP ( 'NONE', ( #1291, #7420, #5699 ) ) ;
#37739=DIRECTION ( 'NONE',  ( 1.702140497302368679E-12, -0.9510565162951529761, 0.3090169943749491166 ) ) ;
#37741=CARTESIAN_POINT ( 'NONE',  ( 0.03674078017396031209, -0.2486088097086599225, -0.4115158447297234123 ) ) ;
#37743=CARTESIAN_POINT ( 'NONE',  ( -0.04154009738085503306, 0.2902754972779528764, -0.3700679770908116284 ) ) ;
#37747=CARTESIAN_POINT ( 'NONE',  ( 0.05561170715395061942, 0.02038383341412389541, 0.4604752114371306604 ) ) ;
#37754=EDGE_CURVE ( 'NONE', #39055, #34829, #18778, .T. ) ;
#37759=CARTESIAN_POINT ( 'NONE',  ( -0.05268850283020189845, 0.2791746226943783160, -0.3764045485075417363 ) ) ;
#37767=CARTESIAN_POINT ( 'NONE',  ( -0.05268850283020295316, 0.2717122958104549735, 0.3818262463465875722 ) ) ;
#37775=DIRECTION ( 'NONE',  ( -2.563099466555626504E-12, -0.5877852522924708056, 0.8090169943749491166 ) ) ;
#37777=AXIS2_PLACEMENT_3D ( 'NONE', #11132, #17100, #29859 ) ;
#37780=CARTESIAN_POINT ( 'NONE',  ( -0.04293694706340306366, -0.07181688488226570244, 0.4893579783149998308 ) ) ;
#37781=VECTOR ( 'NONE', #13858, 39.37007874015748143 ) ;
#37782=CIRCLE ( 'NONE', #29247, 0.5302738246768099462 ) ;
#37788=CARTESIAN_POINT ( 'NONE',  ( 0.05279905671745029061, 0.3065870127358052422, -0.3541429396892920578 ) ) ;
#37805=ORIENTED_EDGE ( 'NONE', *, *, #18046, .F. ) ;
#37810=ORIENTED_EDGE ( 'NONE', *, *, #5765, .F. ) ;
#37822=EDGE_CURVE ( 'NONE', #35420, #17096, #6283, .T. ) ;
#37846=CARTESIAN_POINT ( 'NONE',  ( -0.05082303569918675268, -0.4330427793496107181, -0.1918498709088775622 ) ) ;
#37848=DIRECTION ( 'NONE',  ( -1.000000000000000000, -2.341930812374887555E-31, 1.664003471950578127E-31 ) ) ;
#37852=ORIENTED_EDGE ( 'NONE', *, *, #28999, .T. ) ;
#37864=CARTESIAN_POINT ( 'NONE',  ( -0.01548846960707490547, 0.5198120922912040642, 0.07362328916749247276 ) ) ;
#37870=DIRECTION ( 'NONE',  ( 9.244463733058726621E-33, 0.4685245517976878160, 0.8834504764630419782 ) ) ;
#37874=ADVANCED_FACE ( 'NONE', ( #38674 ), #4107, .T. ) ;
#37876=FACE_OUTER_BOUND ( 'NONE', #36917, .T. ) ;
#37879=AXIS2_PLACEMENT_3D ( 'NONE', #10677, #1255, #13757 ) ;
#37880=CARTESIAN_POINT ( 'NONE',  ( 0.03647060353175276409, -0.3644804546768179443, 0.3593183619073416768 ) ) ;
#37887=CARTESIAN_POINT ( 'NONE',  ( -0.03674078017396703588, 0.4681991728402010167, 0.1092756390057632171 ) ) ;
#37906=CIRCLE ( 'NONE', #35937, 0.01500000000000004108 ) ;
#37912=DIRECTION ( 'NONE',  ( 0.000000000000000000, 0.9510565162951442053, 0.3090169943749759840 ) ) ;
#37932=CARTESIAN_POINT ( 'NONE',  ( -0.05252049209742314095, -0.009108187116140229606, 0.4689942714594981243 ) ) ;
#37935=CARTESIAN_POINT ( 'NONE',  ( 0.06980746140711596714, 0.1750000000000001832, 0.000000000000000000 ) ) ;
#37940=ORIENTED_EDGE ( 'NONE', *, *, #4202, .F. ) ;
#37954=VERTEX_POINT ( 'NONE', #38865 ) ;
#37960=DIRECTION ( 'NONE',  ( 0.000000000000000000, 0.000000000000000000, -1.000000000000000000 ) ) ;
#37966=CARTESIAN_POINT ( 'NONE',  ( -0.05616044724337223432, 0.2616774468955962440, -0.3775835982344354358 ) ) ;
#37969=CARTESIAN_POINT ( 'NONE',  ( -0.04285534776242287680, -0.4433434382090528647, -0.2197501713291542813 ) ) ;
#37975=CARTESIAN_POINT ( 'NONE',  ( 0.05561375719525413902, 0.4316271021131491969, -0.1617018132803443586 ) ) ;
#37991=CYLINDRICAL_SURFACE ( 'NONE', #15378, 0.01500000000000004975 ) ;
#38022=DIRECTION ( 'NONE',  ( 0.000000000000000000, 0.3090169943749439541, -0.9510565162951547524 ) ) ;
#38027=DIRECTION ( 'NONE',  ( -0.9378410757839567014, 0.1072489841977716934, 0.3300784330442341763 ) ) ;
#38059=LINE ( 'NONE', #22053, #6702 ) ;
#38066=CARTESIAN_POINT ( 'NONE',  ( 0.01548846960706677829, -0.4638115001431235562, -0.2459753896937935114 ) ) ;
#38068=CARTESIAN_POINT ( 'NONE',  ( 0.02872242845529797070, -0.3729171224323792888, 0.3802687114177617511 ) ) ;
#38073=CARTESIAN_POINT ( 'NONE',  ( -0.04047043078436820401, 0.4923670751789595568, 0.09403524049742544022 ) ) ;
#38074=CARTESIAN_POINT ( 'NONE',  ( 0.01548846960707528191, 0.3772621329472714558, 0.3651003739303416706 ) ) ;
#38078=VERTEX_POINT ( 'NONE', #5115 ) ;
#38087=ORIENTED_EDGE ( 'NONE', *, *, #18962, .F. ) ;
#38109=CARTESIAN_POINT ( 'NONE',  ( 0.02953079040095673430, -0.5250338024619264354, 0.07436286310882474215 ) ) ;
#38118=CARTESIAN_POINT ( 'NONE',  ( -0.02872242845530525307, 0.07817994906157108015, 0.5268390348591135419 ) ) ;
#38119=EDGE_CURVE ( 'NONE', #35619, #32432, #10230, .T. ) ;
#38120=ORIENTED_EDGE ( 'NONE', *, *, #13555, .F. ) ;
#38132=DIRECTION ( 'NONE',  ( 0.000000000000000000, 0.4393346272636315941, -0.8983234858819654223 ) ) ;
#38135=CARTESIAN_POINT ( 'NONE',  ( 0.01548846960707524721, -0.09061086148575756005, -0.5171215251571035232 ) ) ;
#38137=DIRECTION ( 'NONE',  ( 1.000000000000000000, 1.693379103678900805E-12, -2.967165974375313612E-13 ) ) ;
#38139=EDGE_LOOP ( 'NONE', ( #33084, #35214, #21113 ) ) ;
#38151=CARTESIAN_POINT ( 'NONE',  ( 0.1499999999999990508, -0.5230810839623395436, 0.1699593469062158912 ) ) ;
#38156=CARTESIAN_POINT ( 'NONE',  ( -0.04945776359514979931, 0.3082555652855902273, -0.3644343153303183369 ) ) ;
#38177=CARTESIAN_POINT ( 'NONE',  ( -0.02953079040095680369, -0.09152108205201929525, 0.5223162075576431862 ) ) ;
#38183=FACE_OUTER_BOUND ( 'NONE', #19336, .T. ) ;
#38203=EDGE_LOOP ( 'NONE', ( #28985, #28085, #20671, #25504 ) ) ;
#38204=ORIENTED_EDGE ( 'NONE', *, *, #17479, .T. ) ;
#38230=ORIENTED_EDGE ( 'NONE', *, *, #19620, .F. ) ;
#38231=FACE_OUTER_BOUND ( 'NONE', #5542, .T. ) ;
#38238=ORIENTED_EDGE ( 'NONE', *, *, #1734, .T. ) ;
#38253=CARTESIAN_POINT ( 'NONE',  ( -0.04285561529641037509, -0.4433460678679742029, 0.2197428102801966265 ) ) ;
#38260=CARTESIAN_POINT ( 'NONE',  ( 0.01548846960707524721, 0.000000000000000000, 0.000000000000000000 ) ) ;
#38265=CARTESIAN_POINT ( 'NONE',  ( 0.05279905671744906936, -0.3065870127357976926, 0.3541429396893026049 ) ) ;
#38272=CARTESIAN_POINT ( 'NONE',  ( -0.04946426091937417696, 0.4635716124040153985, 0.1136627969334571137 ) ) ;
#38283=DIRECTION ( 'NONE',  ( 1.654489825136719548E-31, -0.9510565162951568619, -0.3090169943749375703 ) ) ;
#38297=EDGE_CURVE ( 'NONE', #17796, #28034, #6955, .T. ) ;
#38300=CARTESIAN_POINT ( 'NONE',  ( -0.05634304521267748805, 1.092739197465705287E-15, 0.4588823192046724841 ) ) ;
#38305=EDGE_CURVE ( 'NONE', #9503, #8761, #26686, .T. ) ;
#38323=EDGE_CURVE ( 'NONE', #17036, #22774, #18125, .T. ) ;
#38334=VERTEX_POINT ( 'NONE', #34932 ) ;
#38340=CARTESIAN_POINT ( 'NONE',  ( 0.02242828275838944924, -0.2417645306140268069, -0.4517153736362903849 ) ) ;
#38347=CARTESIAN_POINT ( 'NONE',  ( 0.1499999999999993561, 1.639108796198557931E-15, -0.5500000000000003775 ) ) ;
#38354=CARTESIAN_POINT ( 'NONE',  ( -0.03642997641689344618, 0.3645929376994324067, -0.3593586258117690835 ) ) ;
#38357=TOROIDAL_SURFACE ( 'NONE', #24579, 0.5250000000000000222, 0.01499999999999999944 ) ;
#38363=CONICAL_SURFACE ( 'NONE', #33797, 0.5399999999999999245, 1.211529128687673262 ) ;
#38366=CARTESIAN_POINT ( 'NONE',  ( 0.04285640132274042002, 0.4433417433457765289, -0.2197472875419943517 ) ) ;
#38370=CARTESIAN_POINT ( 'NONE',  ( 0.01895494625228206706, -0.07381100255646662334, 0.5147985126481147145 ) ) ;
#38387=DIRECTION ( 'NONE',  ( 1.000000000000000000, 2.549619951388193009E-12, -4.473262954207831680E-13 ) ) ;
#38395=CIRCLE ( 'NONE', #31196, 0.01499999999999994567 ) ;
#38396=VERTEX_POINT ( 'NONE', #28770 ) ;
#38452=CARTESIAN_POINT ( 'NONE',  ( 0.03309060444528763578, 0.4608881774262347242, -0.2425132784556410515 ) ) ;
#38459=FACE_OUTER_BOUND ( 'NONE', #34906, .T. ) ;
#38469=CARTESIAN_POINT ( 'NONE',  ( -0.03674260963082394416, -0.4430101671189292656, 0.1867880763203681183 ) ) ;
#38479=CARTESIAN_POINT ( 'NONE',  ( 0.01548846960707524721, 0.4638115001430989648, -0.2459753896937820483 ) ) ;
#38483=CARTESIAN_POINT ( 'NONE',  ( 0.05634402396114598227, -0.2780622203583502650, 0.3651830615696499138 ) ) ;
#38489=AXIS2_PLACEMENT_3D ( 'NONE', #32419, #1195, #29354 ) ;
#38492=ORIENTED_EDGE ( 'NONE', *, *, #36090, .T. ) ;
#38523=CARTESIAN_POINT ( 'NONE',  ( 0.02953079040095704308, 0.3810518745593911571, 0.3687679460475725701 ) ) ;
#38525=CARTESIAN_POINT ( 'NONE',  ( 0.04230188431063419685, -0.4483687697007490147, -0.1365048020681091379 ) ) ;
#38546=CARTESIAN_POINT ( 'NONE',  ( -0.01548846960707524721, 0.2306506793134049660, -0.4716198300880325434 ) ) ;
#38551=FACE_OUTER_BOUND ( 'NONE', #28701, .T. ) ;
#38565=CARTESIAN_POINT ( 'NONE',  ( -0.04285561529641115919, 0.2295129201144932019, -0.4383679482630419288 ) ) ;
#38572=DIRECTION ( 'NONE',  ( 1.000000000000000000, 2.341930812374887555E-31, -1.664003471950578127E-31 ) ) ;
#38576=CARTESIAN_POINT ( 'NONE',  ( 0.02242828275838943536, 0.5043161982042990710, -0.09034400517546621601 ) ) ;
#38579=CARTESIAN_POINT ( 'NONE',  ( 0.03664605387828129973, -0.04106737781738728499, 0.4792329708773133135 ) ) ;
#38585=SPHERICAL_SURFACE ( 'NONE', #24583, 0.01499999999999999944 ) ;
#38587=ORIENTED_EDGE ( 'NONE', *, *, #20268, .F. ) ;
#38588=ADVANCED_FACE ( 'NONE', ( #1409 ), #11061, .F. ) ;
#38589=CARTESIAN_POINT ( 'NONE',  ( -0.03158843595483526445, -0.3316344853930296988, -0.3635668653053525934 ) ) ;
#38593=EDGE_CURVE ( 'NONE', #38334, #30207, #20782, .T. ) ;
#38595=DIRECTION ( 'NONE',  ( 1.702140497302369487E-12, 0.5877852522924830181, 0.8090169943749403458 ) ) ;
#38611=ORIENTED_EDGE ( 'NONE', *, *, #11422, .T. ) ;
#38614=ADVANCED_FACE ( 'NONE', ( #33055 ), #16699, .T. ) ;
#38617=CARTESIAN_POINT ( 'NONE',  ( -0.02953079040095693900, -0.2329676531120485339, -0.4763574306556319637 ) ) ;
#38626=CARTESIAN_POINT ( 'NONE',  ( 0.05279755784604189817, 0.3065965315811379766, 0.3541401437853790579 ) ) ;
#38648=EDGE_CURVE ( 'NONE', #29903, #6931, #3617, .T. ) ;
#38655=CARTESIAN_POINT ( 'NONE',  ( -0.04230188431063396093, -0.4483687697007506245, 0.1365048020681099428 ) ) ;
#38661=CARTESIAN_POINT ( 'NONE',  ( -0.03171893264489724501, -0.4702476704888112202, 0.2325692314475058253 ) ) ;
#38665=CARTESIAN_POINT ( 'NONE',  ( 0.01548846960712800709, -0.4730347584885825629, 0.2341461249029146152 ) ) ;
#38673=FACE_OUTER_BOUND ( 'NONE', #7409, .T. ) ;
#38674=FACE_OUTER_BOUND ( 'NONE', #8696, .T. ) ;
#38677=DIRECTION ( 'NONE',  ( 0.000000000000000000, -0.4393346272636243222, 0.8983234858819689750 ) ) ;
#38689=EDGE_CURVE ( 'NONE', #37319, #2531, #36534, .T. ) ;
#38696=CARTESIAN_POINT ( 'NONE',  ( -0.01548846960707531660, -0.4770632572900511681, -0.2530032579707427454 ) ) ;
#38697=VERTEX_POINT ( 'NONE', #29111 ) ;
#38711=CARTESIAN_POINT ( 'NONE',  ( -0.04582897286455953068, 0.06484386734940819630, 0.4825967645925812732 ) ) ;
#38713=CARTESIAN_POINT ( 'NONE',  ( 0.1399999999999994582, 8.414405049830459540E-17, 0.2526340763130724976 ) ) ;
#38714=DIRECTION ( 'NONE',  ( -0.9378410757839558132, 0.1072489841977658925, -0.3300784330442383396 ) ) ;
#38727=ORIENTED_EDGE ( 'NONE', *, *, #15467, .F. ) ;
#38728=DIRECTION ( 'NONE',  ( -1.000000000000000000, -2.280301054154495132E-31, 1.664003471950577689E-31 ) ) ;
#38737=EDGE_LOOP ( 'NONE', ( #39304, #34335, #27664 ) ) ;
#38753=CARTESIAN_POINT ( 'NONE',  ( -0.02881329448201560423, 0.2420398234037526297, -0.4354480552436177931 ) ) ;
#38754=CARTESIAN_POINT ( 'NONE',  ( -0.01548846960707427230, -0.5203207976467948415, -0.08861466064782426433 ) ) ;
#38755=CARTESIAN_POINT ( 'NONE',  ( -0.8248651029816859159, -8.267127619740731130E-16, -0.6154198107346400271 ) ) ;
#38765=CARTESIAN_POINT ( 'NONE',  ( 0.03158843595483464689, -0.3316344853930294212, 0.3635668653053538146 ) ) ;
#38766=DIRECTION ( 'NONE',  ( -1.355854680848614260E-31, 3.330669073875470114E-16, 1.000000000000000000 ) ) ;
#38768=ORIENTED_EDGE ( 'NONE', *, *, #23058, .F. ) ;
#38775=CARTESIAN_POINT ( 'NONE',  ( -0.01548846960721245516, -0.3688619771570368910, -0.3775276577325204497 ) ) ;
#38777=CARTESIAN_POINT ( 'NONE',  ( 0.03174060074382084595, 0.07585527192504755434, 0.5190439939302140537 ) ) ;
#38778=CARTESIAN_POINT ( 'NONE',  ( 0.03643058821097028971, -0.5061858935230133527, -0.07642520143595077364 ) ) ;
#38786=SPHERICAL_SURFACE ( 'NONE', #11908, 0.01499999999999999944 ) ;
#38800=CARTESIAN_POINT ( 'NONE',  ( 0.03171861681799757748, -0.5171399723077846344, 0.08825220573710579330 ) ) ;
#38801=CIRCLE ( 'NONE', #40128, 0.01500000000000002547 ) ;
#38812=CARTESIAN_POINT ( 'NONE',  ( 0.01548846960703782229, 0.3772621329472654605, -0.3651003739303476658 ) ) ;
#38813=DIRECTION ( 'NONE',  ( 0.000000000000000000, 3.330669073875470114E-16, 1.000000000000000000 ) ) ;
#38819=EDGE_CURVE ( 'NONE', #31970, #3242, #16844, .T. ) ;
#38821=CARTESIAN_POINT ( 'NONE',  ( -0.05082303569918696085, 0.4631054925596489458, -0.09932635337951989385 ) ) ;
#38824=DIRECTION ( 'NONE',  ( -1.000000000000000000, -2.280301054154495132E-31, 1.664003471950577689E-31 ) ) ;
#38827=CARTESIAN_POINT ( 'NONE',  ( -0.05279185365593383472, -0.3066183444142246417, 0.3541401447632906985 ) ) ;
#38836=FACE_OUTER_BOUND ( 'NONE', #7219, .T. ) ;
#38850=EDGE_LOOP ( 'NONE', ( #28082, #34703 ) ) ;
#38854=CARTESIAN_POINT ( 'NONE',  ( 0.04154009738085434611, 0.4523583096281919014, 0.1287716261385795091 ) ) ;
#38859=CARTESIAN_POINT ( 'NONE',  ( 0.01548846960712783535, -0.2450655194479442189, 0.4674710490748163472 ) ) ;
#38862=CARTESIAN_POINT ( 'NONE',  ( 0.1499999999999994948, -0.4770632572900429524, 0.2530032579707506835 ) ) ;
#38865=CARTESIAN_POINT ( 'NONE',  ( -0.06980746140711623082, -7.971802777789936683E-17, -0.1750000000000000167 ) ) ;
#38878=CARTESIAN_POINT ( 'NONE',  ( 0.01895884884825187189, -0.07380796352548207873, -0.5147901372834211564 ) ) ;
#38892=ORIENTED_EDGE ( 'NONE', *, *, #17491, .F. ) ;
#38898=CARTESIAN_POINT ( 'NONE',  ( 0.01548846960706641053, 0.4730347584886938073, 0.2341461249029914427 ) ) ;
#38902=CIRCLE ( 'NONE', #3429, 0.01500000000000006536 ) ;
#38905=ORIENTED_EDGE ( 'NONE', *, *, #10188, .F. ) ;
#38915=DIRECTION ( 'NONE',  ( 0.000000000000000000, 0.4393346272636334260, 0.8983234858819645341 ) ) ;
#38916=FACE_OUTER_BOUND ( 'NONE', #12394, .T. ) ;
#38919=( LENGTH_UNIT ( ) NAMED_UNIT ( * ) SI_UNIT ( $, .METRE. ) );
#38924=EDGE_CURVE ( 'NONE', #5913, #17036, #39576, .T. ) ;
#38930=VECTOR ( 'NONE', #16627, 39.37007874015748143 ) ;
#38932=CARTESIAN_POINT ( 'NONE',  ( -0.04230188431063486992, 0.4483687697007486817, -0.1365048020681075003 ) ) ;
#38941=ORIENTED_EDGE ( 'NONE', *, *, #18046, .T. ) ;
#38953=CARTESIAN_POINT ( 'NONE',  ( -0.05268850283020629077, 0.4471020566665069862, -0.1404229504685556851 ) ) ;
#38959=AXIS2_PLACEMENT_3D ( 'NONE', #11021, #11415, #30334 ) ;
#38982=CARTESIAN_POINT ( 'NONE',  ( 0.02869712619511914989, -0.06034133159975874766, 0.4947855140619932257 ) ) ;
#38983=CARTESIAN_POINT ( 'NONE',  ( -0.05489899477340663692, -0.2510719788555806353, -0.3887182106515197355 ) ) ;
#38995=AXIS2_PLACEMENT_3D ( 'NONE', #26192, #10538, #16924 ) ;
#38996=DIRECTION ( 'NONE',  ( 1.000000000000000000, 2.099003099963413025E-12, -1.419325098918985577E-12 ) ) ;
#38998=CARTESIAN_POINT ( 'NONE',  ( -0.01548846960707524721, 0.2372406987223596164, -0.4850946823762614102 ) ) ;
#39023=CARTESIAN_POINT ( 'NONE',  ( 0.02953079040095704308, -0.09152108205201929525, 0.5223162075576431862 ) ) ;
#39028=CARTESIAN_POINT ( 'NONE',  ( 0.04230188431063457155, -0.2825024449121523729, -0.3739792551055103331 ) ) ;
#39031=CARTESIAN_POINT ( 'NONE',  ( 0.1399999999999994582, 7.160938508832261116E-17, 0.2149999999999999967 ) ) ;
#39041=CARTESIAN_POINT ( 'NONE',  ( -0.03303708955568371991, -0.3731861634337418354, 0.3634708273687238256 ) ) ;
#39047=AXIS2_PLACEMENT_3D ( 'NONE', #22794, #28535, #38595 ) ;
#39055=VERTEX_POINT ( 'NONE', #36904 ) ;
#39057=EDGE_CURVE ( 'NONE', #28442, #11318, #16873, .T. ) ;
#39058=AXIS2_PLACEMENT_3D ( 'NONE', #33594, #2549, #33207 ) ;
#39061=CARTESIAN_POINT ( 'NONE',  ( -0.05634304521267748805, 1.092739197465705287E-15, 0.4588823192046724841 ) ) ;
#39064=AXIS2_PLACEMENT_3D ( 'NONE', #13333, #6744, #22408 ) ;
#39079=CARTESIAN_POINT ( 'NONE',  ( 0.05283719472145131241, 0.03966590960886431233, -0.4666299489511750997 ) ) ;
#39099=CARTESIAN_POINT ( 'NONE',  ( 0.03159140494780060537, -0.05458666898339327445, -0.4890560705835259592 ) ) ;
#39105=CIRCLE ( 'NONE', #3628, 0.01500000000000005843 ) ;
#39109=CIRCLE ( 'NONE', #26654, 0.01500000000000004802 ) ;
#39115=CARTESIAN_POINT ( 'NONE',  ( -0.03158843595483416811, -0.4819971762524441483, -0.09920191295803088005 ) ) ;
#39123=ORIENTED_EDGE ( 'NONE', *, *, #15523, .T. ) ;
#39126=AXIS2_PLACEMENT_3D ( 'NONE', #10698, #35200, #22877 ) ;
#39153=ORIENTED_EDGE ( 'NONE', *, *, #6663, .F. ) ;
#39166=VERTEX_POINT ( 'NONE', #3351 ) ;
#39170=CARTESIAN_POINT ( 'NONE',  ( -0.04087116408466956452, 0.4416914123362159494, -0.1656680454788639623 ) ) ;
#39181=EDGE_LOOP ( 'NONE', ( #5713, #27011, #11117, #26467 ) ) ;
#39183=CARTESIAN_POINT ( 'NONE',  ( 0.1499999999999996336, 0.09061086148575973886, 0.5171215251571029681 ) ) ;
#39187=CARTESIAN_POINT ( 'NONE',  ( -0.04308745346420585209, -0.4845670975328188468, -0.09763449863321065070 ) ) ;
#39199=DIRECTION ( 'NONE',  ( 2.686534417925915961E-31, -0.5877852522924640333, 0.8090169943749540016 ) ) ;
#39201=CARTESIAN_POINT ( 'NONE',  ( -0.01899468245562016197, -0.2428515268394236259, -0.4597785848521230290 ) ) ;
#39210=CARTESIAN_POINT ( 'NONE',  ( 0.04582889109739184119, 0.2312034125369037685, 0.4285435303321080691 ) ) ;
#39222=ORIENTED_EDGE ( 'NONE', *, *, #14046, .T. ) ;
#39234=CARTESIAN_POINT ( 'NONE',  ( 0.03674078017396374685, -0.4681991728402142283, 0.1092756390057521149 ) ) ;
#39240=CARTESIAN_POINT ( 'NONE',  ( 0.04229956186878609803, -0.2683474741743136494, -0.3842687663629391626 ) ) ;
#39242=FACE_OUTER_BOUND ( 'NONE', #32071, .T. ) ;
#39245=CARTESIAN_POINT ( 'NONE',  ( -0.05561176441985838520, 0.4442366066780379374, -0.1229089882096660452 ) ) ;
#39250=CARTESIAN_POINT ( 'NONE',  ( -0.04574984450155204774, -0.3363984555176520175, 0.3523422282978331266 ) ) ;
#39256=DIRECTION ( 'NONE',  ( 1.386669559958804888E-32, 0.8983234858819696411, 0.4393346272636231564 ) ) ;
#39257=CARTESIAN_POINT ( 'NONE',  ( 0.02238826743733597635, 0.2417677220642130975, -0.4518145715460058498 ) ) ;
#39263=CARTESIAN_POINT ( 'NONE',  ( 0.05083665881509014800, 0.4630607685881601987, -0.09936361682460806422 ) ) ;
#39265=CARTESIAN_POINT ( 'NONE',  ( 0.01548846960706664298, -0.2306506793134169842, -0.4716198300880524719 ) ) ;
#39269=LINE ( 'NONE', #30205, #5002 ) ;
#39274=CARTESIAN_POINT ( 'NONE',  ( 0.03159140494780057068, 0.4819881711443544936, 0.09921162977303653319 ) ) ;
#39282=CARTESIAN_POINT ( 'NONE',  ( 0.03654364704248852513, 0.4542255574219836167, 0.2354487068768196523 ) ) ;
#39304=ORIENTED_EDGE ( 'NONE', *, *, #11512, .T. ) ;
#39309=CARTESIAN_POINT ( 'NONE',  ( -0.03159140494780089681, -0.4482517543799761084, -0.2030416442520474596 ) ) ;
#39355=ORIENTED_EDGE ( 'NONE', *, *, #32264, .F. ) ;
#39359=CARTESIAN_POINT ( 'NONE',  ( -0.1499999999999996336, -2.632527843410151989E-17, -0.1250000000000000000 ) ) ;
#39361=CARTESIAN_POINT ( 'NONE',  ( -0.05187277790672228939, 0.4419080096627327481, -0.1624279055868658173 ) ) ;
#39387=FACE_OUTER_BOUND ( 'NONE', #6006, .T. ) ;
#39389=CARTESIAN_POINT ( 'NONE',  ( -0.03672309138969661463, -0.2485858928251903077, -0.4115746274616722267 ) ) ;
#39398=CARTESIAN_POINT ( 'NONE',  ( 0.02953079040095491978, 0.09152108205202105773, 0.5223162075576462948 ) ) ;
#39401=CARTESIAN_POINT ( 'NONE',  ( 0.02953079040095717839, 0.4684706630666118365, 0.2484463060367366194 ) ) ;
#39405=CARTESIAN_POINT ( 'NONE',  ( -0.05283102792148800658, -0.2421768296208681170, -0.4008516595826048245 ) ) ;
#39421=CARTESIAN_POINT ( 'NONE',  ( 0.05634402396114423367, -0.4396062797411974254, 0.1319984305213770803 ) ) ;
#39426=DIRECTION ( 'NONE',  ( -1.000000000000000000, -2.280301054154495132E-31, 1.664003471950577689E-31 ) ) ;
#39442=CARTESIAN_POINT ( 'NONE',  ( -0.04211812644076929485, -0.2687274166943736664, 0.3844079338164319570 ) ) ;
#39447=DIRECTION ( 'NONE',  ( -0.9378410757839555911, 0.2807814858886595322, -0.2039996905746409572 ) ) ;
#39449=CARTESIAN_POINT ( 'NONE',  ( -0.04293701532779589658, 0.4432143466407589272, 0.2195216604697213802 ) ) ;
#39450=EDGE_LOOP ( 'NONE', ( #23654, #35220, #19592 ) ) ;
#39461=CARTESIAN_POINT ( 'NONE',  ( -0.1499999999999996336, 0.000000000000000000, 0.000000000000000000 ) ) ;
#39471=DIRECTION ( 'NONE',  ( 0.3468893892380805477, -0.2594111197900994537, -0.9013177145509114752 ) ) ;
#39472=CARTESIAN_POINT ( 'NONE',  ( 0.04582889109739231304, 0.4389390569944019438, 0.2108010426992244501 ) ) ;
#39480=AXIS2_PLACEMENT_3D ( 'NONE', #24238, #12479, #27720 ) ;
#39486=CARTESIAN_POINT ( 'NONE',  ( 0.02869942827333498564, -0.06034320897027730529, -0.4947801815387851132 ) ) ;
#39489=DIRECTION ( 'NONE',  ( 2.532366176626896502E-12, 1.000000000000000000, 5.691349986800531115E-16 ) ) ;
#39499=CARTESIAN_POINT ( 'NONE',  ( -0.04230188431063475890, -0.4429734639576313193, -0.1531098457317282835 ) ) ;
#39505=EDGE_LOOP ( 'NONE', ( #26448, #20878, #3482, #24975, #6163 ) ) ;
#39510=CIRCLE ( 'NONE', #21798, 0.1249999999999999584 ) ;
#39530=CARTESIAN_POINT ( 'NONE',  ( 0.03174060074381680058, -0.07585527192505218952, -0.5190439939302199379 ) ) ;
#39533=ORIENTED_EDGE ( 'NONE', *, *, #26487, .T. ) ;
#39535=CIRCLE ( 'NONE', #33643, 0.01499999999999995087 ) ;
#39538=ORIENTED_EDGE ( 'NONE', *, *, #12510, .T. ) ;
#39545=CYLINDRICAL_SURFACE ( 'NONE', #29621, 0.01500000000000004628 ) ;
#39548=CARTESIAN_POINT ( 'NONE',  ( -0.04308745346420850275, 0.4494111352305566465, -0.2058334250444009417 ) ) ;
#39567=AXIS2_PLACEMENT_3D ( 'NONE', #9833, #6740, #19520 ) ;
#39570=CARTESIAN_POINT ( 'NONE',  ( -0.05186792262757027039, -0.4419037732007360386, -0.1624768558011068786 ) ) ;
#39576=LINE ( 'NONE', #23979, #28030 ) ;
#39577=CIRCLE ( 'NONE', #33677, 0.01500000000000002894 ) ;
#39583=CARTESIAN_POINT ( 'NONE',  ( -0.04293324258486902467, -0.07181764475132905445, -0.4893676133895085156 ) ) ;
#39593=AXIS2_PLACEMENT_3D ( 'NONE', #11764, #13490, #29330 ) ;
#39602=CARTESIAN_POINT ( 'NONE',  ( 0.02872242845530344549, -0.3729171224323687417, -0.3802687114177517036 ) ) ;
#39607=EDGE_CURVE ( 'NONE', #4682, #25917, #5692, .T. ) ;
#39639=CARTESIAN_POINT ( 'NONE',  ( -0.05634307799789459864, 0.4395998308137155086, -0.1320249839695989136 ) ) ;
#39647=ORIENTED_EDGE ( 'NONE', *, *, #38305, .T. ) ;
#39653=CARTESIAN_POINT ( 'NONE',  ( -0.03309060444528683087, 0.4608881774262392206, 0.2425132784556342513 ) ) ;
#39659=DIRECTION ( 'NONE',  ( 0.000000000000000000, 3.330669073875470114E-16, 1.000000000000000000 ) ) ;
#39667=ORIENTED_EDGE ( 'NONE', *, *, #13739, .F. ) ;
#39672=AXIS2_PLACEMENT_3D ( 'NONE', #6576, #12562, #15857 ) ;
#39680=DIRECTION ( 'NONE',  ( -1.000000000000000000, -2.280301054154495132E-31, 1.664003471950577689E-31 ) ) ;
#39683=EDGE_CURVE ( 'NONE', #13008, #37512, #26105, .T. ) ;
#39687=CARTESIAN_POINT ( 'NONE',  ( 0.04230188431063326704, -0.4429734639576344279, 0.1531098457317283112 ) ) ;
#39697=CIRCLE ( 'NONE', #31203, 0.01499999999999995608 ) ;
#39698=ORIENTED_EDGE ( 'NONE', *, *, #16281, .F. ) ;
#39700=CIRCLE ( 'NONE', #6834, 0.01499999999999999077 ) ;
#39723=AXIS2_PLACEMENT_3D ( 'NONE', #33896, #18872, #19065 ) ;
#39731=DIRECTION ( 'NONE',  ( 1.000000000000000000, 0.000000000000000000, 0.000000000000000000 ) ) ;
#39739=CARTESIAN_POINT ( 'NONE',  ( 0.01548846960712814240, 0.2450655194479464116, -0.4674710490748144043 ) ) ;
#39778=ORIENTED_EDGE ( 'NONE', *, *, #4117, .F. ) ;
#39793=DIRECTION ( 'NONE',  ( -1.000000000000000000, -2.341930812374887555E-31, 1.664003471950578127E-31 ) ) ;
#39794=ORIENTED_EDGE ( 'NONE', *, *, #12996, .T. ) ;
#39797=DIRECTION ( 'NONE',  ( 1.000000000000000000, 0.000000000000000000, 0.000000000000000000 ) ) ;
#39806=CARTESIAN_POINT ( 'NONE',  ( -0.04229883635638087558, 0.004358580242005115520, -0.4686119955506233281 ) ) ;
#39813=CARTESIAN_POINT ( 'NONE',  ( 0.05268932808079770241, -0.4484995728561511075, -0.1361157601095852043 ) ) ;
#39816=CARTESIAN_POINT ( 'NONE',  ( 0.04047076529492525665, 0.4923674059679383208, 0.09402950075401000918 ) ) ;
#39825=ADVANCED_FACE ( 'NONE', ( #1599 ), #23610, .T. ) ;
#39836=DIRECTION ( 'NONE',  ( -5.879757087911781259E-34, -0.5877852522924815748, -0.8090169943749412340 ) ) ;
#39839=CARTESIAN_POINT ( 'NONE',  ( -0.01548846960707524721, -0.4770632572900429524, 0.2530032579707506835 ) ) ;
#39847=CARTESIAN_POINT ( 'NONE',  ( 0.03647060353175536618, 0.2291014149038373693, 0.4576769917029342993 ) ) ;
#39864=CARTESIAN_POINT ( 'NONE',  ( -0.05283102792148818005, 0.3063958269170702353, -0.3541938269410517259 ) ) ;
#39873=CARTESIAN_POINT ( 'NONE',  ( -0.03868649100028186127, 0.2522293598345317633, -0.4043344736883373036 ) ) ;
#39881=ORIENTED_EDGE ( 'NONE', *, *, #20846, .F. ) ;
#39882=VERTEX_POINT ( 'NONE', #38713 ) ;
#39885=CARTESIAN_POINT ( 'NONE',  ( 0.000000000000000000, 0.000000000000000000, 0.000000000000000000 ) ) ;
#39892=CARTESIAN_POINT ( 'NONE',  ( 0.05083665881508978718, 0.4330284998000944463, 0.1917934360576652730 ) ) ;
#39897=CARTESIAN_POINT ( 'NONE',  ( 0.01548846960721225047, -0.5203207976464844231, 0.08861466064783186936 ) ) ;
#39898=DIRECTION ( 'NONE',  ( 1.702140497302374535E-12, 0.000000000000000000, -1.000000000000000000 ) ) ;
#39902=EDGE_CURVE ( 'NONE', #36780, #13108, #10052, .T. ) ;
#39907=ORIENTED_EDGE ( 'NONE', *, *, #23752, .T. ) ;
#39926=DIRECTION ( 'NONE',  ( -1.000000000000000000, -2.280301054154495132E-31, 1.664003471950577689E-31 ) ) ;
#39950=CARTESIAN_POINT ( 'NONE',  ( 0.03301162916267656733, 0.08829475514027847194, -0.5134720893088496885 ) ) ;
#39966=CARTESIAN_POINT ( 'NONE',  ( -0.05078493045284175611, 0.4330747843660931462, -0.1920285438095961916 ) ) ;
#39976=CARTESIAN_POINT ( 'NONE',  ( 0.1499999999999994948, 0.3880410510314791783, 0.3755318131854940567 ) ) ;
#39990=CARTESIAN_POINT ( 'NONE',  ( -0.03171102739523560393, -0.3312744048890958193, -0.3635303745205933357 ) ) ;
#39996=CARTESIAN_POINT ( 'NONE',  ( -0.03877220711930245978, -0.03321538116298394100, -0.4752084053751546855 ) ) ;
#40000=CARTESIAN_POINT ( 'NONE',  ( -0.03662792686184391383, 0.2484399233013421804, 0.4119056456069879468 ) ) ;
#40001=CARTESIAN_POINT ( 'NONE',  ( 0.01896931156525286447, -0.07379981600433808964, 0.5147676832640479816 ) ) ;
#40002=CARTESIAN_POINT ( 'NONE',  ( 0.05561375719525332717, -0.4442396019574900712, -0.1228845301467967194 ) ) ;
#40005=CARTESIAN_POINT ( 'NONE',  ( 0.02238765564325780749, 0.5044129532808500072, 0.09031612285224414893 ) ) ;
#40015=CARTESIAN_POINT ( 'NONE',  ( -0.02953079040095700838, 0.000000000000000000, 0.000000000000000000 ) ) ;
#40016=CARTESIAN_POINT ( 'NONE',  ( -0.08978098643734171158, -7.148474850891705974E-16, -0.3698489655878013371 ) ) ;
#40024=CARTESIAN_POINT ( 'NONE',  ( -0.03664605387828157035, 0.4684681574363449008, 0.1090337349854993559 ) ) ;
#40027=B_SPLINE_CURVE_WITH_KNOTS ( 'NONE', 3,
 ( #16982, #38370, #35298, #38982, #589, #38579, #10398, #22563, #35481, #25638, #26446, #19268, #23389, #16788, #1181, #31808, #3623, #16188 ),
 .UNSPECIFIED., .F., .F.,
 ( 4, 2, 2, 2, 2, 2, 2, 2, 4 ),
 ( 0.0003425652276237324957, 0.001007165397454245050, 0.001671765567284757767, 0.002336365737115270267, 0.003000965906945782767, 0.003665566076776295267, 0.004330166246606808635, 0.004994766416437320701, 0.005659366586267833635 ),
 .UNSPECIFIED. ) ;
#40030=CARTESIAN_POINT ( 'NONE',  ( -0.03478556507500542988, 0.3590471004907105912, 0.3712136264428257948 ) ) ;
#40057=CARTESIAN_POINT ( 'NONE',  ( -0.01548846960721238578, 0.2450655194478933985, -0.4674710490746305513 ) ) ;
#40068=ADVANCED_FACE ( 'NONE', ( #17528 ), #12713, .T. ) ;
#40078=FACE_OUTER_BOUND ( 'NONE', #31565, .T. ) ;
#40082=CARTESIAN_POINT ( 'NONE',  ( 0.02231181081520441575, -0.4612879682509028467, 0.2235517164227180942 ) ) ;
#40098=ORIENTED_EDGE ( 'NONE', *, *, #4969, .T. ) ;
#40099=ADVANCED_FACE ( 'NONE', ( #32043 ), #21874, .F. ) ;
#40102=DIRECTION ( 'NONE',  ( -2.686534417925922091E-31, 0.5877852522924700285, -0.8090169943749496717 ) ) ;
#40115=CARTESIAN_POINT ( 'NONE',  ( -0.03174036153403787114, -0.5170813853140128202, 0.08825077997795215123 ) ) ;
#40128=AXIS2_PLACEMENT_3D ( 'NONE', #25923, #29190, #28974 ) ;
#40133=CIRCLE ( 'NONE', #15829, 0.01500000000000002373 ) ;
#40142=CARTESIAN_POINT ( 'NONE',  ( 0.04285640132274089187, -0.07199195674533706568, -0.4895487002729275727 ) ) ;
#40145=CARTESIAN_POINT ( 'NONE',  ( -0.1499999999999996336, 5.828670879282072084E-17, 0.1749999999999999889 ) ) ;
#40151=CIRCLE ( 'NONE', #32933, 0.01499999999999996649 ) ;
#40156=AXIS2_PLACEMENT_3D ( 'NONE', #20869, #21054, #33390 ) ;
#40168=CARTESIAN_POINT ( 'NONE',  ( -0.03650581953630603615, -0.3643937567481967954, 0.3592734714612051961 ) ) ;
#40186=AXIS2_PLACEMENT_3D ( 'NONE', #22680, #19765, #28830 ) ;
#40191=DIRECTION ( 'NONE',  ( -0.9378410757839558132, 0.3470650033817761493, 0.000000000000000000 ) ) ;
#40194=CARTESIAN_POINT ( 'NONE',  ( -0.03474824846560015112, -0.3591470389155407283, 0.3712557345097503569 ) ) ;
#40195=CARTESIAN_POINT ( 'NONE',  ( -0.01548846960721259221, -0.2450655194478906784, 0.4674710490746316616 ) ) ;
#40197=CARTESIAN_POINT ( 'NONE',  ( -0.02242905165738916587, -0.06991915049797610415, -0.5075494376218483428 ) ) ;
#40199=ORIENTED_EDGE ( 'NONE', *, *, #9781, .T. ) ;
#40203=CARTESIAN_POINT ( 'NONE',  ( 0.03875673594170444408, -0.4416908594619144979, -0.1785163973046066388 ) ) ;
#40212=VERTEX_POINT ( 'NONE', #38617 ) ;
#40213=CIRCLE ( 'NONE', #15261, 0.1749999999999999889 ) ;
#40219=FACE_OUTER_BOUND ( 'NONE', #18462, .T. ) ;
#40229=DIRECTION ( 'NONE',  ( -1.000000000000000000, -2.280301054154495132E-31, 1.664003471950577689E-31 ) ) ;
#40234=( BOUNDED_SURFACE ( )  B_SPLINE_SURFACE ( 3, 2, ( 
 ( #6381, #18524, #34154 ),
 ( #37653, #40115, #5965 ),
 ( #3106, #31485, #5772 ),
 ( #22049, #27405, #34577 ),
 ( #24917, #18949, #18327 ),
 ( #5564, #3292, #27795 ),
 ( #40539, #18127, #33969 ),
 ( #36829, #31079, #2901 ),
 ( #11747, #15451, #24304 ),
 ( #30682, #2498, #11946 ),
 ( #8642, #24509, #28004 ),
 ( #40329, #12361, #15649 ),
 ( #37444, #37041, #28198 ),
 ( #15235, #21442, #30873 ),
 ( #2691, #9255, #12159 ),
 ( #21833, #6174, #18743 ),
 ( #38469, #13156, #482 ),
 ( #3508, #12766, #26147 ),
 ( #32483, #12977, #38253 ),
 ( #3716, #15847, #16064 ),
 ( #6991, #38661, #22249 ),
 ( #16456, #25327, #10083 ) ),
 .UNSPECIFIED., .F., .F., .F. ) 
 B_SPLINE_SURFACE_WITH_KNOTS ( ( 4, 2, 2, 2, 2, 2, 2, 2, 2, 2, 4 ),
 ( 3, 3 ),
 ( 0.002013519961495850458, 0.002780892266055759107, 0.003548264570615668190, 0.004315636875175577272, 0.004699323027455531814, 0.005083009179735486355, 0.005466695332015440896, 0.005850381484295395437, 0.006617753788855304520, 0.007385126093415213602, 0.008152498397975122685 ),
 ( 0.000000000000000000, 1.000000000000000000 ),
 .UNSPECIFIED. ) 
 GEOMETRIC_REPRESENTATION_ITEM ( )  RATIONAL_B_SPLINE_SURFACE ( (
 ( 1.000000000000000000, 0.7283825911960394306, 1.000000000000000000),
 ( 1.000000000000000000, 0.7404375345927917129, 1.000000000000000000),
 ( 1.000000000000000000, 0.7521483142434843838, 1.000000000000000000),
 ( 1.000000000000000000, 0.7744460733777613903, 1.000000000000000000),
 ( 1.000000000000000000, 0.7845612039381936187, 1.000000000000000000),
 ( 1.000000000000000000, 0.8022035258262242285, 1.000000000000000000),
 ( 1.000000000000000000, 0.8093965293321873089, 1.000000000000000000),
 ( 1.000000000000000000, 0.8169028692725408547, 1.000000000000000000),
 ( 1.000000000000000000, 0.8188329634862903106, 1.000000000000000000),
 ( 1.000000000000000000, 0.8214004505364509434, 1.000000000000000000),
 ( 1.000000000000000000, 0.8220602406260716366, 1.000000000000000000),
 ( 1.000000000000000000, 0.8220736605435879918, 1.000000000000000000),
 ( 1.000000000000000000, 0.8214126668415060450, 1.000000000000000000),
 ( 1.000000000000000000, 0.8188520474558917961, 1.000000000000000000),
 ( 1.000000000000000000, 0.8169545908334260309, 1.000000000000000000),
 ( 1.000000000000000000, 0.8094771004219962762, 1.000000000000000000),
 ( 1.000000000000000000, 0.8022723753805990343, 1.000000000000000000),
 ( 1.000000000000000000, 0.7845733350638980363, 1.000000000000000000),
 ( 1.000000000000000000, 0.7744472902492880451, 1.000000000000000000),
 ( 1.000000000000000000, 0.7522916829163881491, 1.000000000000000000),
 ( 1.000000000000000000, 0.7403553004665528459, 1.000000000000000000),
 ( 1.000000000000000000, 0.7283825911960415400, 1.000000000000000000) ) ) 
 REPRESENTATION_ITEM ( '' )  SURFACE ( )  );
#40235=CARTESIAN_POINT ( 'NONE',  ( -0.05634115714581192091, 0.2655021207500444236, 0.3743162705049740135 ) ) ;
#40242=CARTESIAN_POINT ( 'NONE',  ( 0.1499999999999996336, -0.2372406987223574237, 0.4850946823762633531 ) ) ;
#40257=CARTESIAN_POINT ( 'NONE',  ( 0.05561375719525540190, 0.2541477197272165589, -0.3845235600768820428 ) ) ;
#40288=CIRCLE ( 'NONE', #6781, 0.5302738246768101682 ) ;
#40301=EDGE_CURVE ( 'NONE', #14410, #10166, #39577, .T. ) ;
#40302=ORIENTED_EDGE ( 'NONE', *, *, #15770, .T. ) ;
#40319=AXIS2_PLACEMENT_3D ( 'NONE', #27673, #1696, #10515 ) ;
#40329=CARTESIAN_POINT ( 'NONE',  ( -0.04230258372739791051, -0.4443637212174513795, 0.1488268768076328463 ) ) ;
#40332=CARTESIAN_POINT ( 'NONE',  ( -0.01548846960707477016, 0.4770632572900484480, 0.2530032579707400253 ) ) ;
#40346=VECTOR ( 'NONE', #19477, 39.37007874015748143 ) ;
#40352=CARTESIAN_POINT ( 'NONE',  ( 0.03875673594170000319, 0.03328920108827214397, -0.4752375706209732154 ) ) ;
#40363=ORIENTED_EDGE ( 'NONE', *, *, #40593, .F. ) ;
#40367=ORIENTED_EDGE ( 'NONE', *, *, #22268, .F. ) ;
#40374=DIRECTION ( 'NONE',  ( -1.000000000000000000, -2.341930812374887555E-31, 1.664003471950578127E-31 ) ) ;
#40390=DIRECTION ( 'NONE',  ( 0.000000000000000000, 0.5877852522924367218, -0.8090169943749738746 ) ) ;
#40391=CARTESIAN_POINT ( 'NONE',  ( 0.02953079040095690777, -0.4684706630666085614, 0.2484463060367459175 ) ) ;
#40405=CARTESIAN_POINT ( 'NONE',  ( -0.03171893264489181880, -0.3665010048041572599, -0.3753642664050083066 ) ) ;
#40413=CARTESIAN_POINT ( 'NONE',  ( -0.03171893264488560849, -0.07587196131163935486, -0.5190999561769865656 ) ) ;
#40418=CARTESIAN_POINT ( 'NONE',  ( 0.02872242845529804703, -0.07817994906157445245, 0.5268390348591310834 ) ) ;
#40422=CARTESIAN_POINT ( 'NONE',  ( 0.03170752374382720951, 0.4816921673044493035, 0.09938322573836459728 ) ) ;
#40425=B_SPLINE_CURVE_WITH_KNOTS ( 'NONE', 3,
 ( #11330, #33525, #26966, #7824, #39115, #20606, #20395, #33334, #20816, #39499, #8632, #5143, #8439, #39309, #14830, #36428, #32923, #4733 ),
 .UNSPECIFIED., .F., .F.,
 ( 4, 2, 2, 2, 2, 2, 2, 2, 4 ),
 ( -0.002633528389679640983, -0.001975271857855670846, -0.001317015326031701142, -0.0006587587942077310042, -5.022623837613003628E-07, 0.0006577542694402084035, 0.001316010801264178975, 0.001974267333088148679, 0.002632523864912118382 ),
 .UNSPECIFIED. ) ;
#40427=AXIS2_PLACEMENT_3D ( 'NONE', #26104, #19515, #16829 ) ;
#40429=ORIENTED_EDGE ( 'NONE', *, *, #32958, .F. ) ;
#40430=FACE_OUTER_BOUND ( 'NONE', #19063, .T. ) ;
#40435=CARTESIAN_POINT ( 'NONE',  ( 0.01548846960707306146, 0.2306506793133153710, 0.4716198300880833916 ) ) ;
#40441=ADVANCED_FACE ( 'NONE', ( #3401 ), #579, .T. ) ;
#40447=CARTESIAN_POINT ( 'NONE',  ( -0.01895884884825297517, 0.4667865995382938227, 0.2292744456225711547 ) ) ;
#40452=CARTESIAN_POINT ( 'NONE',  ( -0.02953079040095600918, 0.2329676531120531691, 0.4763574306556323523 ) ) ;
#40464=LINE ( 'NONE', #18443, #8158 ) ;
#40474=CARTESIAN_POINT ( 'NONE',  ( 0.05201782277453608633, 0.2909620873304535893, -0.3697179445082223181 ) ) ;
#40482=ORIENTED_EDGE ( 'NONE', *, *, #32260, .F. ) ;
#40489=ORIENTED_EDGE ( 'NONE', *, *, #16187, .T. ) ;
#40494=CARTESIAN_POINT ( 'NONE',  ( 0.02953079040095687308, 0.09152108205202039160, -0.5223162075576429642 ) ) ;
#40510=DIRECTION ( 'NONE',  ( 8.628166150854818811E-32, -0.1402348365093016580, -0.9901182710308954471 ) ) ;
#40522=CARTESIAN_POINT ( 'NONE',  ( -0.03654364704248874718, -0.5058694728073482860, -0.07650507870001360677 ) ) ;
#40526=AXIS2_PLACEMENT_3D ( 'NONE', #4844, #32430, #13904 ) ;
#40532=CARTESIAN_POINT ( 'NONE',  ( -0.01548846960721252282, -0.4730347584884301293, 0.2341461249027971259 ) ) ;
#40539=CARTESIAN_POINT ( 'NONE',  ( -0.03874953289575334275, -0.4622846869243766310, 0.1151793484519262750 ) ) ;
#40551=CARTESIAN_POINT ( 'NONE',  ( 0.02953079040095489896, -0.2329676531120505323, 0.4763574306556353499 ) ) ;
#40558=CARTESIAN_POINT ( 'NONE',  ( 0.05562144613422614903, -0.2870684680408724931, 0.3605846877396505223 ) ) ;
#40569=ORIENTED_EDGE ( 'NONE', *, *, #15503, .T. ) ;
#40573=FACE_OUTER_BOUND ( 'NONE', #21354, .T. ) ;
#40583=ORIENTED_EDGE ( 'NONE', *, *, #12396, .F. ) ;
#40589=CARTESIAN_POINT ( 'NONE',  ( 0.05283710938261019369, -0.4560492058803811144, 0.1064717188025609967 ) ) ;
#40591=ADVANCED_FACE ( 'NONE', ( #15744 ), #20189, .T. ) ;
#40593=EDGE_CURVE ( 'NONE', #28482, #16052, #26848, .T. ) ;
#40601=ORIENTED_EDGE ( 'NONE', *, *, #5765, .T. ) ;
#40604=CARTESIAN_POINT ( 'NONE',  ( -0.04285534776242042043, -0.07199417564834888206, 0.4895512033229395543 ) ) ;
#40608=LINE ( 'NONE', #27872, #18398 ) ;
#40611=CARTESIAN_POINT ( 'NONE',  ( -0.05281452789367557105, -0.03978571835446843147, -0.4666805157975096874 ) ) ;
#40615=CARTESIAN_POINT ( 'NONE',  ( -0.01548846960707545191, -0.5346638663566677385, -0.07572681171513533094 ) ) ;
#40621=CARTESIAN_POINT ( 'NONE',  ( 0.05561375719525302880, -0.2871676730027881153, -0.3605331597494366713 ) ) ;
#40625=ORIENTED_EDGE ( 'NONE', *, *, #36892, .F. ) ;
#40628=CARTESIAN_POINT ( 'NONE',  ( -0.05082303569918699554, -0.4631054925596483351, 0.09932635337952169796 ) ) ;
#40629=LINE ( 'NONE', #28491, #18270 ) ;
#40632=CARTESIAN_POINT ( 'NONE',  ( -0.01548846960712817709, -0.4730347584885852830, -0.2341461249029094249 ) ) ;
#40636=CARTESIAN_POINT ( 'NONE',  ( -0.01548846960707418556, 0.3688619771572939632, -0.3775276577326990290 ) ) ;
#40642=DIRECTION ( 'NONE',  ( -2.563099466555627715E-12, 0.000000000000000000, 1.000000000000000000 ) ) ;
#40643=ADVANCED_FACE ( 'NONE', ( #6020 ), #37301, .T. ) ;
#40645=CARTESIAN_POINT ( 'NONE',  ( -0.02242905165739062651, 0.3548958552285692569, 0.3695186750059857306 ) ) ;
#40647=CARTESIAN_POINT ( 'NONE',  ( 0.05269111014006346017, 0.2828051265736298281, -0.3737594984297845646 ) ) ;
#40681=COLOUR_RGB('Sky Blue',0.24,0.69,0.87);
#40682=FILL_AREA_STYLE_COLOUR('',#40681);
#40683=FILL_AREA_STYLE('',(#40682));
#40684=SURFACE_STYLE_FILL_AREA(#40683);
#40685=SURFACE_SIDE_STYLE('',(#40684));
#40686=SURFACE_STYLE_USAGE(.BOTH.,#40685);
#40687=PRESENTATION_STYLE_ASSIGNMENT((#40686));
#40719=STYLED_ITEM('',(#40687),#18435);
#40721=MECHANICAL_DESIGN_GEOMETRIC_PRESENTATION_REPRESENTATION('',(#40719),#11399);
ENDSEC;
END-ISO-10303-21;
